ISO-10303-21;
HEADER;
FILE_DESCRIPTION (('STEP AP214'),
    '1' );
FILE_NAME ('internal spur gear_iso_ISO - Internal spur gear 2M 90T 20PA 10FW ---S90S200OD 1.0AF.step',
    '2026-09-30T13:58:28',
    ( '' ),
    ( '' ),
    'SwSTEP 2.0',
    'SolidWorks 2026',
    '' );
FILE_SCHEMA (( 'AUTOMOTIVE_DESIGN' ));
ENDSEC;

DATA;
#1=VERTEX_POINT ( 'NONE', #11430 ) ;
#2=DIRECTION ( 'NONE',  ( 1.000000000000000000, 0.000000000000000000, 0.000000000000000000 ) ) ;
#4=CARTESIAN_POINT ( 'NONE',  ( 10.00000000000000000, -41.21966518005896774, -82.80926399530329718 ) ) ;
#6=EDGE_CURVE ( 'NONE', #10604, #16693, #2923, .T. ) ;
#7=EDGE_CURVE ( 'NONE', #1807, #19086, #14294, .T. ) ;
#9=EDGE_CURVE ( 'NONE', #17849, #4256, #16629, .T. ) ;
#11=DIRECTION ( 'NONE',  ( -1.000000000000000000, 0.000000000000000000, 0.000000000000000000 ) ) ;
#13=FACE_OUTER_BOUND ( 'NONE', #21140, .T. ) ;
#14=CARTESIAN_POINT ( 'NONE',  ( 10.00000000000000000, 10.41137886060228901, -91.91321010181836471 ) ) ;
#17=EDGE_CURVE ( 'NONE', #14755, #17637, #4430, .T. ) ;
#18=ORIENTED_EDGE ( 'NONE', *, *, #6903, .T. ) ;
#20=ADVANCED_FACE ( 'NONE', ( #18069 ), #19725, .F. ) ;
#21=CYLINDRICAL_SURFACE ( 'NONE', #38, 45.00000000000000000 ) ;
#22=ORIENTED_EDGE ( 'NONE', *, *, #21258, .T. ) ;
#25=ORIENTED_EDGE ( 'NONE', *, *, #3908, .T. ) ;
#32=DIRECTION ( 'NONE',  ( 0.000000000000000000, 0.000000000000000000, -1.000000000000000000 ) ) ;
#33=LINE ( 'NONE', #6780, #6309 ) ;
#34=CARTESIAN_POINT ( 'NONE',  ( 0.000000000000000000, -19.83954325428713972, 82.71385593638686373 ) ) ;
#36=CARTESIAN_POINT ( 'NONE',  ( 10.00000000000000000, 29.47587714451147534, -82.91666097089093057 ) ) ;
#38=AXIS2_PLACEMENT_3D ( 'NONE', #6766, #13480, #9727 ) ;
#41=EDGE_CURVE ( 'NONE', #15664, #20418, #3042, .T. ) ;
#42=DIRECTION ( 'NONE',  ( 0.000000000000000000, 0.000000000000000000, 1.000000000000000000 ) ) ;
#43=DIRECTION ( 'NONE',  ( -1.000000000000000000, 0.000000000000000000, 0.000000000000000000 ) ) ;
#45=EDGE_CURVE ( 'NONE', #3976, #18093, #12185, .T. ) ;
#46=DIRECTION ( 'NONE',  ( -1.000000000000000000, -0.000000000000000000, -0.000000000000000000 ) ) ;
#47=EDGE_LOOP ( 'NONE', ( #15509, #8289, #2794, #20756 ) ) ;
#48=EDGE_CURVE ( 'NONE', #21500, #20174, #21008, .T. ) ;
#49=VERTEX_POINT ( 'NONE', #8229 ) ;
#52=VERTEX_POINT ( 'NONE', #11320 ) ;
#53=DIRECTION ( 'NONE',  ( -1.000000000000000000, 0.000000000000000000, -0.000000000000000000 ) ) ;
#55=ORIENTED_EDGE ( 'NONE', *, *, #20082, .T. ) ;
#56=EDGE_CURVE ( 'NONE', #13601, #12425, #16433, .T. ) ;
#57=DIRECTION ( 'NONE',  ( -1.000000000000000000, 0.000000000000000000, -0.000000000000000000 ) ) ;
#58=DIRECTION ( 'NONE',  ( 1.000000000000000000, -0.000000000000000000, 0.000000000000000000 ) ) ;
#59=DIRECTION ( 'NONE',  ( 1.000000000000000000, 0.000000000000000000, 0.000000000000000000 ) ) ;
#60=DIRECTION ( 'NONE',  ( -1.000000000000000000, -0.000000000000000000, -0.000000000000000000 ) ) ;
#63=ORIENTED_EDGE ( 'NONE', *, *, #8306, .T. ) ;
#64=DIRECTION ( 'NONE',  ( 1.000000000000000000, 0.000000000000000000, 0.000000000000000000 ) ) ;
#65=CARTESIAN_POINT ( 'NONE',  ( 10.00000000000000000, 33.95793648385814123, 86.04239391578002483 ) ) ;
#66=CIRCLE ( 'NONE', #8534, 44.99999999999999289 ) ;
#67=ORIENTED_EDGE ( 'NONE', *, *, #11916, .T. ) ;
#68=DIRECTION ( 'NONE',  ( -1.000000000000000000, 0.000000000000000000, 0.000000000000000000 ) ) ;
#70=DIRECTION ( 'NONE',  ( 0.000000000000000000, 0.000000000000000000, 1.000000000000000000 ) ) ;
#71=ORIENTED_EDGE ( 'NONE', *, *, #21788, .F. ) ;
#72=EDGE_CURVE ( 'NONE', #17227, #7603, #6261, .T. ) ;
#73=DIRECTION ( 'NONE',  ( 1.000000000000000000, 0.000000000000000000, 0.000000000000000000 ) ) ;
#75=VERTEX_POINT ( 'NONE', #9649 ) ;
#77=ORIENTED_EDGE ( 'NONE', *, *, #16610, .F. ) ;
#78=DIRECTION ( 'NONE',  ( 1.000000000000000000, 0.000000000000000000, 0.000000000000000000 ) ) ;
#79=ORIENTED_EDGE ( 'NONE', *, *, #6135, .T. ) ;
#83=CARTESIAN_POINT ( 'NONE',  ( 0.000000000000000000, -71.72924546249915068, -45.71766382684744201 ) ) ;
#84=CARTESIAN_POINT ( 'NONE',  ( 10.00000000000000000, 0.000000000000000000, 0.000000000000000000 ) ) ;
#85=AXIS2_PLACEMENT_3D ( 'NONE', #19345, #19670, #5876 ) ;
#87=CARTESIAN_POINT ( 'NONE',  ( 10.00000000000000000, 0.000000000000000000, 0.000000000000000000 ) ) ;
#90=DIRECTION ( 'NONE',  ( 1.000000000000000000, 0.000000000000000000, 0.000000000000000000 ) ) ;
#93=ORIENTED_EDGE ( 'NONE', *, *, #13098, .F. ) ;
#94=DIRECTION ( 'NONE',  ( -1.000000000000000000, -0.000000000000000000, -0.000000000000000000 ) ) ;
#97=FACE_OUTER_BOUND ( 'NONE', #19289, .T. ) ;
#103=CYLINDRICAL_SURFACE ( 'NONE', #17608, 88.00000000000000000 ) ;
#106=DIRECTION ( 'NONE',  ( 0.000000000000000000, 0.000000000000000000, 1.000000000000000000 ) ) ;
#107=CARTESIAN_POINT ( 'NONE',  ( 5.000000000000000000, -30.71797041605752554, -82.46457599186584275 ) ) ;
#108=AXIS2_PLACEMENT_3D ( 'NONE', #5672, #376, #480 ) ;
#110=DIRECTION ( 'NONE',  ( -1.000000000000000000, 0.000000000000000000, 0.000000000000000000 ) ) ;
#111=CYLINDRICAL_SURFACE ( 'NONE', #16029, 92.50100000000000477 ) ;
#113=DIRECTION ( 'NONE',  ( 0.000000000000000000, 0.000000000000000000, 1.000000000000000000 ) ) ;
#114=CIRCLE ( 'NONE', #16698, 45.00000000000000711 ) ;
#120=CIRCLE ( 'NONE', #16359, 44.99999999999999289 ) ;
#122=CARTESIAN_POINT ( 'NONE',  ( 10.00000000000000000, 66.01871308925549897, -64.79170103522952218 ) ) ;
#124=ORIENTED_EDGE ( 'NONE', *, *, #16480, .F. ) ;
#125=FACE_OUTER_BOUND ( 'NONE', #9793, .T. ) ;
#128=EDGE_CURVE ( 'NONE', #16693, #4447, #1608, .T. ) ;
#131=ORIENTED_EDGE ( 'NONE', *, *, #18244, .T. ) ;
#132=DIRECTION ( 'NONE',  ( 0.000000000000000000, 0.000000000000000000, 1.000000000000000000 ) ) ;
#133=EDGE_CURVE ( 'NONE', #20413, #2378, #1921, .T. ) ;
#136=DIRECTION ( 'NONE',  ( 1.000000000000000000, 0.000000000000000000, 0.000000000000000000 ) ) ;
#137=CARTESIAN_POINT ( 'NONE',  ( 0.000000000000000000, -36.60317927562525853, -76.78148674856802813 ) ) ;
#138=CIRCLE ( 'NONE', #20266, 92.50100000000000477 ) ;
#141=DIRECTION ( 'NONE',  ( 0.000000000000000000, 0.2079116908177531808, 0.9781476007338069101 ) ) ;
#143=EDGE_CURVE ( 'NONE', #8340, #1182, #890, .T. ) ;
#145=EDGE_CURVE ( 'NONE', #8013, #10982, #9353, .T. ) ;
#146=DIRECTION ( 'NONE',  ( 1.000000000000000000, -0.000000000000000000, -0.000000000000000000 ) ) ;
#148=ADVANCED_FACE ( 'NONE', ( #13522 ), #13849, .F. ) ;
#150=ORIENTED_EDGE ( 'NONE', *, *, #2176, .F. ) ;
#151=CARTESIAN_POINT ( 'NONE',  ( 0.000000000000000000, -2.208823992044743445, 85.03123271466935762 ) ) ;
#152=ORIENTED_EDGE ( 'NONE', *, *, #8425, .F. ) ;
#155=VERTEX_POINT ( 'NONE', #6910 ) ;
#156=LINE ( 'NONE', #19142, #3295 ) ;
#157=ORIENTED_EDGE ( 'NONE', *, *, #5783, .T. ) ;
#160=FACE_OUTER_BOUND ( 'NONE', #8742, .T. ) ;
#162=EDGE_CURVE ( 'NONE', #8199, #7224, #9947, .T. ) ;
#164=CARTESIAN_POINT ( 'NONE',  ( 10.00000000000000000, 45.60224695560681596, -80.47900393021679122 ) ) ;
#165=FACE_OUTER_BOUND ( 'NONE', #7515, .T. ) ;
#166=AXIS2_PLACEMENT_3D ( 'NONE', #4020, #2367, #12315 ) ;
#167=DIRECTION ( 'NONE',  ( -1.000000000000000000, -0.000000000000000000, -0.000000000000000000 ) ) ;
#168=CARTESIAN_POINT ( 'NONE',  ( 0.000000000000000000, 0.000000000000000000, 0.000000000000000000 ) ) ;
#170=EDGE_CURVE ( 'NONE', #2883, #19416, #16664, .T. ) ;
#171=CARTESIAN_POINT ( 'NONE',  ( 5.000000000000000000, -56.05743251323904985, 67.83483072893783117 ) ) ;
#173=VERTEX_POINT ( 'NONE', #20274 ) ;
#176=CARTESIAN_POINT ( 'NONE',  ( 10.00000000000000000, 27.87320266523557777, 88.20158487341770126 ) ) ;
#180=EDGE_LOOP ( 'NONE', ( #20881, #18064, #12670, #4609 ) ) ;
#181=AXIS2_PLACEMENT_3D ( 'NONE', #12579, #19535, #9476 ) ;
#182=EDGE_CURVE ( 'NONE', #12268, #14735, #15959, .T. ) ;
#183=CARTESIAN_POINT ( 'NONE',  ( 10.00000000000000000, -56.34908017029516714, -63.71789861856507997 ) ) ;
#184=AXIS2_PLACEMENT_3D ( 'NONE', #4735, #1644, #19987 ) ;
#185=FACE_OUTER_BOUND ( 'NONE', #19072, .T. ) ;
#187=CARTESIAN_POINT ( 'NONE',  ( 10.00000000000000000, 0.000000000000000000, 0.000000000000000000 ) ) ;
#189=ORIENTED_EDGE ( 'NONE', *, *, #5432, .T. ) ;
#191=ORIENTED_EDGE ( 'NONE', *, *, #16743, .F. ) ;
#192=LINE ( 'NONE', #6941, #8592 ) ;
#193=CIRCLE ( 'NONE', #20307, 92.50100000000000477 ) ;
#194=ORIENTED_EDGE ( 'NONE', *, *, #10939, .T. ) ;
#195=LINE ( 'NONE', #7048, #17980 ) ;
#196=FACE_OUTER_BOUND ( 'NONE', #2000, .T. ) ;
#197=CARTESIAN_POINT ( 'NONE',  ( 10.00000000000000000, 75.27139873020885830, 53.76477968147838027 ) ) ;
#198=DIRECTION ( 'NONE',  ( -1.000000000000000000, -0.000000000000000000, -0.000000000000000000 ) ) ;
#200=ADVANCED_FACE ( 'NONE', ( #160 ), #12195, .F. ) ;
#202=DIRECTION ( 'NONE',  ( 1.000000000000000000, 0.000000000000000000, 0.000000000000000000 ) ) ;
#203=AXIS2_PLACEMENT_3D ( 'NONE', #2476, #711, #21255 ) ;
#204=CARTESIAN_POINT ( 'NONE',  ( 0.000000000000000000, -65.83713140174766920, 58.39068529131174756 ) ) ;
#205=CIRCLE ( 'NONE', #21358, 44.99999999999999289 ) ;
#210=FACE_OUTER_BOUND ( 'NONE', #13128, .T. ) ;
#211=AXIS2_PLACEMENT_3D ( 'NONE', #19238, #20571, #8854 ) ;
#214=ORIENTED_EDGE ( 'NONE', *, *, #11490, .F. ) ;
#215=VERTEX_POINT ( 'NONE', #17177 ) ;
#216=LINE ( 'NONE', #10686, #17595 ) ;
#218=CIRCLE ( 'NONE', #7573, 92.50100000000000477 ) ;
#219=EDGE_LOOP ( 'NONE', ( #5452, #14194, #8580, #6579 ) ) ;
#220=AXIS2_PLACEMENT_3D ( 'NONE', #15734, #21034, #10973 ) ;
#222=DIRECTION ( 'NONE',  ( 0.000000000000000000, 0.000000000000000000, 1.000000000000000000 ) ) ;
#224=CARTESIAN_POINT ( 'NONE',  ( 10.00000000000000000, -81.97107881582179800, -22.71412948308650925 ) ) ;
#228=DIRECTION ( 'NONE',  ( -1.000000000000000000, 0.000000000000000000, 0.000000000000000000 ) ) ;
#232=ORIENTED_EDGE ( 'NONE', *, *, #45, .T. ) ;
#236=ORIENTED_EDGE ( 'NONE', *, *, #14894, .T. ) ;
#238=DIRECTION ( 'NONE',  ( 1.000000000000000000, 0.000000000000000000, 0.000000000000000000 ) ) ;
#239=VERTEX_POINT ( 'NONE', #15611 ) ;
#244=CIRCLE ( 'NONE', #21755, 92.50099999999999056 ) ;
#245=DIRECTION ( 'NONE',  ( 0.000000000000000000, 0.000000000000000000, 1.000000000000000000 ) ) ;
#246=DIRECTION ( 'NONE',  ( 0.000000000000000000, -0.4694715627858974671, 0.8829475928589232137 ) ) ;
#249=CARTESIAN_POINT ( 'NONE',  ( 10.00000000000000000, -91.49386717542229519, 13.61276130276963414 ) ) ;
#251=LINE ( 'NONE', #3457, #3152 ) ;
#252=CYLINDRICAL_SURFACE ( 'NONE', #7349, 44.99999999999999289 ) ;
#256=CIRCLE ( 'NONE', #9062, 88.00000000000000000 ) ;
#257=CIRCLE ( 'NONE', #4139, 92.50100000000001899 ) ;
#258=DIRECTION ( 'NONE',  ( -1.000000000000000000, -0.000000000000000000, -0.000000000000000000 ) ) ;
#259=DIRECTION ( 'NONE',  ( -1.000000000000000000, -0.000000000000000000, -0.000000000000000000 ) ) ;
#267=CYLINDRICAL_SURFACE ( 'NONE', #10379, 44.99999999999999289 ) ;
#269=CIRCLE ( 'NONE', #5211, 44.99999999999999289 ) ;
#270=CARTESIAN_POINT ( 'NONE',  ( 10.00000000000000000, -84.90234713953988432, 5.175025661883520200 ) ) ;
#271=DIRECTION ( 'NONE',  ( 1.000000000000000000, 0.000000000000000000, 0.000000000000000000 ) ) ;
#272=EDGE_CURVE ( 'NONE', #5074, #2288, #8772, .T. ) ;
#274=ADVANCED_FACE ( 'NONE', ( #3687 ), #15513, .F. ) ;
#275=CARTESIAN_POINT ( 'NONE',  ( 0.000000000000000000, 0.000000000000000000, 0.000000000000000000 ) ) ;
#276=EDGE_CURVE ( 'NONE', #11431, #4861, #15600, .T. ) ;
#277=CARTESIAN_POINT ( 'NONE',  ( 10.00000000000000000, 0.000000000000000000, 0.000000000000000000 ) ) ;
#278=AXIS2_PLACEMENT_3D ( 'NONE', #20316, #8268, #21854 ) ;
#279=CARTESIAN_POINT ( 'NONE',  ( 0.000000000000000000, -61.60362715319078575, 62.84101464466223774 ) ) ;
#280=CARTESIAN_POINT ( 'NONE',  ( 5.000000000000002665, -83.89484365856928605, 26.56417150042919673 ) ) ;
#281=ADVANCED_FACE ( 'NONE', ( #12804 ), #21549, .F. ) ;
#282=VERTEX_POINT ( 'NONE', #6088 ) ;
#283=AXIS2_PLACEMENT_3D ( 'NONE', #3990, #20791, #1007 ) ;
#284=FACE_OUTER_BOUND ( 'NONE', #6940, .T. ) ;
#286=VERTEX_POINT ( 'NONE', #2978 ) ;
#287=CARTESIAN_POINT ( 'NONE',  ( 5.000000000000000000, 87.96697768756401103, -2.410567674970879981 ) ) ;
#290=VECTOR ( 'NONE', #16490, 1000.000000000000000 ) ;
#291=VECTOR ( 'NONE', #5677, 1000.000000000000000 ) ;
#292=CARTESIAN_POINT ( 'NONE',  ( 10.00000000000000000, 0.000000000000000000, 0.000000000000000000 ) ) ;
#293=AXIS2_PLACEMENT_3D ( 'NONE', #2385, #14534, #16196 ) ;
#294=DIRECTION ( 'NONE',  ( -1.000000000000000000, 0.000000000000000000, 0.000000000000000000 ) ) ;
#297=DIRECTION ( 'NONE',  ( -1.000000000000000000, -0.000000000000000000, 0.000000000000000000 ) ) ;
#298=EDGE_CURVE ( 'NONE', #2674, #6765, #4540, .T. ) ;
#300=EDGE_LOOP ( 'NONE', ( #21001, #13570, #8396, #414 ) ) ;
#301=VERTEX_POINT ( 'NONE', #21219 ) ;
#303=ORIENTED_EDGE ( 'NONE', *, *, #3809, .F. ) ;
#304=CARTESIAN_POINT ( 'NONE',  ( 0.000000000000000000, 0.000000000000000000, 0.000000000000000000 ) ) ;
#305=FACE_OUTER_BOUND ( 'NONE', #10474, .T. ) ;
#306=DIRECTION ( 'NONE',  ( 0.000000000000000000, 0.000000000000000000, 1.000000000000000000 ) ) ;
#307=DIRECTION ( 'NONE',  ( 1.000000000000000000, 0.000000000000000000, 0.000000000000000000 ) ) ;
#308=DIRECTION ( 'NONE',  ( -1.000000000000000000, -0.000000000000000000, 0.000000000000000000 ) ) ;
#309=DIRECTION ( 'NONE',  ( 1.000000000000000000, 0.000000000000000000, 0.000000000000000000 ) ) ;
#310=CIRCLE ( 'NONE', #12639, 44.99999999999999289 ) ;
#311=ADVANCED_FACE ( 'NONE', ( #6322 ), #16244, .F. ) ;
#312=AXIS2_PLACEMENT_3D ( 'NONE', #17991, #11339, #16213 ) ;
#314=CARTESIAN_POINT ( 'NONE',  ( 0.000000000000000000, -46.89573839703331259, 79.73220629831473616 ) ) ;
#315=AXIS2_PLACEMENT_3D ( 'NONE', #21324, #3204, #1444 ) ;
#318=FACE_OUTER_BOUND ( 'NONE', #13916, .T. ) ;
#319=DIRECTION ( 'NONE',  ( 1.000000000000000000, 0.000000000000000000, 0.000000000000000000 ) ) ;
#320=DIRECTION ( 'NONE',  ( -1.000000000000000000, -0.000000000000000000, 0.000000000000000000 ) ) ;
#322=ORIENTED_EDGE ( 'NONE', *, *, #9631, .T. ) ;
#323=ORIENTED_EDGE ( 'NONE', *, *, #14086, .T. ) ;
#325=CARTESIAN_POINT ( 'NONE',  ( 10.00000000000000000, -78.83848282823942100, 48.38314403117473006 ) ) ;
#326=ADVANCED_FACE ( 'NONE', ( #19444 ), #4645, .F. ) ;
#329=ORIENTED_EDGE ( 'NONE', *, *, #14866, .F. ) ;
#331=EDGE_CURVE ( 'NONE', #10029, #19516, #19552, .T. ) ;
#332=AXIS2_PLACEMENT_3D ( 'NONE', #13001, #21404, #16426 ) ;
#333=AXIS2_PLACEMENT_3D ( 'NONE', #15679, #658, #762 ) ;
#335=ORIENTED_EDGE ( 'NONE', *, *, #9621, .F. ) ;
#339=DIRECTION ( 'NONE',  ( 0.000000000000000000, -0.6946583704590034714, 0.7193398003386451967 ) ) ;
#342=EDGE_CURVE ( 'NONE', #6864, #16595, #7844, .T. ) ;
#347=CIRCLE ( 'NONE', #5282, 88.00000000000000000 ) ;
#348=AXIS2_PLACEMENT_3D ( 'NONE', #8886, #10652, #17196 ) ;
#349=ORIENTED_EDGE ( 'NONE', *, *, #11633, .F. ) ;
#351=ORIENTED_EDGE ( 'NONE', *, *, #3701, .F. ) ;
#352=ORIENTED_EDGE ( 'NONE', *, *, #15867, .T. ) ;
#355=ORIENTED_EDGE ( 'NONE', *, *, #9307, .T. ) ;
#356=CARTESIAN_POINT ( 'NONE',  ( 10.00000000000000000, 0.000000000000000000, 0.000000000000000000 ) ) ;
#357=ORIENTED_EDGE ( 'NONE', *, *, #9039, .T. ) ;
#360=DIRECTION ( 'NONE',  ( 0.000000000000000000, 0.000000000000000000, 1.000000000000000000 ) ) ;
#362=CARTESIAN_POINT ( 'NONE',  ( 10.00000000000000000, -86.77540292929711541, 14.62974526292689426 ) ) ;
#365=DIRECTION ( 'NONE',  ( -1.000000000000000000, 0.000000000000000000, 0.000000000000000000 ) ) ;
#366=DIRECTION ( 'NONE',  ( 0.000000000000000000, 0.5877852522924742473, -0.8090169943749465631 ) ) ;
#367=ORIENTED_EDGE ( 'NONE', *, *, #16193, .F. ) ;
#368=CIRCLE ( 'NONE', #4963, 44.99999999999998579 ) ;
#369=DIRECTION ( 'NONE',  ( 0.000000000000000000, -0.8660254037844432595, 0.4999999999999920064 ) ) ;
#370=DIRECTION ( 'NONE',  ( 1.000000000000000000, 0.000000000000000000, 0.000000000000000000 ) ) ;
#371=ORIENTED_EDGE ( 'NONE', *, *, #13234, .F. ) ;
#372=EDGE_CURVE ( 'NONE', #3326, #21836, #19668, .T. ) ;
#373=DIRECTION ( 'NONE',  ( -1.000000000000000000, -0.000000000000000000, -0.000000000000000000 ) ) ;
#376=DIRECTION ( 'NONE',  ( -1.000000000000000000, 0.000000000000000000, 0.000000000000000000 ) ) ;
#378=VERTEX_POINT ( 'NONE', #9266 ) ;
#379=CARTESIAN_POINT ( 'NONE',  ( 10.00000000000000000, -57.06999622551850138, 66.98518889142063415 ) ) ;
#380=DIRECTION ( 'NONE',  ( 1.000000000000000000, 0.000000000000000000, 0.000000000000000000 ) ) ;
#382=CARTESIAN_POINT ( 'NONE',  ( 0.000000000000000000, -75.45728100697627383, 39.26051685139039193 ) ) ;
#383=DIRECTION ( 'NONE',  ( 0.000000000000000000, 0.000000000000000000, 1.000000000000000000 ) ) ;
#384=FACE_OUTER_BOUND ( 'NONE', #4779, .T. ) ;
#385=AXIS2_PLACEMENT_3D ( 'NONE', #3175, #1301, #4716 ) ;
#386=CYLINDRICAL_SURFACE ( 'NONE', #20961, 44.99999999999999289 ) ;
#387=DIRECTION ( 'NONE',  ( -1.000000000000000000, -0.000000000000000000, -0.000000000000000000 ) ) ;
#390=CARTESIAN_POINT ( 'NONE',  ( 0.000000000000000000, -79.66702613806754130, -29.80527447819517661 ) ) ;
#392=CARTESIAN_POINT ( 'NONE',  ( 10.00000000000000000, 19.83954325428771881, -82.71385593638672162 ) ) ;
#393=VERTEX_POINT ( 'NONE', #883 ) ;
#395=EDGE_CURVE ( 'NONE', #9256, #19686, #11275, .T. ) ;
#398=ORIENTED_EDGE ( 'NONE', *, *, #6942, .T. ) ;
#399=ORIENTED_EDGE ( 'NONE', *, *, #18525, .T. ) ;
#400=ORIENTED_EDGE ( 'NONE', *, *, #3209, .F. ) ;
#401=ORIENTED_EDGE ( 'NONE', *, *, #14036, .F. ) ;
#403=ORIENTED_EDGE ( 'NONE', *, *, #3916, .T. ) ;
#405=CYLINDRICAL_SURFACE ( 'NONE', #13914, 88.00000000000000000 ) ;
#406=DIRECTION ( 'NONE',  ( -1.000000000000000000, -0.000000000000000000, 0.000000000000000000 ) ) ;
#408=DIRECTION ( 'NONE',  ( 0.000000000000000000, 0.000000000000000000, 1.000000000000000000 ) ) ;
#409=CARTESIAN_POINT ( 'NONE',  ( 0.000000000000000000, 0.000000000000000000, 0.000000000000000000 ) ) ;
#410=EDGE_CURVE ( 'NONE', #2166, #21782, #436, .T. ) ;
#412=FACE_OUTER_BOUND ( 'NONE', #20325, .T. ) ;
#414=ORIENTED_EDGE ( 'NONE', *, *, #12479, .F. ) ;
#415=EDGE_CURVE ( 'NONE', #508, #14361, #20203, .T. ) ;
#416=DIRECTION ( 'NONE',  ( -1.000000000000000000, 0.000000000000000000, -0.000000000000000000 ) ) ;
#418=LINE ( 'NONE', #20634, #10815 ) ;
#419=VERTEX_POINT ( 'NONE', #1003 ) ;
#421=CARTESIAN_POINT ( 'NONE',  ( -10.00000000000000000, 0.000000000000000000, 0.000000000000000000 ) ) ;
#422=EDGE_CURVE ( 'NONE', #6705, #19466, #20900, .T. ) ;
#425=DIRECTION ( 'NONE',  ( 1.000000000000000000, 0.000000000000000000, 0.000000000000000000 ) ) ;
#426=EDGE_LOOP ( 'NONE', ( #2512, #10819, #21191, #16481 ) ) ;
#427=EDGE_CURVE ( 'NONE', #19313, #4861, #15245, .T. ) ;
#430=ORIENTED_EDGE ( 'NONE', *, *, #8428, .T. ) ;
#431=CARTESIAN_POINT ( 'NONE',  ( 0.000000000000000000, -40.72878876293203376, 78.00747250042435610 ) ) ;
#433=CARTESIAN_POINT ( 'NONE',  ( 10.00000000000000000, 0.000000000000000000, 0.000000000000000000 ) ) ;
#435=ADVANCED_FACE ( 'NONE', ( #5083 ), #5200, .F. ) ;
#436=CIRCLE ( 'NONE', #3254, 92.50099999999999056 ) ;
#437=CARTESIAN_POINT ( 'NONE',  ( 10.00000000000000000, 23.10190250628953379, -89.56973317806578905 ) ) ;
#438=DIRECTION ( 'NONE',  ( 0.000000000000000000, -0.9993908270190959842, 0.03489949670249113678 ) ) ;
#439=CARTESIAN_POINT ( 'NONE',  ( 0.000000000000000000, 83.48638250753266732, -27.82128566055030916 ) ) ;
#440=EDGE_CURVE ( 'NONE', #16787, #1439, #11371, .T. ) ;
#441=CARTESIAN_POINT ( 'NONE',  ( 10.00000000000000000, 51.76708072107885528, 67.49339815138510801 ) ) ;
#442=ADVANCED_FACE ( 'NONE', ( #4975 ), #20117, .F. ) ;
#443=CARTESIAN_POINT ( 'NONE',  ( 0.000000000000000000, -61.71252885873428085, 58.53847642588571887 ) ) ;
#444=ORIENTED_EDGE ( 'NONE', *, *, #1345, .F. ) ;
#446=DIRECTION ( 'NONE',  ( -1.000000000000000000, 0.000000000000000000, -0.000000000000000000 ) ) ;
#447=VERTEX_POINT ( 'NONE', #4 ) ;
#449=EDGE_LOOP ( 'NONE', ( #5641, #4304, #5239, #6868 ) ) ;
#450=ORIENTED_EDGE ( 'NONE', *, *, #11470, .F. ) ;
#453=VERTEX_POINT ( 'NONE', #15229 ) ;
#454=VERTEX_POINT ( 'NONE', #1544 ) ;
#456=EDGE_CURVE ( 'NONE', #2112, #5619, #7500, .T. ) ;
#457=CARTESIAN_POINT ( 'NONE',  ( 10.00000000000000000, 0.000000000000000000, 0.000000000000000000 ) ) ;
#459=DIRECTION ( 'NONE',  ( -1.000000000000000000, -0.000000000000000000, -0.000000000000000000 ) ) ;
#460=CARTESIAN_POINT ( 'NONE',  ( 0.000000000000000000, 83.35585896458619004, 16.94078559807978124 ) ) ;
#461=AXIS2_PLACEMENT_3D ( 'NONE', #4977, #18458, #3312 ) ;
#463=DIRECTION ( 'NONE',  ( 0.000000000000000000, 0.000000000000000000, 1.000000000000000000 ) ) ;
#464=CARTESIAN_POINT ( 'NONE',  ( 10.00000000000000000, 81.83745710415276164, 32.35167097270178260 ) ) ;
#466=DIRECTION ( 'NONE',  ( 1.000000000000000000, 0.000000000000000000, 0.000000000000000000 ) ) ;
#467=DIRECTION ( 'NONE',  ( 1.000000000000000000, 0.000000000000000000, 0.000000000000000000 ) ) ;
#471=ORIENTED_EDGE ( 'NONE', *, *, #2986, .T. ) ;
#472=CIRCLE ( 'NONE', #10698, 88.00000000000000000 ) ;
#473=EDGE_CURVE ( 'NONE', #20811, #14806, #13136, .T. ) ;
#474=DIRECTION ( 'NONE',  ( 1.000000000000000000, -0.000000000000000000, -0.000000000000000000 ) ) ;
#475=CARTESIAN_POINT ( 'NONE',  ( 10.00000000000000000, 0.000000000000000000, 0.000000000000000000 ) ) ;
#477=LINE ( 'NONE', #18723, #16771 ) ;
#479=VECTOR ( 'NONE', #8463, 1000.000000000000000 ) ;
#480=DIRECTION ( 'NONE',  ( 0.000000000000000000, 0.000000000000000000, 1.000000000000000000 ) ) ;
#481=VERTEX_POINT ( 'NONE', #13580 ) ;
#482=ORIENTED_EDGE ( 'NONE', *, *, #12164, .F. ) ;
#484=DIRECTION ( 'NONE',  ( -1.000000000000000000, -0.000000000000000000, 0.000000000000000000 ) ) ;
#488=LINE ( 'NONE', #12200, #995 ) ;
#491=ADVANCED_FACE ( 'NONE', ( #3094 ), #1440, .F. ) ;
#493=DIRECTION ( 'NONE',  ( 1.000000000000000000, 0.000000000000000000, -0.000000000000000000 ) ) ;
#494=AXIS2_PLACEMENT_3D ( 'NONE', #84, #10670, #5605 ) ;
#495=EDGE_LOOP ( 'NONE', ( #11685, #11364, #5919, #15728 ) ) ;
#497=AXIS2_PLACEMENT_3D ( 'NONE', #13069, #4792, #16173 ) ;
#498=EDGE_LOOP ( 'NONE', ( #15179, #10420, #7326, #14605 ) ) ;
#500=DIRECTION ( 'NONE',  ( -1.000000000000000000, 0.000000000000000000, -0.000000000000000000 ) ) ;
#502=DIRECTION ( 'NONE',  ( 1.000000000000000000, 0.000000000000000000, 0.000000000000000000 ) ) ;
#504=EDGE_LOOP ( 'NONE', ( #15894, #8627, #3713, #2897 ) ) ;
#505=CIRCLE ( 'NONE', #2264, 44.99999999999998579 ) ;
#506=ORIENTED_EDGE ( 'NONE', *, *, #19036, .F. ) ;
#507=ORIENTED_EDGE ( 'NONE', *, *, #5060, .F. ) ;
#508=VERTEX_POINT ( 'NONE', #9825 ) ;
#509=CARTESIAN_POINT ( 'NONE',  ( 0.000000000000000000, 78.04699792498210797, -49.64978465107211036 ) ) ;
#510=VERTEX_POINT ( 'NONE', #6754 ) ;
#511=AXIS2_PLACEMENT_3D ( 'NONE', #10667, #17317, #5821 ) ;
#513=DIRECTION ( 'NONE',  ( -1.000000000000000000, -0.000000000000000000, 0.000000000000000000 ) ) ;
#515=CARTESIAN_POINT ( 'NONE',  ( 10.00000000000000000, -46.89573839703219704, -79.73220629831536144 ) ) ;
#516=CARTESIAN_POINT ( 'NONE',  ( 0.000000000000000000, 0.000000000000000000, 0.000000000000000000 ) ) ;
#517=EDGE_CURVE ( 'NONE', #19516, #10855, #18813, .T. ) ;
#518=LINE ( 'NONE', #17324, #20205 ) ;
#519=ORIENTED_EDGE ( 'NONE', *, *, #15032, .F. ) ;
#520=CARTESIAN_POINT ( 'NONE',  ( 0.000000000000000000, -19.83954325428602061, -82.71385593638713374 ) ) ;
#521=AXIS2_PLACEMENT_3D ( 'NONE', #551, #12365, #12467 ) ;
#522=DIRECTION ( 'NONE',  ( 0.000000000000000000, -0.4067366430757887175, -0.9135454576426059736 ) ) ;
#523=AXIS2_PLACEMENT_3D ( 'NONE', #5294, #8493, #10353 ) ;
#526=DIRECTION ( 'NONE',  ( 0.000000000000000000, -1.954455116267202870E-14, -1.000000000000000000 ) ) ;
#527=AXIS2_PLACEMENT_3D ( 'NONE', #18273, #14833, #16166 ) ;
#528=AXIS2_PLACEMENT_3D ( 'NONE', #1902, #8639, #3779 ) ;
#529=ORIENTED_EDGE ( 'NONE', *, *, #2959, .T. ) ;
#533=ORIENTED_EDGE ( 'NONE', *, *, #17872, .T. ) ;
#534=ADVANCED_FACE ( 'NONE', ( #10157 ), #3200, .F. ) ;
#535=VERTEX_POINT ( 'NONE', #6644 ) ;
#536=VERTEX_POINT ( 'NONE', #13466 ) ;
#538=ORIENTED_EDGE ( 'NONE', *, *, #2848, .F. ) ;
#540=CYLINDRICAL_SURFACE ( 'NONE', #2987, 92.50100000000000477 ) ;
#541=CARTESIAN_POINT ( 'NONE',  ( 0.000000000000000000, 57.06999622551805373, 66.98518889142101784 ) ) ;
#542=AXIS2_PLACEMENT_3D ( 'NONE', #21181, #2611, #6162 ) ;
#543=AXIS2_PLACEMENT_3D ( 'NONE', #17281, #13952, #2235 ) ;
#545=AXIS2_PLACEMENT_3D ( 'NONE', #9654, #1395, #11435 ) ;
#548=CARTESIAN_POINT ( 'NONE',  ( 10.00000000000000000, 69.25892805976512534, 49.38005998797868301 ) ) ;
#549=EDGE_CURVE ( 'NONE', #481, #1387, #12460, .T. ) ;
#551=CARTESIAN_POINT ( 'NONE',  ( 10.00000000000000000, 0.000000000000000000, 0.000000000000000000 ) ) ;
#552=EDGE_CURVE ( 'NONE', #19754, #4889, #9037, .T. ) ;
#553=DIRECTION ( 'NONE',  ( 1.000000000000000000, -0.000000000000000000, -0.000000000000000000 ) ) ;
#554=DIRECTION ( 'NONE',  ( -1.000000000000000000, 0.000000000000000000, 0.000000000000000000 ) ) ;
#555=EDGE_CURVE ( 'NONE', #7130, #7194, #6103, .T. ) ;
#558=ORIENTED_EDGE ( 'NONE', *, *, #12580, .T. ) ;
#559=ORIENTED_EDGE ( 'NONE', *, *, #2768, .F. ) ;
#561=ORIENTED_EDGE ( 'NONE', *, *, #20234, .T. ) ;
#562=EDGE_CURVE ( 'NONE', #6281, #4746, #2302, .T. ) ;
#564=CARTESIAN_POINT ( 'NONE',  ( -10.00000000000000000, 0.000000000000000000, 0.000000000000000000 ) ) ;
#565=ORIENTED_EDGE ( 'NONE', *, *, #7928, .T. ) ;
#567=EDGE_CURVE ( 'NONE', #14361, #6281, #9246, .T. ) ;
#568=CARTESIAN_POINT ( 'NONE',  ( 10.00000000000000000, 86.77540292929701593, 14.62974526292747868 ) ) ;
#570=CYLINDRICAL_SURFACE ( 'NONE', #13210, 92.50100000000000477 ) ;
#571=DIRECTION ( 'NONE',  ( 0.000000000000000000, 0.000000000000000000, 1.000000000000000000 ) ) ;
#573=CARTESIAN_POINT ( 'NONE',  ( -10.00000000000000000, 0.000000000000000000, 0.000000000000000000 ) ) ;
#574=AXIS2_PLACEMENT_3D ( 'NONE', #19114, #15472, #1997 ) ;
#575=DIRECTION ( 'NONE',  ( 0.000000000000000000, 0.000000000000000000, 1.000000000000000000 ) ) ;
#576=AXIS2_PLACEMENT_3D ( 'NONE', #16604, #1464, #10075 ) ;
#577=DIRECTION ( 'NONE',  ( 0.000000000000000000, 0.000000000000000000, 1.000000000000000000 ) ) ;
#578=DIRECTION ( 'NONE',  ( 1.000000000000000000, 0.000000000000000000, 0.000000000000000000 ) ) ;
#579=CARTESIAN_POINT ( 'NONE',  ( 10.00000000000000000, 0.000000000000000000, 0.000000000000000000 ) ) ;
#580=CIRCLE ( 'NONE', #5471, 44.99999999999999289 ) ;
#581=EDGE_CURVE ( 'NONE', #14715, #6477, #17390, .T. ) ;
#583=DIRECTION ( 'NONE',  ( 0.000000000000000000, 0.5299192642331999048, 0.8480480961564291764 ) ) ;
#584=EDGE_CURVE ( 'NONE', #11040, #9927, #13903, .T. ) ;
#585=DIRECTION ( 'NONE',  ( 0.000000000000000000, -0.5877852522924632561, -0.8090169943749546677 ) ) ;
#589=VERTEX_POINT ( 'NONE', #541 ) ;
#590=VECTOR ( 'NONE', #17368, 1000.000000000000000 ) ;
#593=ORIENTED_EDGE ( 'NONE', *, *, #19598, .F. ) ;
#595=EDGE_CURVE ( 'NONE', #18348, #18539, #20217, .T. ) ;
#596=DIRECTION ( 'NONE',  ( -1.000000000000000000, 0.000000000000000000, -0.000000000000000000 ) ) ;
#600=DIRECTION ( 'NONE',  ( 1.000000000000000000, 0.000000000000000000, 0.000000000000000000 ) ) ;
#601=DIRECTION ( 'NONE',  ( 1.000000000000000000, 0.000000000000000000, 0.000000000000000000 ) ) ;
#603=CARTESIAN_POINT ( 'NONE',  ( 0.000000000000000000, 0.000000000000000000, 0.000000000000000000 ) ) ;
#605=VECTOR ( 'NONE', #3170, 1000.000000000000000 ) ;
#608=ORIENTED_EDGE ( 'NONE', *, *, #11246, .T. ) ;
#609=CARTESIAN_POINT ( 'NONE',  ( 10.00000000000000000, 14.02138820415029663, -83.89630571862271324 ) ) ;
#610=VERTEX_POINT ( 'NONE', #10481 ) ;
#612=FACE_OUTER_BOUND ( 'NONE', #18647, .T. ) ;
#613=ORIENTED_EDGE ( 'NONE', *, *, #13922, .F. ) ;
#614=CIRCLE ( 'NONE', #16845, 44.99999999999999289 ) ;
#615=EDGE_LOOP ( 'NONE', ( #5922, #19113 ) ) ;
#617=AXIS2_PLACEMENT_3D ( 'NONE', #12857, #4142, #19606 ) ;
#618=ORIENTED_EDGE ( 'NONE', *, *, #20802, .T. ) ;
#621=CIRCLE ( 'NONE', #16136, 92.50100000000001899 ) ;
#622=ORIENTED_EDGE ( 'NONE', *, *, #14710, .F. ) ;
#623=DIRECTION ( 'NONE',  ( 1.000000000000000000, -0.000000000000000000, -0.000000000000000000 ) ) ;
#625=CARTESIAN_POINT ( 'NONE',  ( 0.000000000000000000, 41.21966518005955038, 82.80926399530301296 ) ) ;
#627=DIRECTION ( 'NONE',  ( -1.000000000000000000, -0.000000000000000000, 0.000000000000000000 ) ) ;
#629=CARTESIAN_POINT ( 'NONE',  ( 10.00000000000000000, 62.44821182181184582, -68.23969402963440700 ) ) ;
#630=CIRCLE ( 'NONE', #2393, 44.99999999999999289 ) ;
#634=CARTESIAN_POINT ( 'NONE',  ( 10.00000000000000000, 0.000000000000000000, 0.000000000000000000 ) ) ;
#635=EDGE_LOOP ( 'NONE', ( #2174, #21660, #4771, #5388 ) ) ;
#636=DIRECTION ( 'NONE',  ( 0.000000000000000000, 0.000000000000000000, 1.000000000000000000 ) ) ;
#637=ORIENTED_EDGE ( 'NONE', *, *, #6937, .T. ) ;
#638=CYLINDRICAL_SURFACE ( 'NONE', #2415, 45.00000000000000000 ) ;
#639=ORIENTED_EDGE ( 'NONE', *, *, #10676, .T. ) ;
#640=ORIENTED_EDGE ( 'NONE', *, *, #862, .T. ) ;
#641=EDGE_CURVE ( 'NONE', #13683, #10766, #5390, .T. ) ;
#642=ORIENTED_EDGE ( 'NONE', *, *, #6404, .T. ) ;
#643=CARTESIAN_POINT ( 'NONE',  ( -10.00000000000000000, 0.000000000000000000, 0.000000000000000000 ) ) ;
#644=ORIENTED_EDGE ( 'NONE', *, *, #3566, .T. ) ;
#645=FACE_OUTER_BOUND ( 'NONE', #12452, .T. ) ;
#646=AXIS2_PLACEMENT_3D ( 'NONE', #7957, #770, #14364 ) ;
#647=DIRECTION ( 'NONE',  ( 1.000000000000000000, 0.000000000000000000, 0.000000000000000000 ) ) ;
#649=VECTOR ( 'NONE', #1759, 1000.000000000000000 ) ;
#650=AXIS2_PLACEMENT_3D ( 'NONE', #3327, #16813, #1788 ) ;
#651=AXIS2_PLACEMENT_3D ( 'NONE', #18135, #14591, #2989 ) ;
#653=ADVANCED_FACE ( 'NONE', ( #15782 ), #20449, .F. ) ;
#654=FACE_OUTER_BOUND ( 'NONE', #10649, .T. ) ;
#655=CYLINDRICAL_SURFACE ( 'NONE', #14717, 88.00000000000000000 ) ;
#657=DIRECTION ( 'NONE',  ( -1.000000000000000000, 0.000000000000000000, 0.000000000000000000 ) ) ;
#658=DIRECTION ( 'NONE',  ( -1.000000000000000000, 0.000000000000000000, 0.000000000000000000 ) ) ;
#659=VERTEX_POINT ( 'NONE', #12137 ) ;
#662=ORIENTED_EDGE ( 'NONE', *, *, #19083, .F. ) ;
#664=ORIENTED_EDGE ( 'NONE', *, *, #11903, .T. ) ;
#665=CIRCLE ( 'NONE', #2431, 92.50100000000000477 ) ;
#670=EDGE_CURVE ( 'NONE', #9397, #13601, #10805, .T. ) ;
#672=EDGE_LOOP ( 'NONE', ( #10904, #6762, #21714, #12996 ) ) ;
#673=ORIENTED_EDGE ( 'NONE', *, *, #21444, .T. ) ;
#675=EDGE_CURVE ( 'NONE', #17526, #5244, #19164, .T. ) ;
#676=ORIENTED_EDGE ( 'NONE', *, *, #17682, .F. ) ;
#677=FACE_OUTER_BOUND ( 'NONE', #2204, .T. ) ;
#678=CARTESIAN_POINT ( 'NONE',  ( 10.00000000000000000, 0.000000000000000000, 0.000000000000000000 ) ) ;
#679=AXIS2_PLACEMENT_3D ( 'NONE', #20194, #6619, #4621 ) ;
#684=AXIS2_PLACEMENT_3D ( 'NONE', #20100, #1853, #13565 ) ;
#686=DIRECTION ( 'NONE',  ( -1.000000000000000000, 0.000000000000000000, 0.000000000000000000 ) ) ;
#687=EDGE_CURVE ( 'NONE', #13715, #20567, #2193, .T. ) ;
#691=LINE ( 'NONE', #12093, #15370 ) ;
#693=DIRECTION ( 'NONE',  ( 1.000000000000000000, 0.000000000000000000, 0.000000000000000000 ) ) ;
#695=EDGE_LOOP ( 'NONE', ( #21049, #1674, #16074, #3574 ) ) ;
#697=AXIS2_PLACEMENT_3D ( 'NONE', #16951, #8544, #9755 ) ;
#700=ORIENTED_EDGE ( 'NONE', *, *, #9307, .F. ) ;
#701=CARTESIAN_POINT ( 'NONE',  ( 0.000000000000000000, 0.000000000000000000, 0.000000000000000000 ) ) ;
#704=EDGE_LOOP ( 'NONE', ( #7336, #749, #17679, #6492 ) ) ;
#709=DIRECTION ( 'NONE',  ( 1.000000000000000000, 0.000000000000000000, 0.000000000000000000 ) ) ;
#711=DIRECTION ( 'NONE',  ( 1.000000000000000000, 0.000000000000000000, 0.000000000000000000 ) ) ;
#713=DIRECTION ( 'NONE',  ( 0.000000000000000000, 0.000000000000000000, 1.000000000000000000 ) ) ;
#714=AXIS2_PLACEMENT_3D ( 'NONE', #18039, #9610, #5889 ) ;
#717=CYLINDRICAL_SURFACE ( 'NONE', #8680, 45.00000000000000000 ) ;
#718=EDGE_LOOP ( 'NONE', ( #1372, #13579, #6111, #12415 ) ) ;
#720=DIRECTION ( 'NONE',  ( 0.000000000000000000, 0.000000000000000000, 1.000000000000000000 ) ) ;
#721=ORIENTED_EDGE ( 'NONE', *, *, #9312, .F. ) ;
#722=CARTESIAN_POINT ( 'NONE',  ( 0.000000000000000000, 12.90135963484081216, 87.04915231966650424 ) ) ;
#724=ORIENTED_EDGE ( 'NONE', *, *, #1221, .T. ) ;
#727=ADVANCED_FACE ( 'NONE', ( #14346 ), #11021, .F. ) ;
#728=ORIENTED_EDGE ( 'NONE', *, *, #6190, .F. ) ;
#729=ORIENTED_EDGE ( 'NONE', *, *, #19205, .F. ) ;
#730=AXIS2_PLACEMENT_3D ( 'NONE', #4831, #4390, #11574 ) ;
#732=LINE ( 'NONE', #19288, #5569 ) ;
#733=VERTEX_POINT ( 'NONE', #18005 ) ;
#734=CARTESIAN_POINT ( 'NONE',  ( 0.000000000000000000, 46.89573839703275127, 79.73220629831503459 ) ) ;
#737=CARTESIAN_POINT ( 'NONE',  ( 10.00000000000000000, 41.89587599971545018, 77.38692120905484728 ) ) ;
#738=DIRECTION ( 'NONE',  ( 0.000000000000000000, 0.000000000000000000, 1.000000000000000000 ) ) ;
#740=DIRECTION ( 'NONE',  ( 0.000000000000000000, 0.000000000000000000, 1.000000000000000000 ) ) ;
#741=DIRECTION ( 'NONE',  ( 0.000000000000000000, 0.000000000000000000, 1.000000000000000000 ) ) ;
#743=DIRECTION ( 'NONE',  ( 0.000000000000000000, 0.000000000000000000, 1.000000000000000000 ) ) ;
#744=EDGE_LOOP ( 'NONE', ( #351, #1727, #7139, #729 ) ) ;
#748=ORIENTED_EDGE ( 'NONE', *, *, #2986, .F. ) ;
#749=ORIENTED_EDGE ( 'NONE', *, *, #6495, .F. ) ;
#750=VERTEX_POINT ( 'NONE', #21197 ) ;
#751=DIRECTION ( 'NONE',  ( 0.000000000000000000, 0.9945218953682729568, 0.1045284632676569958 ) ) ;
#752=VERTEX_POINT ( 'NONE', #9469 ) ;
#754=DIRECTION ( 'NONE',  ( 1.000000000000000000, 0.000000000000000000, -0.000000000000000000 ) ) ;
#757=DIRECTION ( 'NONE',  ( 0.000000000000000000, 0.5299192642332060110, -0.8480480961564252906 ) ) ;
#758=CARTESIAN_POINT ( 'NONE',  ( 10.00000000000000000, 0.000000000000000000, 0.000000000000000000 ) ) ;
#761=DIRECTION ( 'NONE',  ( -1.000000000000000000, -0.000000000000000000, -0.000000000000000000 ) ) ;
#762=DIRECTION ( 'NONE',  ( 0.000000000000000000, 0.000000000000000000, 1.000000000000000000 ) ) ;
#763=DIRECTION ( 'NONE',  ( 0.000000000000000000, 0.000000000000000000, -1.000000000000000000 ) ) ;
#764=ORIENTED_EDGE ( 'NONE', *, *, #2482, .F. ) ;
#765=AXIS2_PLACEMENT_3D ( 'NONE', #409, #2389, #9126 ) ;
#768=ORIENTED_EDGE ( 'NONE', *, *, #15411, .F. ) ;
#770=DIRECTION ( 'NONE',  ( 1.000000000000000000, 0.000000000000000000, 0.000000000000000000 ) ) ;
#773=DIRECTION ( 'NONE',  ( 0.000000000000000000, 0.000000000000000000, 1.000000000000000000 ) ) ;
#776=CARTESIAN_POINT ( 'NONE',  ( 0.000000000000000000, 0.000000000000000000, 0.000000000000000000 ) ) ;
#777=LINE ( 'NONE', #19128, #4471 ) ;
#782=EDGE_CURVE ( 'NONE', #11100, #20998, #1173, .T. ) ;
#783=VERTEX_POINT ( 'NONE', #9569 ) ;
#785=EDGE_CURVE ( 'NONE', #13297, #18504, #11406, .T. ) ;
#786=AXIS2_PLACEMENT_3D ( 'NONE', #20099, #4960, #11696 ) ;
#788=CARTESIAN_POINT ( 'NONE',  ( 0.000000000000000000, 0.000000000000000000, 0.000000000000000000 ) ) ;
#791=VERTEX_POINT ( 'NONE', #5849 ) ;
#794=CARTESIAN_POINT ( 'NONE',  ( 0.000000000000000000, -77.39385041987125646, -35.28996114464684553 ) ) ;
#795=CIRCLE ( 'NONE', #461, 92.50100000000000477 ) ;
#797=VERTEX_POINT ( 'NONE', #5957 ) ;
#799=CARTESIAN_POINT ( 'NONE',  ( 0.000000000000000000, -21.65267340503189430, -89.93106657554454841 ) ) ;
#803=DIRECTION ( 'NONE',  ( 1.000000000000000000, 0.000000000000000000, 0.000000000000000000 ) ) ;
#804=DIRECTION ( 'NONE',  ( -1.000000000000000000, -0.000000000000000000, -0.000000000000000000 ) ) ;
#805=FACE_OUTER_BOUND ( 'NONE', #14332, .T. ) ;
#807=FACE_OUTER_BOUND ( 'NONE', #17843, .T. ) ;
#809=CIRCLE ( 'NONE', #16569, 44.99999999999999289 ) ;
#812=ORIENTED_EDGE ( 'NONE', *, *, #20256, .F. ) ;
#813=DIRECTION ( 'NONE',  ( -1.000000000000000000, 0.000000000000000000, 0.000000000000000000 ) ) ;
#814=ADVANCED_FACE ( 'NONE', ( #4516 ), #18101, .F. ) ;
#815=AXIS2_PLACEMENT_3D ( 'NONE', #14347, #14231, #7936 ) ;
#816=EDGE_LOOP ( 'NONE', ( #4202, #19739, #5033, #17926 ) ) ;
#820=CARTESIAN_POINT ( 'NONE',  ( 10.00000000000000000, 83.35585896458643163, -16.94078559807864792 ) ) ;
#821=ORIENTED_EDGE ( 'NONE', *, *, #4046, .T. ) ;
#824=ADVANCED_FACE ( 'NONE', ( #16766 ), #1311, .F. ) ;
#825=ORIENTED_EDGE ( 'NONE', *, *, #12856, .T. ) ;
#827=VERTEX_POINT ( 'NONE', #10017 ) ;
#828=FACE_OUTER_BOUND ( 'NONE', #3218, .T. ) ;
#829=LINE ( 'NONE', #21054, #6628 ) ;
#831=EDGE_CURVE ( 'NONE', #10390, #7164, #20196, .T. ) ;
#832=CIRCLE ( 'NONE', #8597, 88.00000000000000000 ) ;
#833=CARTESIAN_POINT ( 'NONE',  ( 0.000000000000000000, 0.000000000000000000, 0.000000000000000000 ) ) ;
#835=DIRECTION ( 'NONE',  ( -1.000000000000000000, -0.000000000000000000, -0.000000000000000000 ) ) ;
#836=DIRECTION ( 'NONE',  ( 0.000000000000000000, 0.000000000000000000, 1.000000000000000000 ) ) ;
#837=EDGE_CURVE ( 'NONE', #11042, #12235, #8052, .T. ) ;
#838=DIRECTION ( 'NONE',  ( -1.000000000000000000, 0.000000000000000000, 0.000000000000000000 ) ) ;
#841=CARTESIAN_POINT ( 'NONE',  ( 10.00000000000000000, 0.000000000000000000, 0.000000000000000000 ) ) ;
#843=LINE ( 'NONE', #5831, #6195 ) ;
#845=VERTEX_POINT ( 'NONE', #3400 ) ;
#846=CIRCLE ( 'NONE', #10371, 92.50100000000000477 ) ;
#847=CARTESIAN_POINT ( 'NONE',  ( 10.00000000000000000, -24.89070495400792637, 84.40647372620493627 ) ) ;
#849=DIRECTION ( 'NONE',  ( 0.000000000000000000, 0.000000000000000000, 1.000000000000000000 ) ) ;
#851=EDGE_CURVE ( 'NONE', #1324, #20085, #15279, .T. ) ;
#852=CIRCLE ( 'NONE', #19198, 92.50099999999999056 ) ;
#857=CIRCLE ( 'NONE', #10034, 92.50100000000000477 ) ;
#859=LINE ( 'NONE', #15895, #13012 ) ;
#860=CYLINDRICAL_SURFACE ( 'NONE', #6187, 44.99999999999999289 ) ;
#862=EDGE_CURVE ( 'NONE', #10755, #14140, #4705, .T. ) ;
#863=LINE ( 'NONE', #3186, #9617 ) ;
#864=EDGE_CURVE ( 'NONE', #15586, #17743, #13558, .T. ) ;
#866=DIRECTION ( 'NONE',  ( -1.000000000000000000, 0.000000000000000000, 0.000000000000000000 ) ) ;
#868=CARTESIAN_POINT ( 'NONE',  ( 0.000000000000000000, 3.728035544477412255, -84.97818067823766341 ) ) ;
#870=CARTESIAN_POINT ( 'NONE',  ( 10.00000000000000000, 15.51843147776349063, 83.63233659819657362 ) ) ;
#871=VECTOR ( 'NONE', #754, 1000.000000000000000 ) ;
#872=CARTESIAN_POINT ( 'NONE',  ( 0.000000000000000000, -16.79755869217711250, 90.96305306542248559 ) ) ;
#875=ORIENTED_EDGE ( 'NONE', *, *, #21748, .F. ) ;
#876=VECTOR ( 'NONE', #14562, 1000.000000000000000 ) ;
#877=ORIENTED_EDGE ( 'NONE', *, *, #15846, .T. ) ;
#879=VERTEX_POINT ( 'NONE', #13337 ) ;
#881=FACE_OUTER_BOUND ( 'NONE', #9645, .T. ) ;
#883=CARTESIAN_POINT ( 'NONE',  ( 10.00000000000000000, -83.89484365856893078, -26.56417150043033359 ) ) ;
#885=AXIS2_PLACEMENT_3D ( 'NONE', #19974, #18332, #18752 ) ;
#886=LINE ( 'NONE', #9268, #11719 ) ;
#887=CARTESIAN_POINT ( 'NONE',  ( 10.00000000000000000, 0.000000000000000000, 0.000000000000000000 ) ) ;
#890=CIRCLE ( 'NONE', #6565, 92.50099999999999056 ) ;
#892=DIRECTION ( 'NONE',  ( 1.000000000000000000, 0.000000000000000000, 0.000000000000000000 ) ) ;
#893=DIRECTION ( 'NONE',  ( 0.000000000000000000, -0.1391731009600725710, 0.9902680687415692518 ) ) ;
#894=AXIS2_PLACEMENT_3D ( 'NONE', #6128, #12845, #14176 ) ;
#898=CIRCLE ( 'NONE', #16789, 44.99999999999998579 ) ;
#901=CYLINDRICAL_SURFACE ( 'NONE', #8136, 44.99999999999999289 ) ;
#902=ORIENTED_EDGE ( 'NONE', *, *, #2575, .T. ) ;
#903=DIRECTION ( 'NONE',  ( 1.000000000000000000, 0.000000000000000000, 0.000000000000000000 ) ) ;
#904=ORIENTED_EDGE ( 'NONE', *, *, #20980, .F. ) ;
#905=ORIENTED_EDGE ( 'NONE', *, *, #5519, .T. ) ;
#906=FACE_OUTER_BOUND ( 'NONE', #19726, .T. ) ;
#909=CIRCLE ( 'NONE', #10107, 45.00000000000000000 ) ;
#911=CARTESIAN_POINT ( 'NONE',  ( 10.00000000000000000, 56.05743251323954013, -67.83483072893743326 ) ) ;
#913=DIRECTION ( 'NONE',  ( 1.000000000000000000, -0.000000000000000000, 0.000000000000000000 ) ) ;
#914=CIRCLE ( 'NONE', #11508, 44.99999999999999289 ) ;
#915=DIRECTION ( 'NONE',  ( -1.000000000000000000, -0.000000000000000000, 0.000000000000000000 ) ) ;
#917=CARTESIAN_POINT ( 'NONE',  ( 10.00000000000000000, -72.53479564998751528, -44.42851404693431761 ) ) ;
#918=CARTESIAN_POINT ( 'NONE',  ( 10.00000000000000000, 84.79630770241077187, 6.691460262316813790 ) ) ;
#919=EDGE_CURVE ( 'NONE', #1655, #12268, #20311, .T. ) ;
#920=CARTESIAN_POINT ( 'NONE',  ( 10.00000000000000000, 78.83848282823974785, -48.38314403117421847 ) ) ;
#923=VERTEX_POINT ( 'NONE', #6621 ) ;
#925=ORIENTED_EDGE ( 'NONE', *, *, #3398, .F. ) ;
#926=VECTOR ( 'NONE', #988, 1000.000000000000000 ) ;
#927=CIRCLE ( 'NONE', #12927, 92.50099999999999056 ) ;
#929=FACE_OUTER_BOUND ( 'NONE', #18523, .T. ) ;
#931=CARTESIAN_POINT ( 'NONE',  ( 10.00000000000000000, -79.66702613806795341, 29.80527447819410369 ) ) ;
#935=VERTEX_POINT ( 'NONE', #3072 ) ;
#936=EDGE_CURVE ( 'NONE', #17111, #14755, #12097, .T. ) ;
#940=DIRECTION ( 'NONE',  ( 0.000000000000000000, 0.000000000000000000, 1.000000000000000000 ) ) ;
#942=ORIENTED_EDGE ( 'NONE', *, *, #10497, .T. ) ;
#943=CIRCLE ( 'NONE', #18950, 88.00000000000000000 ) ;
#945=CIRCLE ( 'NONE', #13292, 44.99999999999998579 ) ;
#946=DIRECTION ( 'NONE',  ( 0.000000000000000000, -0.9993908270190960952, 0.03489949670249099800 ) ) ;
#947=DIRECTION ( 'NONE',  ( -1.000000000000000000, 0.000000000000000000, 0.000000000000000000 ) ) ;
#950=DIRECTION ( 'NONE',  ( 0.000000000000000000, 0.000000000000000000, 1.000000000000000000 ) ) ;
#952=CARTESIAN_POINT ( 'NONE',  ( 10.00000000000000000, -90.32141448704695108, 19.96189084378191936 ) ) ;
#953=ORIENTED_EDGE ( 'NONE', *, *, #4607, .T. ) ;
#956=CARTESIAN_POINT ( 'NONE',  ( 0.000000000000000000, -82.02147376274702140, 42.76579056660835221 ) ) ;
#958=DIRECTION ( 'NONE',  ( 0.000000000000000000, 0.000000000000000000, 1.000000000000000000 ) ) ;
#960=AXIS2_PLACEMENT_3D ( 'NONE', #12650, #6149, #14100 ) ;
#961=DIRECTION ( 'NONE',  ( 0.000000000000000000, 0.000000000000000000, 1.000000000000000000 ) ) ;
#963=EDGE_LOOP ( 'NONE', ( #18501, #329, #19096, #19394 ) ) ;
#964=CARTESIAN_POINT ( 'NONE',  ( 10.00000000000000000, 0.000000000000000000, 0.000000000000000000 ) ) ;
#965=CIRCLE ( 'NONE', #3448, 88.00000000000000000 ) ;
#966=VERTEX_POINT ( 'NONE', #10244 ) ;
#968=EDGE_LOOP ( 'NONE', ( #5803, #6928, #18960, #21650 ) ) ;
#969=EDGE_CURVE ( 'NONE', #1449, #453, #1838, .T. ) ;
#971=VERTEX_POINT ( 'NONE', #12335 ) ;
#972=FACE_OUTER_BOUND ( 'NONE', #9390, .T. ) ;
#975=DIRECTION ( 'NONE',  ( 1.000000000000000000, 0.000000000000000000, 0.000000000000000000 ) ) ;
#976=CARTESIAN_POINT ( 'NONE',  ( 0.000000000000000000, 17.64925110578583300, -86.21197095186326464 ) ) ;
#977=AXIS2_PLACEMENT_3D ( 'NONE', #21570, #6448, #15046 ) ;
#978=VECTOR ( 'NONE', #19817, 1000.000000000000000 ) ;
#979=DIRECTION ( 'NONE',  ( 0.000000000000000000, 0.000000000000000000, -1.000000000000000000 ) ) ;
#980=DIRECTION ( 'NONE',  ( 1.000000000000000000, 0.000000000000000000, 0.000000000000000000 ) ) ;
#981=AXIS2_PLACEMENT_3D ( 'NONE', #13424, #14758, #11554 ) ;
#982=AXIS2_PLACEMENT_3D ( 'NONE', #15495, #7108, #13941 ) ;
#983=DIRECTION ( 'NONE',  ( 0.000000000000000000, 0.000000000000000000, 1.000000000000000000 ) ) ;
#986=ADVANCED_FACE ( 'NONE', ( #8697 ), #2070, .F. ) ;
#988=DIRECTION ( 'NONE',  ( -1.000000000000000000, -0.000000000000000000, 0.000000000000000000 ) ) ;
#990=EDGE_LOOP ( 'NONE', ( #16974, #16725, #17713, #12754 ) ) ;
#992=EDGE_CURVE ( 'NONE', #10156, #6719, #16864, .T. ) ;
#995=VECTOR ( 'NONE', #18944, 1000.000000000000000 ) ;
#997=CIRCLE ( 'NONE', #15090, 92.50100000000000477 ) ;
#998=AXIS2_PLACEMENT_3D ( 'NONE', #20798, #10950, #12491 ) ;
#999=ORIENTED_EDGE ( 'NONE', *, *, #7471, .T. ) ;
#1000=CARTESIAN_POINT ( 'NONE',  ( 5.000000000000000000, 47.19205848891765243, 74.27590198428138990 ) ) ;
#1002=VERTEX_POINT ( 'NONE', #197 ) ;
#1003=CARTESIAN_POINT ( 'NONE',  ( 0.000000000000000000, 87.92084725184948013, 3.731570516143270400 ) ) ;
#1006=CARTESIAN_POINT ( 'NONE',  ( 10.00000000000000000, 0.000000000000000000, 0.000000000000000000 ) ) ;
#1007=DIRECTION ( 'NONE',  ( 0.000000000000000000, 0.000000000000000000, 1.000000000000000000 ) ) ;
#1012=VECTOR ( 'NONE', #19204, 1000.000000000000000 ) ;
#1014=CIRCLE ( 'NONE', #12642, 88.00000000000000000 ) ;
#1015=ORIENTED_EDGE ( 'NONE', *, *, #12966, .F. ) ;
#1016=AXIS2_PLACEMENT_3D ( 'NONE', #2312, #2525, #9046 ) ;
#1018=ORIENTED_EDGE ( 'NONE', *, *, #21788, .T. ) ;
#1019=DIRECTION ( 'NONE',  ( 1.000000000000000000, 0.000000000000000000, 0.000000000000000000 ) ) ;
#1020=DIRECTION ( 'NONE',  ( 1.000000000000000000, 0.000000000000000000, 0.000000000000000000 ) ) ;
#1021=ORIENTED_EDGE ( 'NONE', *, *, #19486, .T. ) ;
#1022=DIRECTION ( 'NONE',  ( -1.000000000000000000, 0.000000000000000000, 0.000000000000000000 ) ) ;
#1023=EDGE_LOOP ( 'NONE', ( #18094, #13299, #11011, #7678 ) ) ;
#1026=CARTESIAN_POINT ( 'NONE',  ( 10.00000000000000000, -64.95266917914358373, 59.37298010462950515 ) ) ;
#1027=EDGE_LOOP ( 'NONE', ( #1374, #15749, #17083, #5933 ) ) ;
#1029=ORIENTED_EDGE ( 'NONE', *, *, #440, .T. ) ;
#1030=DIRECTION ( 'NONE',  ( -1.000000000000000000, 0.000000000000000000, 0.000000000000000000 ) ) ;
#1032=CIRCLE ( 'NONE', #15506, 44.99999999999998579 ) ;
#1033=CARTESIAN_POINT ( 'NONE',  ( 0.000000000000000000, -51.18896083639317851, 71.57995730992162464 ) ) ;
#1034=CYLINDRICAL_SURFACE ( 'NONE', #2287, 44.99999999999999289 ) ;
#1035=CARTESIAN_POINT ( 'NONE',  ( 10.00000000000000000, 65.83713140174806711, -58.39068529131128571 ) ) ;
#1036=FACE_OUTER_BOUND ( 'NONE', #4942, .T. ) ;
#1037=DIRECTION ( 'NONE',  ( 1.000000000000000000, 0.000000000000000000, 0.000000000000000000 ) ) ;
#1038=DIRECTION ( 'NONE',  ( -1.000000000000000000, -0.000000000000000000, 0.000000000000000000 ) ) ;
#1040=DIRECTION ( 'NONE',  ( 0.000000000000000000, 0.000000000000000000, 1.000000000000000000 ) ) ;
#1042=FACE_OUTER_BOUND ( 'NONE', #8115, .T. ) ;
#1044=EDGE_CURVE ( 'NONE', #19647, #12067, #12628, .T. ) ;
#1046=VERTEX_POINT ( 'NONE', #12111 ) ;
#1048=CIRCLE ( 'NONE', #12678, 44.99999999999999289 ) ;
#1051=ORIENTED_EDGE ( 'NONE', *, *, #20140, .T. ) ;
#1052=EDGE_CURVE ( 'NONE', #10469, #1594, #17418, .T. ) ;
#1057=DIRECTION ( 'NONE',  ( 0.000000000000000000, -0.9271838545667832054, -0.3746065934159225619 ) ) ;
#1058=LINE ( 'NONE', #12541, #19335 ) ;
#1059=ORIENTED_EDGE ( 'NONE', *, *, #15255, .F. ) ;
#1060=CARTESIAN_POINT ( 'NONE',  ( -10.00000000000000000, 0.000000000000000000, 0.000000000000000000 ) ) ;
#1061=DIRECTION ( 'NONE',  ( -1.000000000000000000, -0.000000000000000000, -0.000000000000000000 ) ) ;
#1062=CYLINDRICAL_SURFACE ( 'NONE', #1947, 92.50100000000000477 ) ;
#1065=DIRECTION ( 'NONE',  ( 1.000000000000000000, 0.000000000000000000, 0.000000000000000000 ) ) ;
#1066=VERTEX_POINT ( 'NONE', #3832 ) ;
#1072=ORIENTED_EDGE ( 'NONE', *, *, #21649, .T. ) ;
#1075=VERTEX_POINT ( 'NONE', #12011 ) ;
#1077=ORIENTED_EDGE ( 'NONE', *, *, #16064, .F. ) ;
#1078=ORIENTED_EDGE ( 'NONE', *, *, #3097, .T. ) ;
#1079=DIRECTION ( 'NONE',  ( 0.000000000000000000, -5.396917480816734322E-15, -1.000000000000000000 ) ) ;
#1081=ADVANCED_FACE ( 'NONE', ( #10457 ), #1957, .F. ) ;
#1083=CARTESIAN_POINT ( 'NONE',  ( 10.00000000000000000, 0.000000000000000000, 0.000000000000000000 ) ) ;
#1086=EDGE_CURVE ( 'NONE', #10454, #12130, #13989, .T. ) ;
#1087=DIRECTION ( 'NONE',  ( 1.000000000000000000, 0.000000000000000000, 0.000000000000000000 ) ) ;
#1089=VECTOR ( 'NONE', #5047, 1000.000000000000000 ) ;
#1090=DIRECTION ( 'NONE',  ( 0.000000000000000000, -0.9945218953682722907, -0.1045284632676634767 ) ) ;
#1092=ADVANCED_FACE ( 'NONE', ( #10571 ), #8896, .F. ) ;
#1094=ADVANCED_FACE ( 'NONE', ( #10890 ), #9439, .F. ) ;
#1095=FACE_OUTER_BOUND ( 'NONE', #12563, .T. ) ;
#1096=VERTEX_POINT ( 'NONE', #21276 ) ;
#1099=VERTEX_POINT ( 'NONE', #11111 ) ;
#1100=ORIENTED_EDGE ( 'NONE', *, *, #14360, .T. ) ;
#1102=ORIENTED_EDGE ( 'NONE', *, *, #8383, .T. ) ;
#1105=ORIENTED_EDGE ( 'NONE', *, *, #19818, .F. ) ;
#1109=DIRECTION ( 'NONE',  ( -1.000000000000000000, 0.000000000000000000, 0.000000000000000000 ) ) ;
#1112=EDGE_CURVE ( 'NONE', #13174, #7194, #7347, .T. ) ;
#1113=CARTESIAN_POINT ( 'NONE',  ( -10.00000000000000000, 0.000000000000000000, 0.000000000000000000 ) ) ;
#1118=DIRECTION ( 'NONE',  ( -1.000000000000000000, -0.000000000000000000, -0.000000000000000000 ) ) ;
#1119=EDGE_CURVE ( 'NONE', #6824, #5168, #17976, .T. ) ;
#1120=VERTEX_POINT ( 'NONE', #17749 ) ;
#1122=EDGE_CURVE ( 'NONE', #1840, #510, #2828, .T. ) ;
#1124=DIRECTION ( 'NONE',  ( 0.000000000000000000, 0.000000000000000000, 1.000000000000000000 ) ) ;
#1125=ORIENTED_EDGE ( 'NONE', *, *, #2337, .T. ) ;
#1130=DIRECTION ( 'NONE',  ( 1.000000000000000000, -0.000000000000000000, 0.000000000000000000 ) ) ;
#1132=ORIENTED_EDGE ( 'NONE', *, *, #4715, .F. ) ;
#1134=CARTESIAN_POINT ( 'NONE',  ( 5.000000000000002665, -17.64925110578526812, 86.21197095186339254 ) ) ;
#1135=ADVANCED_FACE ( 'NONE', ( #2497 ), #9223, .F. ) ;
#1136=DIRECTION ( 'NONE',  ( -1.000000000000000000, -0.000000000000000000, -0.000000000000000000 ) ) ;
#1137=VECTOR ( 'NONE', #21789, 1000.000000000000000 ) ;
#1138=DIRECTION ( 'NONE',  ( -1.000000000000000000, 0.000000000000000000, -0.000000000000000000 ) ) ;
#1139=DIRECTION ( 'NONE',  ( 0.000000000000000000, 0.000000000000000000, 1.000000000000000000 ) ) ;
#1140=DIRECTION ( 'NONE',  ( -1.000000000000000000, 0.000000000000000000, -0.000000000000000000 ) ) ;
#1141=CYLINDRICAL_SURFACE ( 'NONE', #4749, 88.00000000000000000 ) ;
#1143=FACE_OUTER_BOUND ( 'NONE', #3471, .T. ) ;
#1145=FACE_OUTER_BOUND ( 'NONE', #10184, .T. ) ;
#1146=AXIS2_PLACEMENT_3D ( 'NONE', #6429, #8181, #19885 ) ;
#1147=EDGE_LOOP ( 'NONE', ( #21730, #17643, #10337, #13826 ) ) ;
#1148=AXIS2_PLACEMENT_3D ( 'NONE', #12342, #2173, #10349 ) ;
#1149=DIRECTION ( 'NONE',  ( -1.000000000000000000, -0.000000000000000000, -0.000000000000000000 ) ) ;
#1150=ORIENTED_EDGE ( 'NONE', *, *, #10525, .T. ) ;
#1154=LINE ( 'NONE', #7564, #6347 ) ;
#1155=ORIENTED_EDGE ( 'NONE', *, *, #4441, .F. ) ;
#1156=EDGE_LOOP ( 'NONE', ( #622, #6943, #3985, #9583 ) ) ;
#1157=CIRCLE ( 'NONE', #4338, 92.50100000000000477 ) ;
#1158=AXIS2_PLACEMENT_3D ( 'NONE', #19000, #8927, #14126 ) ;
#1161=CARTESIAN_POINT ( 'NONE',  ( 0.000000000000000000, 73.32282170386913833, -48.65967342042704757 ) ) ;
#1163=AXIS2_PLACEMENT_3D ( 'NONE', #13630, #11866, #16624 ) ;
#1164=ORIENTED_EDGE ( 'NONE', *, *, #12479, .T. ) ;
#1165=AXIS2_PLACEMENT_3D ( 'NONE', #5657, #19239, #3886 ) ;
#1166=DIRECTION ( 'NONE',  ( 0.000000000000000000, -0.6946583704589887054, -0.7193398003386594075 ) ) ;
#1167=DIRECTION ( 'NONE',  ( -1.000000000000000000, 0.000000000000000000, 0.000000000000000000 ) ) ;
#1168=CARTESIAN_POINT ( 'NONE',  ( 0.000000000000000000, 81.97107881582226696, -22.71412948308482171 ) ) ;
#1172=DIRECTION ( 'NONE',  ( 1.000000000000000000, 0.000000000000000000, 0.000000000000000000 ) ) ;
#1173=CIRCLE ( 'NONE', #18468, 44.99999999999999289 ) ;
#1174=CARTESIAN_POINT ( 'NONE',  ( 0.000000000000000000, -29.29369617358407396, -87.74003855418429509 ) ) ;
#1175=ORIENTED_EDGE ( 'NONE', *, *, #10704, .T. ) ;
#1176=AXIS2_PLACEMENT_3D ( 'NONE', #19936, #10094, #16839 ) ;
#1177=FACE_OUTER_BOUND ( 'NONE', #14420, .T. ) ;
#1178=VERTEX_POINT ( 'NONE', #17861 ) ;
#1179=AXIS2_PLACEMENT_3D ( 'NONE', #8319, #21357, #1139 ) ;
#1180=LINE ( 'NONE', #4712, #6697 ) ;
#1181=DIRECTION ( 'NONE',  ( 1.000000000000000000, 0.000000000000000000, 0.000000000000000000 ) ) ;
#1182=VERTEX_POINT ( 'NONE', #5928 ) ;
#1184=VERTEX_POINT ( 'NONE', #21173 ) ;
#1187=EDGE_LOOP ( 'NONE', ( #16962, #16925, #4808, #12317 ) ) ;
#1190=CARTESIAN_POINT ( 'NONE',  ( 0.000000000000000000, -37.96946988134224910, 76.11510229470846411 ) ) ;
#1192=EDGE_CURVE ( 'NONE', #5691, #4328, #1346, .T. ) ;
#1194=CARTESIAN_POINT ( 'NONE',  ( 10.00000000000000000, 52.34334029047875703, 76.26670130689501548 ) ) ;
#1195=AXIS2_PLACEMENT_3D ( 'NONE', #3828, #2594, #4035 ) ;
#1196=DIRECTION ( 'NONE',  ( 0.000000000000000000, 0.000000000000000000, 1.000000000000000000 ) ) ;
#1201=VECTOR ( 'NONE', #7124, 1000.000000000000000 ) ;
#1204=APPLICATION_CONTEXT ( 'automotive_design' ) ;
#1205=EDGE_CURVE ( 'NONE', #6716, #14855, #9432, .T. ) ;
#1207=ORIENTED_EDGE ( 'NONE', *, *, #15551, .F. ) ;
#1210=EDGE_LOOP ( 'NONE', ( #20671, #21312, #12567, #637 ) ) ;
#1213=LINE ( 'NONE', #9932, #21124 ) ;
#1214=CIRCLE ( 'NONE', #9305, 45.00000000000000000 ) ;
#1215=ORIENTED_EDGE ( 'NONE', *, *, #21120, .T. ) ;
#1216=DIRECTION ( 'NONE',  ( 0.000000000000000000, 0.000000000000000000, 1.000000000000000000 ) ) ;
#1218=EDGE_CURVE ( 'NONE', #10690, #21676, #5822, .T. ) ;
#1219=CARTESIAN_POINT ( 'NONE',  ( 10.00000000000000000, 90.32141448704707898, -19.96189084378132961 ) ) ;
#1221=EDGE_CURVE ( 'NONE', #15501, #16339, #9099, .T. ) ;
#1222=LINE ( 'NONE', #8076, #3271 ) ;
#1225=VECTOR ( 'NONE', #19473, 1000.000000000000000 ) ;
#1227=DIRECTION ( 'NONE',  ( 0.000000000000000000, 0.000000000000000000, 1.000000000000000000 ) ) ;
#1228=ORIENTED_EDGE ( 'NONE', *, *, #17732, .F. ) ;
#1230=EDGE_CURVE ( 'NONE', #16156, #10882, #4696, .T. ) ;
#1231=CIRCLE ( 'NONE', #1578, 44.99999999999999289 ) ;
#1239=ORIENTED_EDGE ( 'NONE', *, *, #864, .F. ) ;
#1240=DIRECTION ( 'NONE',  ( 0.000000000000000000, 0.000000000000000000, 1.000000000000000000 ) ) ;
#1243=CIRCLE ( 'NONE', #5123, 92.50100000000000477 ) ;
#1244=DIRECTION ( 'NONE',  ( 0.000000000000000000, 0.000000000000000000, 1.000000000000000000 ) ) ;
#1246=VERTEX_POINT ( 'NONE', #16633 ) ;
#1248=DIRECTION ( 'NONE',  ( -1.000000000000000000, -0.000000000000000000, 0.000000000000000000 ) ) ;
#1249=EDGE_CURVE ( 'NONE', #19371, #752, #11324, .T. ) ;
#1250=CYLINDRICAL_SURFACE ( 'NONE', #527, 44.99999999999999289 ) ;
#1251=CARTESIAN_POINT ( 'NONE',  ( 10.00000000000000000, 80.18694381077108346, 28.37681241246682973 ) ) ;
#1252=CIRCLE ( 'NONE', #894, 88.00000000000000000 ) ;
#1253=AXIS2_PLACEMENT_3D ( 'NONE', #9998, #13203, #16535 ) ;
#1256=AXIS2_PLACEMENT_3D ( 'NONE', #11906, #8897, #17210 ) ;
#1257=LINE ( 'NONE', #11412, #5780 ) ;
#1258=DIRECTION ( 'NONE',  ( -1.000000000000000000, -0.000000000000000000, -0.000000000000000000 ) ) ;
#1260=AXIS2_PLACEMENT_3D ( 'NONE', #11047, #7847, #16138 ) ;
#1262=EDGE_CURVE ( 'NONE', #3326, #13846, #13699, .T. ) ;
#1263=VERTEX_POINT ( 'NONE', #1394 ) ;
#1265=EDGE_CURVE ( 'NONE', #12668, #14422, #17222, .T. ) ;
#1267=DIRECTION ( 'NONE',  ( 0.000000000000000000, 1.233581138472396191E-14, -1.000000000000000000 ) ) ;
#1270=EDGE_CURVE ( 'NONE', #783, #19484, #3805, .T. ) ;
#1271=LINE ( 'NONE', #16835, #19594 ) ;
#1272=AXIS2_PLACEMENT_3D ( 'NONE', #2049, #5687, #15524 ) ;
#1276=AXIS2_PLACEMENT_3D ( 'NONE', #7395, #19201, #751 ) ;
#1277=ORIENTED_EDGE ( 'NONE', *, *, #3532, .T. ) ;
#1278=ORIENTED_EDGE ( 'NONE', *, *, #13906, .T. ) ;
#1283=DIRECTION ( 'NONE',  ( -1.000000000000000000, 0.000000000000000000, 0.000000000000000000 ) ) ;
#1284=CYLINDRICAL_SURFACE ( 'NONE', #17187, 88.00000000000000000 ) ;
#1286=DIRECTION ( 'NONE',  ( 0.000000000000000000, 0.000000000000000000, 1.000000000000000000 ) ) ;
#1287=LINE ( 'NONE', #19321, #4356 ) ;
#1291=ORIENTED_EDGE ( 'NONE', *, *, #19736, .T. ) ;
#1297=VERTEX_POINT ( 'NONE', #11764 ) ;
#1300=ORIENTED_EDGE ( 'NONE', *, *, #1463, .T. ) ;
#1301=DIRECTION ( 'NONE',  ( 1.000000000000000000, 0.000000000000000000, 0.000000000000000000 ) ) ;
#1302=ORIENTED_EDGE ( 'NONE', *, *, #18247, .F. ) ;
#1303=AXIS2_PLACEMENT_3D ( 'NONE', #16732, #1603, #18410 ) ;
#1305=VERTEX_POINT ( 'NONE', #3154 ) ;
#1306=CARTESIAN_POINT ( 'NONE',  ( 10.00000000000000000, -31.15801000616886896, 79.14775961996379294 ) ) ;
#1307=AXIS2_PLACEMENT_3D ( 'NONE', #8958, #3991, #7524 ) ;
#1311=CYLINDRICAL_SURFACE ( 'NONE', #20232, 44.99999999999999289 ) ;
#1312=SURFACE_SIDE_STYLE ('',( #21739 ) ) ;
#1313=CARTESIAN_POINT ( 'NONE',  ( 0.000000000000000000, -60.65655256511196569, -59.63197188857583342 ) ) ;
#1315=CARTESIAN_POINT ( 'NONE',  ( 10.00000000000000000, 0.000000000000000000, 0.000000000000000000 ) ) ;
#1316=FACE_OUTER_BOUND ( 'NONE', #17117, .T. ) ;
#1317=CIRCLE ( 'NONE', #17186, 44.99999999999999289 ) ;
#1318=DIRECTION ( 'NONE',  ( 0.000000000000000000, 0.000000000000000000, 1.000000000000000000 ) ) ;
#1319=AXIS2_PLACEMENT_3D ( 'NONE', #12252, #2196, #5855 ) ;
#1321=ORIENTED_EDGE ( 'NONE', *, *, #7879, .T. ) ;
#1323=ORIENTED_EDGE ( 'NONE', *, *, #12827, .F. ) ;
#1324=VERTEX_POINT ( 'NONE', #16847 ) ;
#1325=ORIENTED_EDGE ( 'NONE', *, *, #4026, .F. ) ;
#1327=EDGE_LOOP ( 'NONE', ( #11454, #5915, #8351, #1352 ) ) ;
#1328=CARTESIAN_POINT ( 'NONE',  ( 10.00000000000000000, 79.66702613806732813, 29.80527447819576636 ) ) ;
#1329=CIRCLE ( 'NONE', #19320, 44.99999999999999289 ) ;
#1332=CIRCLE ( 'NONE', #12251, 44.99999999999999289 ) ;
#1334=DIRECTION ( 'NONE',  ( -1.000000000000000000, 0.000000000000000000, 0.000000000000000000 ) ) ;
#1336=CARTESIAN_POINT ( 'NONE',  ( 0.000000000000000000, 0.000000000000000000, 0.000000000000000000 ) ) ;
#1338=DIRECTION ( 'NONE',  ( -1.000000000000000000, 0.000000000000000000, 0.000000000000000000 ) ) ;
#1339=CYLINDRICAL_SURFACE ( 'NONE', #15828, 44.99999999999999289 ) ;
#1341=DIRECTION ( 'NONE',  ( 0.000000000000000000, -0.8660254037844328234, -0.5000000000000101030 ) ) ;
#1343=ADVANCED_FACE ( 'NONE', ( #16525 ), #1284, .F. ) ;
#1345=EDGE_CURVE ( 'NONE', #12967, #75, #20006, .T. ) ;
#1346=CIRCLE ( 'NONE', #12978, 45.00000000000000000 ) ;
#1347=VERTEX_POINT ( 'NONE', #18073 ) ;
#1349=CARTESIAN_POINT ( 'NONE',  ( 0.000000000000000000, 0.000000000000000000, 88.00000000000000000 ) ) ;
#1352=ORIENTED_EDGE ( 'NONE', *, *, #16064, .T. ) ;
#1353=ORIENTED_EDGE ( 'NONE', *, *, #11192, .F. ) ;
#1355=VERTEX_POINT ( 'NONE', #14863 ) ;
#1359=AXIS2_PLACEMENT_3D ( 'NONE', #1891, #8630, #19665 ) ;
#1360=CARTESIAN_POINT ( 'NONE',  ( 10.00000000000000000, 0.000000000000000000, 0.000000000000000000 ) ) ;
#1362=VECTOR ( 'NONE', #12240, 1000.000000000000000 ) ;
#1363=DIRECTION ( 'NONE',  ( 0.000000000000000000, 0.9993908270190955401, 0.03489949670250439701 ) ) ;
#1364=VECTOR ( 'NONE', #2984, 1000.000000000000000 ) ;
#1365=CIRCLE ( 'NONE', #3821, 92.50099999999999056 ) ;
#1367=CIRCLE ( 'NONE', #13714, 44.99999999999999289 ) ;
#1370=CARTESIAN_POINT ( 'NONE',  ( 10.00000000000000000, 84.12297548659704205, 12.59025161327141618 ) ) ;
#1371=DIRECTION ( 'NONE',  ( -1.000000000000000000, 0.000000000000000000, 0.000000000000000000 ) ) ;
#1372=ORIENTED_EDGE ( 'NONE', *, *, #8112, .T. ) ;
#1374=ORIENTED_EDGE ( 'NONE', *, *, #2299, .F. ) ;
#1375=EDGE_CURVE ( 'NONE', #9371, #2869, #9653, .T. ) ;
#1379=EDGE_CURVE ( 'NONE', #12369, #21410, #2346, .T. ) ;
#1382=VECTOR ( 'NONE', #2261, 1000.000000000000000 ) ;
#1385=ORIENTED_EDGE ( 'NONE', *, *, #16876, .F. ) ;
#1386=EDGE_LOOP ( 'NONE', ( #19141, #2368, #1408, #10089 ) ) ;
#1387=VERTEX_POINT ( 'NONE', #8559 ) ;
#1389=DIRECTION ( 'NONE',  ( 1.000000000000000000, 0.000000000000000000, 0.000000000000000000 ) ) ;
#1390=DIRECTION ( 'NONE',  ( -1.000000000000000000, -0.000000000000000000, -0.000000000000000000 ) ) ;
#1392=ADVANCED_FACE ( 'NONE', ( #5252 ), #1924, .F. ) ;
#1393=DIRECTION ( 'NONE',  ( 0.000000000000000000, 0.000000000000000000, 1.000000000000000000 ) ) ;
#1394=CARTESIAN_POINT ( 'NONE',  ( 0.000000000000000000, -87.92084725184945171, -3.731570516143874361 ) ) ;
#1395=DIRECTION ( 'NONE',  ( 1.000000000000000000, 0.000000000000000000, 0.000000000000000000 ) ) ;
#1396=EDGE_CURVE ( 'NONE', #18927, #10469, #10472, .T. ) ;
#1398=CARTESIAN_POINT ( 'NONE',  ( 10.00000000000000000, -10.41137886060169038, 91.91321010181843576 ) ) ;
#1400=CIRCLE ( 'NONE', #679, 88.00000000000000000 ) ;
#1401=AXIS2_PLACEMENT_3D ( 'NONE', #14414, #15956, #9113 ) ;
#1403=EDGE_LOOP ( 'NONE', ( #9580, #19229, #13619, #15952 ) ) ;
#1404=CIRCLE ( 'NONE', #11975, 88.00000000000000000 ) ;
#1405=ADVANCED_FACE ( 'NONE', ( #165 ), #3802, .F. ) ;
#1408=ORIENTED_EDGE ( 'NONE', *, *, #19959, .F. ) ;
#1409=CYLINDRICAL_SURFACE ( 'NONE', #2364, 45.00000000000000000 ) ;
#1411=EDGE_CURVE ( 'NONE', #3473, #4200, #3064, .T. ) ;
#1412=LINE ( 'NONE', #17762, #14791 ) ;
#1413=DIRECTION ( 'NONE',  ( 0.000000000000000000, 0.000000000000000000, 1.000000000000000000 ) ) ;
#1418=CYLINDRICAL_SURFACE ( 'NONE', #16406, 92.50100000000000477 ) ;
#1422=DIRECTION ( 'NONE',  ( 1.000000000000000000, 0.000000000000000000, 0.000000000000000000 ) ) ;
#1423=DIRECTION ( 'NONE',  ( 0.000000000000000000, -0.8660254037844432595, 0.4999999999999920064 ) ) ;
#1424=DIRECTION ( 'NONE',  ( 0.000000000000000000, 0.000000000000000000, 1.000000000000000000 ) ) ;
#1425=CARTESIAN_POINT ( 'NONE',  ( 10.00000000000000000, 0.000000000000000000, 0.000000000000000000 ) ) ;
#1427=CARTESIAN_POINT ( 'NONE',  ( 0.000000000000000000, -87.44637528609668209, 9.855528870798345054 ) ) ;
#1429=CARTESIAN_POINT ( 'NONE',  ( 10.00000000000000000, 36.60317927562579854, 76.78148674856777234 ) ) ;
#1430=DIRECTION ( 'NONE',  ( 0.000000000000000000, -0.9271838545667908660, 0.3746065934159032440 ) ) ;
#1434=ORIENTED_EDGE ( 'NONE', *, *, #5820, .F. ) ;
#1435=VERTEX_POINT ( 'NONE', #10218 ) ;
#1437=ORIENTED_EDGE ( 'NONE', *, *, #9467, .F. ) ;
#1438=DIRECTION ( 'NONE',  ( 1.000000000000000000, 0.000000000000000000, 0.000000000000000000 ) ) ;
#1439=VERTEX_POINT ( 'NONE', #11874 ) ;
#1440=CYLINDRICAL_SURFACE ( 'NONE', #16326, 44.99999999999999289 ) ;
#1441=AXIS2_PLACEMENT_3D ( 'NONE', #1677, #1785, #8419 ) ;
#1442=DIRECTION ( 'NONE',  ( -1.000000000000000000, -0.000000000000000000, 0.000000000000000000 ) ) ;
#1443=CYLINDRICAL_SURFACE ( 'NONE', #8906, 88.00000000000000000 ) ;
#1444=DIRECTION ( 'NONE',  ( 0.000000000000000000, 0.7880107536067190166, 0.6156614753256620665 ) ) ;
#1447=ORIENTED_EDGE ( 'NONE', *, *, #12333, .F. ) ;
#1448=DIRECTION ( 'NONE',  ( -1.000000000000000000, -0.000000000000000000, -0.000000000000000000 ) ) ;
#1449=VERTEX_POINT ( 'NONE', #8978 ) ;
#1453=CARTESIAN_POINT ( 'NONE',  ( 0.000000000000000000, 85.05652083079334602, 0.7600687895874258526 ) ) ;
#1455=EDGE_LOOP ( 'NONE', ( #11743, #5949, #5509, #16369 ) ) ;
#1458=LINE ( 'NONE', #1569, #6882 ) ;
#1461=AXIS2_PLACEMENT_3D ( 'NONE', #17185, #15619, #15402 ) ;
#1462=CARTESIAN_POINT ( 'NONE',  ( 10.00000000000000000, 83.89484365856945658, -26.56417150042864961 ) ) ;
#1463=EDGE_CURVE ( 'NONE', #1099, #19677, #945, .T. ) ;
#1464=DIRECTION ( 'NONE',  ( 1.000000000000000000, 0.000000000000000000, 0.000000000000000000 ) ) ;
#1468=CARTESIAN_POINT ( 'NONE',  ( 0.000000000000000000, -39.87723064937059547, -83.46401306393613595 ) ) ;
#1471=DIRECTION ( 'NONE',  ( -1.000000000000000000, -0.000000000000000000, -0.000000000000000000 ) ) ;
#1474=ORIENTED_EDGE ( 'NONE', *, *, #427, .F. ) ;
#1475=ORIENTED_EDGE ( 'NONE', *, *, #3523, .T. ) ;
#1476=CARTESIAN_POINT ( 'NONE',  ( 10.00000000000000000, -36.39558101400191248, 80.12091913260368869 ) ) ;
#1477=VERTEX_POINT ( 'NONE', #8668 ) ;
#1483=CARTESIAN_POINT ( 'NONE',  ( 5.000000000000002665, 73.32282170386848463, 48.65967342042805655 ) ) ;
#1484=ORIENTED_EDGE ( 'NONE', *, *, #10253, .T. ) ;
#1486=AXIS2_PLACEMENT_3D ( 'NONE', #20493, #17289, #3477 ) ;
#1488=CARTESIAN_POINT ( 'NONE',  ( 5.000000000000002665, 6.797690662956386021, -87.73705831432209834 ) ) ;
#1489=ADVANCED_FACE ( 'NONE', ( #11984 ), #18731, .F. ) ;
#1490=CARTESIAN_POINT ( 'NONE',  ( -10.00000000000000000, 0.000000000000000000, 0.000000000000000000 ) ) ;
#1492=CARTESIAN_POINT ( 'NONE',  ( 0.000000000000000000, 0.000000000000000000, 0.000000000000000000 ) ) ;
#1493=CARTESIAN_POINT ( 'NONE',  ( 10.00000000000000000, 68.93609746931163329, 54.69748134696484954 ) ) ;
#1494=CARTESIAN_POINT ( 'NONE',  ( 0.000000000000000000, 72.53479564998782791, 44.42851404693380601 ) ) ;
#1497=ORIENTED_EDGE ( 'NONE', *, *, #8425, .T. ) ;
#1499=CIRCLE ( 'NONE', #14541, 92.50100000000000477 ) ;
#1500=CARTESIAN_POINT ( 'NONE',  ( 10.00000000000000000, 0.000000000000000000, 0.000000000000000000 ) ) ;
#1501=ORIENTED_EDGE ( 'NONE', *, *, #4741, .F. ) ;
#1502=DIRECTION ( 'NONE',  ( 0.000000000000000000, 0.000000000000000000, 1.000000000000000000 ) ) ;
#1503=EDGE_CURVE ( 'NONE', #750, #2613, #7122, .T. ) ;
#1505=DIRECTION ( 'NONE',  ( 1.000000000000000000, 0.000000000000000000, -0.000000000000000000 ) ) ;
#1508=EDGE_CURVE ( 'NONE', #9443, #9115, #488, .T. ) ;
#1510=ORIENTED_EDGE ( 'NONE', *, *, #6218, .T. ) ;
#1511=CARTESIAN_POINT ( 'NONE',  ( 0.000000000000000000, 46.93287725819779155, 70.94007663282461351 ) ) ;
#1512=ORIENTED_EDGE ( 'NONE', *, *, #11078, .F. ) ;
#1514=AXIS2_PLACEMENT_3D ( 'NONE', #17451, #10596, #3963 ) ;
#1516=DIRECTION ( 'NONE',  ( 0.000000000000000000, -0.9993908270190953180, -0.03489949670251103753 ) ) ;
#1517=CARTESIAN_POINT ( 'NONE',  ( 10.00000000000000000, -8.134922360105496963, -84.67002113262489615 ) ) ;
#1522=LINE ( 'NONE', #15000, #2381 ) ;
#1523=DIRECTION ( 'NONE',  ( -1.000000000000000000, -0.000000000000000000, 0.000000000000000000 ) ) ;
#1525=DIRECTION ( 'NONE',  ( 0.000000000000000000, 0.000000000000000000, 1.000000000000000000 ) ) ;
#1526=CARTESIAN_POINT ( 'NONE',  ( 10.00000000000000000, 75.87763420127893710, -44.57111876559645225 ) ) ;
#1527=CARTESIAN_POINT ( 'NONE',  ( 0.000000000000000000, 37.96946988134172329, 76.11510229470873412 ) ) ;
#1531=CYLINDRICAL_SURFACE ( 'NONE', #20778, 88.00000000000000000 ) ;
#1532=EDGE_LOOP ( 'NONE', ( #8337, #17524, #20603, #12767 ) ) ;
#1533=EDGE_CURVE ( 'NONE', #15558, #11042, #15456, .T. ) ;
#1534=ORIENTED_EDGE ( 'NONE', *, *, #6971, .T. ) ;
#1535=CIRCLE ( 'NONE', #19877, 44.99999999999998579 ) ;
#1536=VERTEX_POINT ( 'NONE', #17620 ) ;
#1537=EDGE_CURVE ( 'NONE', #20116, #18424, #13695, .T. ) ;
#1541=LINE ( 'NONE', #13250, #4532 ) ;
#1542=AXIS2_PLACEMENT_3D ( 'NONE', #18159, #16603, #21791 ) ;
#1544=CARTESIAN_POINT ( 'NONE',  ( 0.000000000000000000, -41.21966518006011881, 82.80926399530274296 ) ) ;
#1545=CARTESIAN_POINT ( 'NONE',  ( -10.00000000000000000, 0.000000000000000000, 0.000000000000000000 ) ) ;
#1547=DIRECTION ( 'NONE',  ( 0.000000000000000000, 0.000000000000000000, 1.000000000000000000 ) ) ;
#1548=CARTESIAN_POINT ( 'NONE',  ( 10.00000000000000000, -18.94217447942500598, -85.93715160505971085 ) ) ;
#1549=DIRECTION ( 'NONE',  ( -1.000000000000000000, 0.000000000000000000, 0.000000000000000000 ) ) ;
#1553=EDGE_LOOP ( 'NONE', ( #10951, #17472, #17504, #2375 ) ) ;
#1555=CIRCLE ( 'NONE', #8604, 92.50099999999999056 ) ;
#1557=ORIENTED_EDGE ( 'NONE', *, *, #1864, .T. ) ;
#1559=CARTESIAN_POINT ( 'NONE',  ( 10.00000000000000000, -32.56745702629792305, 78.57830605990643846 ) ) ;
#1561=ORIENTED_EDGE ( 'NONE', *, *, #8114, .T. ) ;
#1562=DIRECTION ( 'NONE',  ( -1.000000000000000000, -0.000000000000000000, -0.000000000000000000 ) ) ;
#1568=ORIENTED_EDGE ( 'NONE', *, *, #6891, .F. ) ;
#1569=CARTESIAN_POINT ( 'NONE',  ( 10.00000000000000000, 10.41137886060107576, 91.91321010181850681 ) ) ;
#1573=DIRECTION ( 'NONE',  ( -1.000000000000000000, 0.000000000000000000, 0.000000000000000000 ) ) ;
#1577=DIRECTION ( 'NONE',  ( 1.000000000000000000, 0.000000000000000000, 0.000000000000000000 ) ) ;
#1578=AXIS2_PLACEMENT_3D ( 'NONE', #19110, #15572, #5636 ) ;
#1581=CIRCLE ( 'NONE', #11820, 44.99999999999999289 ) ;
#1582=CIRCLE ( 'NONE', #2981, 92.50100000000000477 ) ;
#1584=DIRECTION ( 'NONE',  ( 1.000000000000000000, 0.000000000000000000, -0.000000000000000000 ) ) ;
#1586=VERTEX_POINT ( 'NONE', #12625 ) ;
#1587=EDGE_CURVE ( 'NONE', #1246, #1789, #17719, .T. ) ;
#1590=ORIENTED_EDGE ( 'NONE', *, *, #6143, .F. ) ;
#1593=AXIS2_PLACEMENT_3D ( 'NONE', #19189, #7483, #17757 ) ;
#1594=VERTEX_POINT ( 'NONE', #1035 ) ;
#1596=DIRECTION ( 'NONE',  ( -1.000000000000000000, 0.000000000000000000, -0.000000000000000000 ) ) ;
#1597=AXIS2_PLACEMENT_3D ( 'NONE', #2134, #13512, #12295 ) ;
#1602=CYLINDRICAL_SURFACE ( 'NONE', #13215, 88.00000000000000000 ) ;
#1603=DIRECTION ( 'NONE',  ( -1.000000000000000000, -0.000000000000000000, -0.000000000000000000 ) ) ;
#1604=FACE_OUTER_BOUND ( 'NONE', #18499, .T. ) ;
#1606=DIRECTION ( 'NONE',  ( 0.000000000000000000, 0.000000000000000000, 1.000000000000000000 ) ) ;
#1607=CARTESIAN_POINT ( 'NONE',  ( 0.000000000000000000, -51.18896083639217665, -71.57995730992236361 ) ) ;
#1608=CIRCLE ( 'NONE', #15721, 92.50100000000000477 ) ;
#1610=CYLINDRICAL_SURFACE ( 'NONE', #15878, 44.99999999999998579 ) ;
#1612=ORIENTED_EDGE ( 'NONE', *, *, #473, .T. ) ;
#1615=CARTESIAN_POINT ( 'NONE',  ( 10.00000000000000000, -25.56104204395359503, 81.12843256239655432 ) ) ;
#1617=EDGE_LOOP ( 'NONE', ( #7199, #15983, #11344, #1051 ) ) ;
#1620=EDGE_CURVE ( 'NONE', #8870, #18369, #7699, .T. ) ;
#1622=ORIENTED_EDGE ( 'NONE', *, *, #21444, .F. ) ;
#1623=CARTESIAN_POINT ( 'NONE',  ( 10.00000000000000000, 11.59241532900628258, 87.23311244498744088 ) ) ;
#1624=EDGE_CURVE ( 'NONE', #20752, #12067, #9096, .T. ) ;
#1625=VERTEX_POINT ( 'NONE', #17943 ) ;
#1626=ORIENTED_EDGE ( 'NONE', *, *, #6269, .F. ) ;
#1627=ORIENTED_EDGE ( 'NONE', *, *, #17106, .T. ) ;
#1628=CARTESIAN_POINT ( 'NONE',  ( 10.00000000000000000, -65.64563793391867819, 54.09103124042793098 ) ) ;
#1629=CIRCLE ( 'NONE', #13972, 88.00000000000000000 ) ;
#1634=CARTESIAN_POINT ( 'NONE',  ( 0.000000000000000000, 0.000000000000000000, 0.000000000000000000 ) ) ;
#1635=VECTOR ( 'NONE', #8939, 1000.000000000000000 ) ;
#1640=CARTESIAN_POINT ( 'NONE',  ( 10.00000000000000000, 70.37753541436022431, -60.02863908169562279 ) ) ;
#1641=CARTESIAN_POINT ( 'NONE',  ( 10.00000000000000000, 87.58454185039451545, -8.540961822680756654 ) ) ;
#1643=DIRECTION ( 'NONE',  ( 0.000000000000000000, 0.000000000000000000, 1.000000000000000000 ) ) ;
#1644=DIRECTION ( 'NONE',  ( -1.000000000000000000, -0.000000000000000000, 0.000000000000000000 ) ) ;
#1646=ORIENTED_EDGE ( 'NONE', *, *, #20959, .F. ) ;
#1650=EDGE_LOOP ( 'NONE', ( #20054, #7165, #4558, #9351 ) ) ;
#1655=VERTEX_POINT ( 'NONE', #9524 ) ;
#1659=DIRECTION ( 'NONE',  ( -1.000000000000000000, -0.000000000000000000, 0.000000000000000000 ) ) ;
#1661=EDGE_CURVE ( 'NONE', #14806, #6246, #6021, .T. ) ;
#1662=VECTOR ( 'NONE', #11381, 1000.000000000000000 ) ;
#1664=CIRCLE ( 'NONE', #11180, 44.99999999999999289 ) ;
#1666=EDGE_CURVE ( 'NONE', #1099, #19664, #12402, .T. ) ;
#1669=CYLINDRICAL_SURFACE ( 'NONE', #14435, 92.50100000000000477 ) ;
#1670=ADVANCED_FACE ( 'NONE', ( #10748 ), #16382, .F. ) ;
#1672=ADVANCED_FACE ( 'NONE', ( #6681 ), #11527, .F. ) ;
#1673=CARTESIAN_POINT ( 'NONE',  ( 10.00000000000000000, 0.000000000000000000, 0.000000000000000000 ) ) ;
#1674=ORIENTED_EDGE ( 'NONE', *, *, #1906, .F. ) ;
#1675=ORIENTED_EDGE ( 'NONE', *, *, #15133, .T. ) ;
#1677=CARTESIAN_POINT ( 'NONE',  ( 10.00000000000000000, -84.12297548659712731, -12.59025161327086906 ) ) ;
#1679=ORIENTED_EDGE ( 'NONE', *, *, #15846, .F. ) ;
#1680=CARTESIAN_POINT ( 'NONE',  ( 0.000000000000000000, 10.41137886060228901, -91.91321010181836471 ) ) ;
#1681=ORIENTED_EDGE ( 'NONE', *, *, #10837, .T. ) ;
#1682=ORIENTED_EDGE ( 'NONE', *, *, #15928, .T. ) ;
#1683=AXIS2_PLACEMENT_3D ( 'NONE', #6953, #18660, #20525 ) ;
#1684=SHAPE_DEFINITION_REPRESENTATION ( #10206, #6721 ) ;
#1685=DIRECTION ( 'NONE',  ( 0.000000000000000000, 0.000000000000000000, 1.000000000000000000 ) ) ;
#1687=DIRECTION ( 'NONE',  ( 0.000000000000000000, 0.000000000000000000, -1.000000000000000000 ) ) ;
#1689=DIRECTION ( 'NONE',  ( 0.000000000000000000, 0.6946583704589984753, -0.7193398003386500816 ) ) ;
#1690=DIRECTION ( 'NONE',  ( 1.000000000000000000, -0.000000000000000000, 0.000000000000000000 ) ) ;
#1692=DIRECTION ( 'NONE',  ( 0.000000000000000000, 0.000000000000000000, 1.000000000000000000 ) ) ;
#1693=DIRECTION ( 'NONE',  ( -1.000000000000000000, 0.000000000000000000, 0.000000000000000000 ) ) ;
#1694=AXIS2_PLACEMENT_3D ( 'NONE', #14424, #17642, #2707 ) ;
#1695=CIRCLE ( 'NONE', #2057, 88.00000000000000000 ) ;
#1699=EDGE_CURVE ( 'NONE', #10259, #19663, #7996, .T. ) ;
#1700=LINE ( 'NONE', #8444, #5939 ) ;
#1703=CARTESIAN_POINT ( 'NONE',  ( 0.000000000000000000, 9.646732466566502850, -84.51112348751837544 ) ) ;
#1706=CIRCLE ( 'NONE', #7010, 44.99999999999999289 ) ;
#1707=ORIENTED_EDGE ( 'NONE', *, *, #18953, .T. ) ;
#1708=DIRECTION ( 'NONE',  ( 0.000000000000000000, 0.3420201433256693235, -0.9396926207859080948 ) ) ;
#1710=VECTOR ( 'NONE', #18038, 1000.000000000000000 ) ;
#1711=ORIENTED_EDGE ( 'NONE', *, *, #1870, .T. ) ;
#1714=AXIS2_PLACEMENT_3D ( 'NONE', #19789, #14919, #1227 ) ;
#1716=DIRECTION ( 'NONE',  ( -1.000000000000000000, 0.000000000000000000, -0.000000000000000000 ) ) ;
#1719=DIRECTION ( 'NONE',  ( 0.000000000000000000, 4.085273785925381338E-14, -1.000000000000000000 ) ) ;
#1721=DIRECTION ( 'NONE',  ( 0.000000000000000000, 0.8660254037844399289, -0.4999999999999979461 ) ) ;
#1723=ORIENTED_EDGE ( 'NONE', *, *, #3809, .T. ) ;
#1725=CIRCLE ( 'NONE', #9466, 92.50100000000000477 ) ;
#1727=ORIENTED_EDGE ( 'NONE', *, *, #19063, .T. ) ;
#1728=CARTESIAN_POINT ( 'NONE',  ( -10.00000000000000000, 0.000000000000000000, 0.000000000000000000 ) ) ;
#1732=ORIENTED_EDGE ( 'NONE', *, *, #3834, .F. ) ;
#1733=FACE_OUTER_BOUND ( 'NONE', #6081, .T. ) ;
#1735=ORIENTED_EDGE ( 'NONE', *, *, #9, .T. ) ;
#1739=FACE_OUTER_BOUND ( 'NONE', #2617, .T. ) ;
#1741=CARTESIAN_POINT ( 'NONE',  ( 10.00000000000000000, -52.34334029047821701, -76.26670130689538496 ) ) ;
#1742=VECTOR ( 'NONE', #20832, 1000.000000000000000 ) ;
#1743=CARTESIAN_POINT ( 'NONE',  ( 0.000000000000000000, 0.000000000000000000, 0.000000000000000000 ) ) ;
#1744=AXIS2_PLACEMENT_3D ( 'NONE', #2260, #19067, #13979 ) ;
#1745=PRODUCT ( 'internal spur gear_iso_ISO - Internal spur gear 2M 90T 20PA 10FW ---S90S200OD 1.0AF', 'internal spur gear_iso_ISO - Internal spur gear 2M 90T 20PA 10FW ---S90S200OD 1.0AF', '', ( #4992 ) ) ;
#1747=DIRECTION ( 'NONE',  ( -1.000000000000000000, -0.000000000000000000, 0.000000000000000000 ) ) ;
#1749=DIRECTION ( 'NONE',  ( 0.000000000000000000, -0.8290375725550350738, -0.5591929034707565638 ) ) ;
#1750=CARTESIAN_POINT ( 'NONE',  ( 0.000000000000000000, -87.44637528609653998, -9.855528870799524555 ) ) ;
#1751=DIRECTION ( 'NONE',  ( -1.000000000000000000, -0.000000000000000000, -0.000000000000000000 ) ) ;
#1752=CARTESIAN_POINT ( 'NONE',  ( 0.000000000000000000, -84.33453774737651543, -11.08490790852216534 ) ) ;
#1754=CIRCLE ( 'NONE', #2813, 92.50100000000000477 ) ;
#1755=ORIENTED_EDGE ( 'NONE', *, *, #13137, .F. ) ;
#1756=DIRECTION ( 'NONE',  ( 0.000000000000000000, 0.000000000000000000, 1.000000000000000000 ) ) ;
#1758=AXIS2_PLACEMENT_3D ( 'NONE', #17735, #14521, #21488 ) ;
#1759=DIRECTION ( 'NONE',  ( -1.000000000000000000, -0.000000000000000000, 0.000000000000000000 ) ) ;
#1764=ORIENTED_EDGE ( 'NONE', *, *, #10681, .T. ) ;
#1766=VERTEX_POINT ( 'NONE', #8106 ) ;
#1768=CARTESIAN_POINT ( 'NONE',  ( 10.00000000000000000, 64.95266917914317162, 59.37298010462993858 ) ) ;
#1769=EDGE_CURVE ( 'NONE', #6526, #5588, #20939, .T. ) ;
#1771=EDGE_CURVE ( 'NONE', #13577, #12634, #19883, .T. ) ;
#1774=EDGE_CURVE ( 'NONE', #3544, #13981, #3998, .T. ) ;
#1775=CIRCLE ( 'NONE', #20824, 44.99999999999999289 ) ;
#1776=DIRECTION ( 'NONE',  ( -1.000000000000000000, 0.000000000000000000, -0.000000000000000000 ) ) ;
#1777=CARTESIAN_POINT ( 'NONE',  ( 0.000000000000000000, 67.05625154133453236, 63.71729851637834940 ) ) ;
#1780=DIRECTION ( 'NONE',  ( 0.000000000000000000, 0.000000000000000000, 1.000000000000000000 ) ) ;
#1781=EDGE_CURVE ( 'NONE', #11509, #16102, #15996, .T. ) ;
#1782=ORIENTED_EDGE ( 'NONE', *, *, #14864, .T. ) ;
#1783=ORIENTED_EDGE ( 'NONE', *, *, #19778, .F. ) ;
#1784=EDGE_CURVE ( 'NONE', #9397, #10412, #6493, .T. ) ;
#1785=DIRECTION ( 'NONE',  ( 1.000000000000000000, 0.000000000000000000, 0.000000000000000000 ) ) ;
#1786=ORIENTED_EDGE ( 'NONE', *, *, #14688, .F. ) ;
#1788=DIRECTION ( 'NONE',  ( 0.000000000000000000, 0.000000000000000000, 1.000000000000000000 ) ) ;
#1789=VERTEX_POINT ( 'NONE', #14834 ) ;
#1790=ORIENTED_EDGE ( 'NONE', *, *, #19319, .T. ) ;
#1792=EDGE_CURVE ( 'NONE', #6729, #12424, #19809, .T. ) ;
#1793=CARTESIAN_POINT ( 'NONE',  ( 0.000000000000000000, 78.80192417387979731, -39.16958956249220591 ) ) ;
#1794=VERTEX_POINT ( 'NONE', #4670 ) ;
#1795=CARTESIAN_POINT ( 'NONE',  ( 0.000000000000000000, 0.6609040254623582689, -87.99751818016873983 ) ) ;
#1797=DIRECTION ( 'NONE',  ( -1.000000000000000000, -0.000000000000000000, -0.000000000000000000 ) ) ;
#1799=CARTESIAN_POINT ( 'NONE',  ( 10.00000000000000000, 3.974475837764916530, 92.41557521768191918 ) ) ;
#1802=DIRECTION ( 'NONE',  ( -1.000000000000000000, 0.000000000000000000, -0.000000000000000000 ) ) ;
#1803=ADVANCED_FACE ( 'NONE', ( #15053 ), #16496, .F. ) ;
#1804=ORIENTED_EDGE ( 'NONE', *, *, #8132, .F. ) ;
#1806=FACE_OUTER_BOUND ( 'NONE', #10129, .T. ) ;
#1807=VERTEX_POINT ( 'NONE', #1462 ) ;
#1808=DIRECTION ( 'NONE',  ( 0.000000000000000000, 0.8660254037844362651, 0.5000000000000041078 ) ) ;
#1813=CARTESIAN_POINT ( 'NONE',  ( 0.000000000000000000, 0.000000000000000000, 0.000000000000000000 ) ) ;
#1817=ADVANCED_FACE ( 'NONE', ( #13609 ), #20249, .F. ) ;
#1820=ORIENTED_EDGE ( 'NONE', *, *, #21401, .F. ) ;
#1821=ADVANCED_FACE ( 'NONE', ( #7104 ), #3562, .F. ) ;
#1822=CARTESIAN_POINT ( 'NONE',  ( 10.00000000000000000, 0.000000000000000000, 0.000000000000000000 ) ) ;
#1825=DIRECTION ( 'NONE',  ( -1.000000000000000000, -0.000000000000000000, 0.000000000000000000 ) ) ;
#1826=DIRECTION ( 'NONE',  ( 0.000000000000000000, 0.3420201433256693235, -0.9396926207859080948 ) ) ;
#1827=ORIENTED_EDGE ( 'NONE', *, *, #6393, .F. ) ;
#1828=CARTESIAN_POINT ( 'NONE',  ( 10.00000000000000000, 27.00677879429135331, -80.65868421664406185 ) ) ;
#1829=DIRECTION ( 'NONE',  ( -1.000000000000000000, -0.000000000000000000, -0.000000000000000000 ) ) ;
#1830=AXIS2_PLACEMENT_3D ( 'NONE', #516, #7265, #738 ) ;
#1831=ORIENTED_EDGE ( 'NONE', *, *, #4588, .T. ) ;
#1832=CARTESIAN_POINT ( 'NONE',  ( 10.00000000000000000, 43.18649929580291058, -73.28107340219372645 ) ) ;
#1833=ORIENTED_EDGE ( 'NONE', *, *, #2176, .T. ) ;
#1834=DIRECTION ( 'NONE',  ( 0.000000000000000000, 0.9510565162951521989, 0.3090169943749514481 ) ) ;
#1836=ORIENTED_EDGE ( 'NONE', *, *, #16622, .F. ) ;
#1837=DIRECTION ( 'NONE',  ( -1.000000000000000000, 0.000000000000000000, -0.000000000000000000 ) ) ;
#1838=CIRCLE ( 'NONE', #14174, 44.99999999999999289 ) ;
#1840=VERTEX_POINT ( 'NONE', #16823 ) ;
#1843=VERTEX_POINT ( 'NONE', #362 ) ;
#1844=DIRECTION ( 'NONE',  ( -1.000000000000000000, -0.000000000000000000, -0.000000000000000000 ) ) ;
#1846=CARTESIAN_POINT ( 'NONE',  ( 5.000000000000000000, 65.83713140174806711, -58.39068529131128571 ) ) ;
#1847=DIRECTION ( 'NONE',  ( 0.000000000000000000, 0.000000000000000000, 1.000000000000000000 ) ) ;
#1848=VECTOR ( 'NONE', #6161, 1000.000000000000000 ) ;
#1850=CIRCLE ( 'NONE', #9585, 44.99999999999999289 ) ;
#1851=CARTESIAN_POINT ( 'NONE',  ( 5.000000000000002665, 85.22372865846323009, -21.92979875759543162 ) ) ;
#1853=DIRECTION ( 'NONE',  ( -1.000000000000000000, -0.000000000000000000, -0.000000000000000000 ) ) ;
#1854=AXIS2_PLACEMENT_3D ( 'NONE', #13252, #1659, #20001 ) ;
#1857=DIRECTION ( 'NONE',  ( 0.000000000000000000, 0.000000000000000000, 1.000000000000000000 ) ) ;
#1858=ORIENTED_EDGE ( 'NONE', *, *, #6956, .T. ) ;
#1861=EDGE_LOOP ( 'NONE', ( #12412, #8285, #1711, #157 ) ) ;
#1863=ORIENTED_EDGE ( 'NONE', *, *, #19036, .T. ) ;
#1864=EDGE_CURVE ( 'NONE', #15501, #9734, #13526, .T. ) ;
#1865=VERTEX_POINT ( 'NONE', #18807 ) ;
#1866=FACE_OUTER_BOUND ( 'NONE', #5528, .T. ) ;
#1869=DIRECTION ( 'NONE',  ( 1.000000000000000000, 0.000000000000000000, 0.000000000000000000 ) ) ;
#1870=EDGE_CURVE ( 'NONE', #12371, #16840, #11579, .T. ) ;
#1873=CIRCLE ( 'NONE', #19870, 44.99999999999999289 ) ;
#1874=DIRECTION ( 'NONE',  ( 1.000000000000000000, 0.000000000000000000, 0.000000000000000000 ) ) ;
#1877=VECTOR ( 'NONE', #2746, 1000.000000000000000 ) ;
#1878=ORIENTED_EDGE ( 'NONE', *, *, #7342, .F. ) ;
#1883=ORIENTED_EDGE ( 'NONE', *, *, #10525, .F. ) ;
#1884=CARTESIAN_POINT ( 'NONE',  ( 0.000000000000000000, -68.93609746931124960, -54.69748134696530428 ) ) ;
#1885=EDGE_LOOP ( 'NONE', ( #18750, #1626, #20193, #3850 ) ) ;
#1890=ORIENTED_EDGE ( 'NONE', *, *, #9749, .T. ) ;
#1891=CARTESIAN_POINT ( 'NONE',  ( 10.00000000000000000, 0.000000000000000000, 0.000000000000000000 ) ) ;
#1894=ORIENTED_EDGE ( 'NONE', *, *, #1993, .T. ) ;
#1895=CARTESIAN_POINT ( 'NONE',  ( 10.00000000000000000, 84.19736439813857487, -38.30455363800848545 ) ) ;
#1896=AXIS2_PLACEMENT_3D ( 'NONE', #15054, #11853, #13401 ) ;
#1897=LINE ( 'NONE', #18596, #15716 ) ;
#1898=CARTESIAN_POINT ( 'NONE',  ( 10.00000000000000000, -52.96496548042809138, -66.55750800669412115 ) ) ;
#1899=CYLINDRICAL_SURFACE ( 'NONE', #4108, 92.50100000000000477 ) ;
#1901=DIRECTION ( 'NONE',  ( 1.000000000000000000, 0.000000000000000000, 0.000000000000000000 ) ) ;
#1902=CARTESIAN_POINT ( 'NONE',  ( 0.000000000000000000, -8.134922360105496963, -84.67002113262489615 ) ) ;
#1903=ADVANCED_FACE ( 'NONE', ( #15160 ), #6885, .F. ) ;
#1904=CYLINDRICAL_SURFACE ( 'NONE', #11934, 92.50100000000000477 ) ;
#1906=EDGE_CURVE ( 'NONE', #4702, #11578, #4874, .T. ) ;
#1907=AXIS2_PLACEMENT_3D ( 'NONE', #1492, #6482, #11557 ) ;
#1908=CARTESIAN_POINT ( 'NONE',  ( 10.00000000000000000, 37.96946988134275358, -76.11510229470822253 ) ) ;
#1910=ORIENTED_EDGE ( 'NONE', *, *, #7365, .F. ) ;
#1916=CARTESIAN_POINT ( 'NONE',  ( 0.000000000000000000, 71.72924546250010280, -45.71766382684594276 ) ) ;
#1917=EDGE_CURVE ( 'NONE', #18043, #1449, #33, .T. ) ;
#1918=ORIENTED_EDGE ( 'NONE', *, *, #5142, .F. ) ;
#1920=DIRECTION ( 'NONE',  ( -1.000000000000000000, 0.000000000000000000, -0.000000000000000000 ) ) ;
#1921=LINE ( 'NONE', #8873, #16783 ) ;
#1924=CYLINDRICAL_SURFACE ( 'NONE', #14695, 88.00000000000000000 ) ;
#1925=AXIS2_PLACEMENT_3D ( 'NONE', #16639, #11882, #5363 ) ;
#1926=CARTESIAN_POINT ( 'NONE',  ( 0.000000000000000000, -74.74361964203257003, 40.60271866773520344 ) ) ;
#1928=CARTESIAN_POINT ( 'NONE',  ( 0.000000000000000000, 14.02138820414913845, 83.89630571862289798 ) ) ;
#1937=EDGE_LOOP ( 'NONE', ( #16405, #7438, #14750, #2350 ) ) ;
#1940=CARTESIAN_POINT ( 'NONE',  ( 10.00000000000000000, 57.47876254627226444, -62.70072803846332476 ) ) ;
#1946=ORIENTED_EDGE ( 'NONE', *, *, #19010, .T. ) ;
#1947=AXIS2_PLACEMENT_3D ( 'NONE', #12432, #11224, #4489 ) ;
#1949=EDGE_LOOP ( 'NONE', ( #11976, #18648, #13217, #8141 ) ) ;
#1950=EDGE_LOOP ( 'NONE', ( #5973, #17634, #5714, #2466 ) ) ;
#1951=ORIENTED_EDGE ( 'NONE', *, *, #3908, .F. ) ;
#1953=AXIS2_PLACEMENT_3D ( 'NONE', #11348, #18100, #21626 ) ;
#1954=ORIENTED_EDGE ( 'NONE', *, *, #4616, .T. ) ;
#1955=CARTESIAN_POINT ( 'NONE',  ( -10.00000000000000000, 0.000000000000000000, 0.000000000000000000 ) ) ;
#1956=LINE ( 'NONE', #8696, #20967 ) ;
#1957=CYLINDRICAL_SURFACE ( 'NONE', #9804, 92.50100000000000477 ) ;
#1958=DIRECTION ( 'NONE',  ( 1.000000000000000000, 0.000000000000000000, 0.000000000000000000 ) ) ;
#1959=CLOSED_SHELL ( 'NONE', ( #15510, #15926, #19174, #21610, #17084, #10169, #8327, #20565, #19329, #17150, #326, #12725, #11223, #3786, #1803, #17987, #14034, #20, #14191, #10830, #7129, #9588, #18112, #311, #12383, #2698, #16095, #7831, #18003, #18664, #21235, #6920, #19178, #1343, #16660, #2982, #15138, #9090, #17035, #10135, #200, #13822, #1903, #13505, #4378, #12040, #4788, #10844, #17378, #5179, #6893, #12784, #15464, #5145, #1094, #7623, #435, #5010, #13378, #4196, #2066, #4754, #16087, #11922, #5007, #14274, #20399, #2055, #12689, #20314, #17613, #9936, #5860, #17968, #4463, #12931, #20727, #15396, #15404, #14366, #21216, #10038, #17065, #2686, #11366, #5151, #2147, #9857, #19764, #15224, #7523, #20568, #1392, #17463, #10767, #14767, #13908, #7695, #12343, #13266, #5414, #16083, #19547, #19878, #10981, #13652, #18823, #7200, #12775, #814, #19777, #19462, #2045, #10953, #11762, #11994, #15707, #15126, #5297, #15145, #16777, #19575, #13005, #10291, #10247, #1670, #7176, #7749, #18391, #14982, #13506, #8116, #14514, #1672, #6926, #10992, #17162, #1405, #4722, #19107, #5237, #7183, #14438, #11337, #1081, #10937, #2602, #18111, #21293, #1135, #20536, #1489, #9901, #6074, #4637, #2726, #8113, #11206, #10566, #6243, #15965, #21384, #10956, #18303, #15378, #12165, #653, #14883, #3909, #14908, #8982, #7072, #21579, #21482, #10666, #7024, #15973, #11774, #17452, #2934, #19742, #20134, #15280, #2857, #6018, #2061, #6769, #10662, #14163, #9084, #20848, #11321, #4383, #6121, #7966, #5615, #148, #8439, #12542, #17974, #20394, #14835, #12119, #9185, #19071, #4589, #4631, #15264, #19380, #9989, #5581, #5511, #19224, #18387, #19899, #21514, #13796, #17483, #3635, #11532, #14353, #9872, #727, #13362, #9532, #534, #19301, #20694, #18109, #3789, #20180, #9554, #17881, #14494, #5292, #13364, #15200, #18933, #4908, #21773, #17670, #6652, #12962, #20931, #21100, #15583, #7453, #18924, #20692, #9682, #18938, #15028, #16232, #1817, #6263, #1092, #11626, #16509, #8397, #20258, #19862, #18156, #13812, #7077, #14407, #21098, #2359, #17780, #16334, #16329, #5579, #3490, #11058, #14284, #18260, #986, #17811, #14183, #11868, #21047, #7708, #18804, #19887, #8207, #824, #3436, #15296, #442, #2732, #15824, #274, #12720, #1821, #15706, #5417, #14010, #17970, #4495, #2975, #18569, #17470, #21747, #18115, #3357, #2152, #12959, #11745, #4112, #3026, #7562, #8435, #10223, #10433, #10260, #13112, #11516, #19868, #12421, #4239, #12436, #18784, #11095, #21453, #9445, #9920, #6770, #11352, #2615, #18217, #12139, #9605, #7156, #16327, #17305, #6869, #19654, #10983, #16755, #5705, #14567, #8707, #3659, #5968, #8675, #10924, #15975, #14741, #3662, #281, #15809, #18619, #16113, #491, #6400, #19328, #12960, #14999, #18641, #20026, #20004, #21856, #16778, #18443, #14950, #4707, #13102, #10435 ) ) ;
#1961=CARTESIAN_POINT ( 'NONE',  ( 10.00000000000000000, 78.04699792498210797, -49.64978465107211747 ) ) ;
#1962=CIRCLE ( 'NONE', #14297, 45.00000000000000000 ) ;
#1963=DIRECTION ( 'NONE',  ( -1.000000000000000000, -0.000000000000000000, -0.000000000000000000 ) ) ;
#1964=VECTOR ( 'NONE', #6052, 1000.000000000000000 ) ;
#1966=AXIS2_PLACEMENT_3D ( 'NONE', #1703, #20047, #6466 ) ;
#1967=ORIENTED_EDGE ( 'NONE', *, *, #427, .T. ) ;
#1968=DIRECTION ( 'NONE',  ( 0.000000000000000000, 0.000000000000000000, 1.000000000000000000 ) ) ;
#1969=AXIS2_PLACEMENT_3D ( 'NONE', #12709, #1109, #21439 ) ;
#1972=VERTEX_POINT ( 'NONE', #17265 ) ;
#1973=DIRECTION ( 'NONE',  ( 0.000000000000000000, -0.8290375725550350738, -0.5591929034707565638 ) ) ;
#1974=VERTEX_POINT ( 'NONE', #2125 ) ;
#1975=DIRECTION ( 'NONE',  ( 0.000000000000000000, 0.000000000000000000, 1.000000000000000000 ) ) ;
#1976=VERTEX_POINT ( 'NONE', #8855 ) ;
#1977=EDGE_LOOP ( 'NONE', ( #19937, #639, #18793, #17527 ) ) ;
#1980=VECTOR ( 'NONE', #20366, 1000.000000000000000 ) ;
#1984=ORIENTED_EDGE ( 'NONE', *, *, #13752, .F. ) ;
#1985=CARTESIAN_POINT ( 'NONE',  ( 5.000000000000000000, -68.93609746931198856, 54.69748134696436637 ) ) ;
#1986=DIRECTION ( 'NONE',  ( 1.000000000000000000, -0.000000000000000000, -0.000000000000000000 ) ) ;
#1989=CARTESIAN_POINT ( 'NONE',  ( 0.000000000000000000, 0.000000000000000000, 0.000000000000000000 ) ) ;
#1990=FACE_OUTER_BOUND ( 'NONE', #12078, .T. ) ;
#1992=CARTESIAN_POINT ( 'NONE',  ( 10.00000000000000000, 71.72924546250010280, -45.71766382684594276 ) ) ;
#1993=EDGE_CURVE ( 'NONE', #10561, #3324, #2405, .T. ) ;
#1994=AXIS2_PLACEMENT_3D ( 'NONE', #4763, #3211, #21772 ) ;
#1996=AXIS2_PLACEMENT_3D ( 'NONE', #17692, #7322, #575 ) ;
#1997=DIRECTION ( 'NONE',  ( 0.000000000000000000, -0.9993908270190953180, -0.03489949670251103753 ) ) ;
#1998=ORIENTED_EDGE ( 'NONE', *, *, #1508, .T. ) ;
#2000=EDGE_LOOP ( 'NONE', ( #3147, #16523, #11212, #14638 ) ) ;
#2002=ORIENTED_EDGE ( 'NONE', *, *, #20917, .F. ) ;
#2003=ORIENTED_EDGE ( 'NONE', *, *, #14233, .T. ) ;
#2005=AXIS2_PLACEMENT_3D ( 'NONE', #3206, #20013, #21442 ) ;
#2007=ORIENTED_EDGE ( 'NONE', *, *, #17207, .F. ) ;
#2008=AXIS2_PLACEMENT_3D ( 'NONE', #9253, #14356, #21101 ) ;
#2010=DIRECTION ( 'NONE',  ( -1.000000000000000000, -0.000000000000000000, 0.000000000000000000 ) ) ;
#2011=CARTESIAN_POINT ( 'NONE',  ( 10.00000000000000000, 15.32665449652044920, -91.22241316115403720 ) ) ;
#2013=CARTESIAN_POINT ( 'NONE',  ( 5.000000000000000000, 69.74988376404090218, -53.65588238863266213 ) ) ;
#2017=EDGE_CURVE ( 'NONE', #2438, #16240, #9383, .T. ) ;
#2018=EDGE_CURVE ( 'NONE', #14822, #3811, #21462, .T. ) ;
#2022=AXIS2_PLACEMENT_3D ( 'NONE', #21256, #14620, #19482 ) ;
#2025=ORIENTED_EDGE ( 'NONE', *, *, #6937, .F. ) ;
#2026=CYLINDRICAL_SURFACE ( 'NONE', #1597, 88.00000000000000000 ) ;
#2029=CARTESIAN_POINT ( 'NONE',  ( 0.000000000000000000, -72.58367602204151581, -49.75550195834941292 ) ) ;
#2030=ORIENTED_EDGE ( 'NONE', *, *, #12606, .F. ) ;
#2031=ORIENTED_EDGE ( 'NONE', *, *, #9687, .T. ) ;
#2034=EDGE_CURVE ( 'NONE', #18952, #6202, #12790, .T. ) ;
#2037=DIRECTION ( 'NONE',  ( 0.000000000000000000, -0.6946583704589887054, -0.7193398003386594075 ) ) ;
#2038=AXIS2_PLACEMENT_3D ( 'NONE', #14409, #21162, #6032 ) ;
#2039=DIRECTION ( 'NONE',  ( -1.000000000000000000, 0.000000000000000000, 0.000000000000000000 ) ) ;
#2040=AXIS2_PLACEMENT_3D ( 'NONE', #9770, #18305, #6593 ) ;
#2041=CARTESIAN_POINT ( 'NONE',  ( 10.00000000000000000, -82.02147376274702140, 42.76579056660835221 ) ) ;
#2042=CIRCLE ( 'NONE', #2022, 88.00000000000000000 ) ;
#2043=CARTESIAN_POINT ( 'NONE',  ( 0.000000000000000000, -57.53593069156319473, -72.42963261301021305 ) ) ;
#2044=DIRECTION ( 'NONE',  ( -1.000000000000000000, -0.000000000000000000, -0.000000000000000000 ) ) ;
#2045=ADVANCED_FACE ( 'NONE', ( #11048 ), #4104, .F. ) ;
#2046=EDGE_CURVE ( 'NONE', #21836, #16223, #2926, .T. ) ;
#2048=ORIENTED_EDGE ( 'NONE', *, *, #11113, .T. ) ;
#2049=CARTESIAN_POINT ( 'NONE',  ( 10.00000000000000000, 84.12297548659721258, -12.59025161327029529 ) ) ;
#2050=EDGE_CURVE ( 'NONE', #447, #12668, #12486, .T. ) ;
#2051=ORIENTED_EDGE ( 'NONE', *, *, #20131, .F. ) ;
#2052=DIRECTION ( 'NONE',  ( 0.000000000000000000, 0.6427876096865353661, 0.7660444431189812331 ) ) ;
#2053=ORIENTED_EDGE ( 'NONE', *, *, #13082, .F. ) ;
#2055=ADVANCED_FACE ( 'NONE', ( #10946 ), #6095, .F. ) ;
#2057=AXIS2_PLACEMENT_3D ( 'NONE', #5448, #258, #42 ) ;
#2058=CYLINDRICAL_SURFACE ( 'NONE', #10550, 92.50100000000000477 ) ;
#2061=ADVANCED_FACE ( 'NONE', ( #15919 ), #12809, .F. ) ;
#2063=ORIENTED_EDGE ( 'NONE', *, *, #13457, .F. ) ;
#2065=DIRECTION ( 'NONE',  ( 0.000000000000000000, 0.9271838545667883125, -0.3746065934159096833 ) ) ;
#2066=ADVANCED_FACE ( 'NONE', ( #8957 ), #15704, .F. ) ;
#2067=ORIENTED_EDGE ( 'NONE', *, *, #2488, .T. ) ;
#2068=DIRECTION ( 'NONE',  ( 1.000000000000000000, 0.000000000000000000, 0.000000000000000000 ) ) ;
#2070=CYLINDRICAL_SURFACE ( 'NONE', #2752, 44.99999999999999289 ) ;
#2071=CYLINDRICAL_SURFACE ( 'NONE', #4076, 44.99999999999999289 ) ;
#2072=CYLINDRICAL_SURFACE ( 'NONE', #13175, 44.99999999999999289 ) ;
#2074=DIRECTION ( 'NONE',  ( -1.000000000000000000, 0.000000000000000000, 0.000000000000000000 ) ) ;
#2077=AXIS2_PLACEMENT_3D ( 'NONE', #1336, #14696, #6206 ) ;
#2078=CIRCLE ( 'NONE', #2766, 45.00000000000000000 ) ;
#2081=DIRECTION ( 'NONE',  ( 1.000000000000000000, 0.000000000000000000, 0.000000000000000000 ) ) ;
#2082=EDGE_CURVE ( 'NONE', #15909, #3420, #3984, .T. ) ;
#2084=DIRECTION ( 'NONE',  ( -1.000000000000000000, 0.000000000000000000, -0.000000000000000000 ) ) ;
#2085=ORIENTED_EDGE ( 'NONE', *, *, #4086, .F. ) ;
#2087=VERTEX_POINT ( 'NONE', #16019 ) ;
#2089=CARTESIAN_POINT ( 'NONE',  ( 10.00000000000000000, 0.000000000000000000, 0.000000000000000000 ) ) ;
#2090=ORIENTED_EDGE ( 'NONE', *, *, #12151, .T. ) ;
#2091=AXIS2_PLACEMENT_3D ( 'NONE', #7397, #21086, #17771 ) ;
#2092=ORIENTED_EDGE ( 'NONE', *, *, #6190, .T. ) ;
#2093=CIRCLE ( 'NONE', #13728, 92.50100000000000477 ) ;
#2095=ORIENTED_EDGE ( 'NONE', *, *, #12972, .T. ) ;
#2097=DIRECTION ( 'NONE',  ( 1.000000000000000000, 0.000000000000000000, 0.000000000000000000 ) ) ;
#2099=FACE_OUTER_BOUND ( 'NONE', #1455, .T. ) ;
#2100=EDGE_CURVE ( 'NONE', #510, #5341, #1873, .T. ) ;
#2103=DIRECTION ( 'NONE',  ( -1.000000000000000000, 0.000000000000000000, 0.000000000000000000 ) ) ;
#2104=DIRECTION ( 'NONE',  ( 0.000000000000000000, 0.4694715627858856988, 0.8829475928589297640 ) ) ;
#2105=DIRECTION ( 'NONE',  ( -1.000000000000000000, -0.000000000000000000, -0.000000000000000000 ) ) ;
#2107=AXIS2_PLACEMENT_3D ( 'NONE', #10990, #17523, #2372 ) ;
#2110=CIRCLE ( 'NONE', #13743, 88.00000000000000000 ) ;
#2112=VERTEX_POINT ( 'NONE', #13041 ) ;
#2113=ORIENTED_EDGE ( 'NONE', *, *, #5865, .F. ) ;
#2114=ORIENTED_EDGE ( 'NONE', *, *, #11119, .T. ) ;
#2115=DIRECTION ( 'NONE',  ( -1.000000000000000000, 0.000000000000000000, -0.000000000000000000 ) ) ;
#2116=ORIENTED_EDGE ( 'NONE', *, *, #9631, .F. ) ;
#2117=ORIENTED_EDGE ( 'NONE', *, *, #19332, .T. ) ;
#2120=ORIENTED_EDGE ( 'NONE', *, *, #17838, .F. ) ;
#2122=CARTESIAN_POINT ( 'NONE',  ( 0.000000000000000000, 0.000000000000000000, 0.000000000000000000 ) ) ;
#2123=LINE ( 'NONE', #12274, #2545 ) ;
#2125=CARTESIAN_POINT ( 'NONE',  ( 0.000000000000000000, 68.93609746931237225, -54.69748134696388320 ) ) ;
#2127=DIRECTION ( 'NONE',  ( 1.000000000000000000, 0.000000000000000000, 0.000000000000000000 ) ) ;
#2129=DIRECTION ( 'NONE',  ( 0.000000000000000000, 0.000000000000000000, 1.000000000000000000 ) ) ;
#2132=DIRECTION ( 'NONE',  ( 0.000000000000000000, 0.8660254037844363761, 0.5000000000000041078 ) ) ;
#2134=CARTESIAN_POINT ( 'NONE',  ( -10.00000000000000000, 0.000000000000000000, 0.000000000000000000 ) ) ;
#2135=VERTEX_POINT ( 'NONE', #1548 ) ;
#2136=CARTESIAN_POINT ( 'NONE',  ( 10.00000000000000000, 0.000000000000000000, 0.000000000000000000 ) ) ;
#2139=VERTEX_POINT ( 'NONE', #12925 ) ;
#2141=DIRECTION ( 'NONE',  ( 1.000000000000000000, 0.000000000000000000, 0.000000000000000000 ) ) ;
#2143=CARTESIAN_POINT ( 'NONE',  ( 10.00000000000000000, -36.60317927562525853, -76.78148674856802813 ) ) ;
#2144=DIRECTION ( 'NONE',  ( 1.000000000000000000, 0.000000000000000000, 0.000000000000000000 ) ) ;
#2146=DIRECTION ( 'NONE',  ( 0.000000000000000000, 0.000000000000000000, 1.000000000000000000 ) ) ;
#2147=ADVANCED_FACE ( 'NONE', ( #4543 ), #21655, .F. ) ;
#2149=CARTESIAN_POINT ( 'NONE',  ( 5.000000000000000000, -56.05743251323810483, -67.83483072893858434 ) ) ;
#2150=ORIENTED_EDGE ( 'NONE', *, *, #17838, .T. ) ;
#2152=ADVANCED_FACE ( 'NONE', ( #4871 ), #8184, .F. ) ;
#2153=VERTEX_POINT ( 'NONE', #21440 ) ;
#2154=DIRECTION ( 'NONE',  ( -1.000000000000000000, -0.000000000000000000, -0.000000000000000000 ) ) ;
#2155=VERTEX_POINT ( 'NONE', #11279 ) ;
#2157=DIRECTION ( 'NONE',  ( -1.000000000000000000, 0.000000000000000000, -0.000000000000000000 ) ) ;
#2158=ORIENTED_EDGE ( 'NONE', *, *, #422, .T. ) ;
#2159=VERTEX_POINT ( 'NONE', #15321 ) ;
#2160=EDGE_CURVE ( 'NONE', #20330, #7224, #9818, .T. ) ;
#2161=ORIENTED_EDGE ( 'NONE', *, *, #18164, .T. ) ;
#2166=VERTEX_POINT ( 'NONE', #6952 ) ;
#2167=EDGE_CURVE ( 'NONE', #13890, #3424, #19557, .T. ) ;
#2168=LINE ( 'NONE', #19401, #14607 ) ;
#2171=LINE ( 'NONE', #2274, #5085 ) ;
#2173=DIRECTION ( 'NONE',  ( -1.000000000000000000, 0.000000000000000000, 0.000000000000000000 ) ) ;
#2174=ORIENTED_EDGE ( 'NONE', *, *, #11312, .T. ) ;
#2175=FACE_OUTER_BOUND ( 'NONE', #3979, .T. ) ;
#2176=EDGE_CURVE ( 'NONE', #17490, #13354, #16467, .T. ) ;
#2179=EDGE_CURVE ( 'NONE', #4068, #19613, #18317, .T. ) ;
#2180=DIRECTION ( 'NONE',  ( 0.000000000000000000, 0.000000000000000000, 1.000000000000000000 ) ) ;
#2181=EDGE_LOOP ( 'NONE', ( #1878, #15276, #6793, #14161 ) ) ;
#2182=FACE_OUTER_BOUND ( 'NONE', #3133, .T. ) ;
#2184=CYLINDRICAL_SURFACE ( 'NONE', #14053, 92.50100000000000477 ) ;
#2185=ORIENTED_EDGE ( 'NONE', *, *, #7062, .F. ) ;
#2187=DIRECTION ( 'NONE',  ( -1.000000000000000000, -0.000000000000000000, -0.000000000000000000 ) ) ;
#2188=EDGE_LOOP ( 'NONE', ( #16537, #1437, #1782, #15450 ) ) ;
#2189=DIRECTION ( 'NONE',  ( -1.000000000000000000, 0.000000000000000000, -0.000000000000000000 ) ) ;
#2190=EDGE_CURVE ( 'NONE', #18794, #6346, #11600, .T. ) ;
#2191=AXIS2_PLACEMENT_3D ( 'NONE', #21437, #6323, #21221 ) ;
#2192=DIRECTION ( 'NONE',  ( 0.000000000000000000, 0.000000000000000000, 1.000000000000000000 ) ) ;
#2193=LINE ( 'NONE', #5735, #4339 ) ;
#2195=CARTESIAN_POINT ( 'NONE',  ( 0.000000000000000000, 65.64563793391906188, -54.09103124042745492 ) ) ;
#2196=DIRECTION ( 'NONE',  ( -1.000000000000000000, -0.000000000000000000, -0.000000000000000000 ) ) ;
#2199=CARTESIAN_POINT ( 'NONE',  ( 10.00000000000000000, 85.22372865846323009, -21.92979875759543162 ) ) ;
#2204=EDGE_LOOP ( 'NONE', ( #14119, #4888, #21368, #5020 ) ) ;
#2206=ORIENTED_EDGE ( 'NONE', *, *, #11511, .T. ) ;
#2207=EDGE_CURVE ( 'NONE', #2619, #6547, #18236, .T. ) ;
#2210=FACE_OUTER_BOUND ( 'NONE', #19200, .T. ) ;
#2211=AXIS2_PLACEMENT_3D ( 'NONE', #18894, #3751, #17240 ) ;
#2212=AXIS2_PLACEMENT_3D ( 'NONE', #224, #10595, #339 ) ;
#2214=VERTEX_POINT ( 'NONE', #3611 ) ;
#2215=AXIS2_PLACEMENT_3D ( 'NONE', #21202, #5964, #4404 ) ;
#2218=DIRECTION ( 'NONE',  ( 0.000000000000000000, 0.9510565162951544194, -0.3090169943749448977 ) ) ;
#2219=DIRECTION ( 'NONE',  ( 0.000000000000000000, 0.000000000000000000, 1.000000000000000000 ) ) ;
#2220=CIRCLE ( 'NONE', #12437, 44.99999999999999289 ) ;
#2222=DIRECTION ( 'NONE',  ( 0.000000000000000000, 0.000000000000000000, 1.000000000000000000 ) ) ;
#2223=CARTESIAN_POINT ( 'NONE',  ( 0.000000000000000000, -2.208823992043557283, -85.03123271466938604 ) ) ;
#2224=CARTESIAN_POINT ( 'NONE',  ( 10.00000000000000000, 0.000000000000000000, 0.000000000000000000 ) ) ;
#2227=VECTOR ( 'NONE', #13531, 1000.000000000000000 ) ;
#2231=CARTESIAN_POINT ( 'NONE',  ( 0.000000000000000000, -64.66851233300764079, 55.25552418572942059 ) ) ;
#2235=DIRECTION ( 'NONE',  ( 0.000000000000000000, 0.2756373558169932791, 0.9612616959383205595 ) ) ;
#2240=VERTEX_POINT ( 'NONE', #10576 ) ;
#2241=EDGE_LOOP ( 'NONE', ( #11968, #17439, #21457, #9613 ) ) ;
#2244=AXIS2_PLACEMENT_3D ( 'NONE', #19804, #6229, #21023 ) ;
#2245=CARTESIAN_POINT ( 'NONE',  ( 0.000000000000000000, 74.39348546125053474, 54.97312363261438151 ) ) ;
#2246=CARTESIAN_POINT ( 'NONE',  ( 10.00000000000000000, 61.71252885873388294, 58.53847642588613809 ) ) ;
#2248=DIRECTION ( 'NONE',  ( 0.000000000000000000, -0.3420201433256757073, 0.9396926207859057634 ) ) ;
#2249=DIRECTION ( 'NONE',  ( 1.000000000000000000, 0.000000000000000000, 0.000000000000000000 ) ) ;
#2250=DIRECTION ( 'NONE',  ( 0.000000000000000000, -0.7431448254774000173, 0.6691306063588517983 ) ) ;
#2251=AXIS2_PLACEMENT_3D ( 'NONE', #2388, #11002, #20846 ) ;
#2253=CARTESIAN_POINT ( 'NONE',  ( 0.000000000000000000, -91.70173545986510533, -12.13370160540135778 ) ) ;
#2254=AXIS2_PLACEMENT_3D ( 'NONE', #12984, #9769, #1393 ) ;
#2255=EDGE_CURVE ( 'NONE', #5950, #18176, #17099, .T. ) ;
#2257=VECTOR ( 'NONE', #16842, 1000.000000000000000 ) ;
#2260=CARTESIAN_POINT ( 'NONE',  ( -10.00000000000000000, 0.000000000000000000, 0.000000000000000000 ) ) ;
#2261=DIRECTION ( 'NONE',  ( -1.000000000000000000, 0.000000000000000000, 0.000000000000000000 ) ) ;
#2262=VERTEX_POINT ( 'NONE', #1961 ) ;
#2264=AXIS2_PLACEMENT_3D ( 'NONE', #9410, #1037, #10975 ) ;
#2265=ORIENTED_EDGE ( 'NONE', *, *, #1533, .F. ) ;
#2267=VERTEX_POINT ( 'NONE', #14108 ) ;
#2268=DIRECTION ( 'NONE',  ( 1.000000000000000000, 0.000000000000000000, 0.000000000000000000 ) ) ;
#2269=ORIENTED_EDGE ( 'NONE', *, *, #17543, .F. ) ;
#2270=VECTOR ( 'NONE', #1283, 1000.000000000000000 ) ;
#2271=DIRECTION ( 'NONE',  ( 0.000000000000000000, 0.9510565162951544194, -0.3090169943749450088 ) ) ;
#2274=CARTESIAN_POINT ( 'NONE',  ( 10.00000000000000000, -27.87320266523496315, -88.20158487341788600 ) ) ;
#2275=AXIS2_PLACEMENT_3D ( 'NONE', #15843, #7445, #8975 ) ;
#2277=ORIENTED_EDGE ( 'NONE', *, *, #12001, .F. ) ;
#2278=CARTESIAN_POINT ( 'NONE',  ( 10.00000000000000000, -84.12297548659712731, -12.59025161327086906 ) ) ;
#2279=AXIS2_PLACEMENT_3D ( 'NONE', #11304, #20344, #13169 ) ;
#2282=CIRCLE ( 'NONE', #8291, 92.50100000000000477 ) ;
#2283=EDGE_CURVE ( 'NONE', #21012, #3811, #18978, .T. ) ;
#2285=CIRCLE ( 'NONE', #7288, 44.99999999999998579 ) ;
#2286=CARTESIAN_POINT ( 'NONE',  ( 0.000000000000000000, -87.96697768756401103, -2.410567674971490604 ) ) ;
#2287=AXIS2_PLACEMENT_3D ( 'NONE', #12951, #7778, #19589 ) ;
#2288=VERTEX_POINT ( 'NONE', #10462 ) ;
#2290=CARTESIAN_POINT ( 'NONE',  ( -10.00000000000000000, 0.000000000000000000, 100.0000000000000000 ) ) ;
#2292=CARTESIAN_POINT ( 'NONE',  ( 0.000000000000000000, 0.000000000000000000, 0.000000000000000000 ) ) ;
#2298=EDGE_LOOP ( 'NONE', ( #10010, #1946, #18590, #12079 ) ) ;
#2299=EDGE_CURVE ( 'NONE', #8019, #6618, #4822, .T. ) ;
#2300=DIRECTION ( 'NONE',  ( 0.000000000000000000, 0.000000000000000000, 1.000000000000000000 ) ) ;
#2302=LINE ( 'NONE', #15566, #2548 ) ;
#2304=AXIS2_PLACEMENT_3D ( 'NONE', #13626, #17053, #15604 ) ;
#2306=VECTOR ( 'NONE', #16526, 1000.000000000000000 ) ;
#2307=EDGE_CURVE ( 'NONE', #18181, #13603, #17004, .T. ) ;
#2309=FACE_OUTER_BOUND ( 'NONE', #5727, .T. ) ;
#2310=DIRECTION ( 'NONE',  ( 1.000000000000000000, 0.000000000000000000, 0.000000000000000000 ) ) ;
#2311=LINE ( 'NONE', #5744, #2728 ) ;
#2312=CARTESIAN_POINT ( 'NONE',  ( 0.000000000000000000, 0.000000000000000000, 0.000000000000000000 ) ) ;
#2313=EDGE_CURVE ( 'NONE', #8737, #9671, #17322, .T. ) ;
#2314=ORIENTED_EDGE ( 'NONE', *, *, #5454, .T. ) ;
#2316=ORIENTED_EDGE ( 'NONE', *, *, #18957, .F. ) ;
#2317=EDGE_CURVE ( 'NONE', #6258, #13543, #66, .T. ) ;
#2318=ORIENTED_EDGE ( 'NONE', *, *, #1463, .F. ) ;
#2319=CIRCLE ( 'NONE', #15327, 44.99999999999998579 ) ;
#2323=ORIENTED_EDGE ( 'NONE', *, *, #14471, .F. ) ;
#2324=ORIENTED_EDGE ( 'NONE', *, *, #1375, .T. ) ;
#2325=EDGE_CURVE ( 'NONE', #17111, #5399, #19819, .T. ) ;
#2327=ORIENTED_EDGE ( 'NONE', *, *, #18525, .F. ) ;
#2329=DIRECTION ( 'NONE',  ( 0.000000000000000000, 0.000000000000000000, 1.000000000000000000 ) ) ;
#2335=EDGE_CURVE ( 'NONE', #6010, #20772, #5712, .T. ) ;
#2336=VECTOR ( 'NONE', #3665, 1000.000000000000000 ) ;
#2337=EDGE_CURVE ( 'NONE', #2883, #17333, #13995, .T. ) ;
#2338=DIRECTION ( 'NONE',  ( 0.000000000000000000, -0.4694715627858974116, 0.8829475928589234357 ) ) ;
#2339=CARTESIAN_POINT ( 'NONE',  ( 10.00000000000000000, -81.32027326007839463, -44.08455690949136851 ) ) ;
#2340=DIRECTION ( 'NONE',  ( 0.000000000000000000, -0.7431448254773861395, -0.6691306063588671194 ) ) ;
#2345=CYLINDRICAL_SURFACE ( 'NONE', #15877, 44.99999999999999289 ) ;
#2346=CIRCLE ( 'NONE', #11535, 45.00000000000000000 ) ;
#2347=ORIENTED_EDGE ( 'NONE', *, *, #18669, .F. ) ;
#2348=CIRCLE ( 'NONE', #20361, 44.99999999999998579 ) ;
#2349=CARTESIAN_POINT ( 'NONE',  ( 5.000000000000002665, -86.54587337002888603, 15.93147207946976707 ) ) ;
#2350=ORIENTED_EDGE ( 'NONE', *, *, #19282, .T. ) ;
#2351=CARTESIAN_POINT ( 'NONE',  ( 0.000000000000000000, 51.76708072107978609, -67.49339815138442589 ) ) ;
#2352=ORIENTED_EDGE ( 'NONE', *, *, #15535, .T. ) ;
#2354=CARTESIAN_POINT ( 'NONE',  ( 10.00000000000000000, -62.44821182181044605, -68.23969402963567177 ) ) ;
#2355=CYLINDRICAL_SURFACE ( 'NONE', #20987, 88.00000000000000000 ) ;
#2358=DIRECTION ( 'NONE',  ( 0.000000000000000000, 0.4694715627858856988, 0.8829475928589297640 ) ) ;
#2359=ADVANCED_FACE ( 'NONE', ( #5711 ), #9011, .F. ) ;
#2362=FACE_OUTER_BOUND ( 'NONE', #15065, .T. ) ;
#2364=AXIS2_PLACEMENT_3D ( 'NONE', #1615, #15086, #13103 ) ;
#2365=ORIENTED_EDGE ( 'NONE', *, *, #14355, .T. ) ;
#2367=DIRECTION ( 'NONE',  ( -1.000000000000000000, -0.000000000000000000, -0.000000000000000000 ) ) ;
#2368=ORIENTED_EDGE ( 'NONE', *, *, #19445, .T. ) ;
#2369=FACE_OUTER_BOUND ( 'NONE', #704, .T. ) ;
#2370=EDGE_LOOP ( 'NONE', ( #1833, #5367, #4927, #13954 ) ) ;
#2372=DIRECTION ( 'NONE',  ( 0.000000000000000000, 0.000000000000000000, 1.000000000000000000 ) ) ;
#2373=ORIENTED_EDGE ( 'NONE', *, *, #11742, .T. ) ;
#2375=ORIENTED_EDGE ( 'NONE', *, *, #21568, .F. ) ;
#2376=ORIENTED_EDGE ( 'NONE', *, *, #3937, .T. ) ;
#2378=VERTEX_POINT ( 'NONE', #21177 ) ;
#2379=DIRECTION ( 'NONE',  ( 0.000000000000000000, 0.000000000000000000, 1.000000000000000000 ) ) ;
#2380=DIRECTION ( 'NONE',  ( 0.000000000000000000, -0.4067366430758070917, 0.9135454576425977580 ) ) ;
#2381=VECTOR ( 'NONE', #6129, 1000.000000000000000 ) ;
#2383=ORIENTED_EDGE ( 'NONE', *, *, #4759, .F. ) ;
#2384=CARTESIAN_POINT ( 'NONE',  ( 5.000000000000000000, 86.54587337002878655, 15.93147207947034971 ) ) ;
#2385=CARTESIAN_POINT ( 'NONE',  ( -10.00000000000000000, 0.000000000000000000, 0.000000000000000000 ) ) ;
#2387=CARTESIAN_POINT ( 'NONE',  ( 10.00000000000000000, -56.35896156214896280, -73.34918167666369015 ) ) ;
#2388=CARTESIAN_POINT ( 'NONE',  ( 10.00000000000000000, -81.55207211302094095, 24.17537951050038814 ) ) ;
#2389=DIRECTION ( 'NONE',  ( -1.000000000000000000, -0.000000000000000000, -0.000000000000000000 ) ) ;
#2393=AXIS2_PLACEMENT_3D ( 'NONE', #4154, #10887, #14311 ) ;
#2399=CARTESIAN_POINT ( 'NONE',  ( 10.00000000000000000, -85.22372865846278955, -21.92979875759713693 ) ) ;
#2400=ORIENTED_EDGE ( 'NONE', *, *, #7207, .F. ) ;
#2401=DIRECTION ( 'NONE',  ( 0.000000000000000000, -0.8987940462991618196, -0.4383711467890877289 ) ) ;
#2402=EDGE_LOOP ( 'NONE', ( #14186, #5487, #1077, #20352 ) ) ;
#2404=ORIENTED_EDGE ( 'NONE', *, *, #13422, .T. ) ;
#2405=CIRCLE ( 'NONE', #283, 88.00000000000000000 ) ;
#2406=ORIENTED_EDGE ( 'NONE', *, *, #13279, .F. ) ;
#2407=ORIENTED_EDGE ( 'NONE', *, *, #5738, .T. ) ;
#2410=DIRECTION ( 'NONE',  ( 1.000000000000000000, 0.000000000000000000, 0.000000000000000000 ) ) ;
#2411=VECTOR ( 'NONE', #4973, 1000.000000000000000 ) ;
#2413=DIRECTION ( 'NONE',  ( -1.000000000000000000, 0.000000000000000000, 0.000000000000000000 ) ) ;
#2414=EDGE_CURVE ( 'NONE', #18093, #4970, #19508, .T. ) ;
#2415=AXIS2_PLACEMENT_3D ( 'NONE', #14118, #8823, #8916 ) ;
#2417=CARTESIAN_POINT ( 'NONE',  ( 10.00000000000000000, -14.02138820414970688, 83.89630571862279851 ) ) ;
#2418=DIRECTION ( 'NONE',  ( -1.000000000000000000, 0.000000000000000000, -0.000000000000000000 ) ) ;
#2419=DIRECTION ( 'NONE',  ( -1.000000000000000000, 0.000000000000000000, 0.000000000000000000 ) ) ;
#2421=EDGE_CURVE ( 'NONE', #16693, #9876, #4907, .T. ) ;
#2422=DIRECTION ( 'NONE',  ( 0.000000000000000000, 0.000000000000000000, 1.000000000000000000 ) ) ;
#2423=LINE ( 'NONE', #7297, #17962 ) ;
#2426=AXIS2_PLACEMENT_3D ( 'NONE', #11926, #2410, #14455 ) ;
#2427=VERTEX_POINT ( 'NONE', #5826 ) ;
#2431=AXIS2_PLACEMENT_3D ( 'NONE', #19748, #2729, #16544 ) ;
#2432=AXIS2_PLACEMENT_3D ( 'NONE', #20986, #5858, #12581 ) ;
#2435=ORIENTED_EDGE ( 'NONE', *, *, #11948, .F. ) ;
#2436=CARTESIAN_POINT ( 'NONE',  ( -10.00000000000000000, 0.000000000000000000, 0.000000000000000000 ) ) ;
#2437=EDGE_CURVE ( 'NONE', #5370, #16155, #8784, .T. ) ;
#2438=VERTEX_POINT ( 'NONE', #14648 ) ;
#2440=EDGE_CURVE ( 'NONE', #21840, #6987, #13721, .T. ) ;
#2442=CARTESIAN_POINT ( 'NONE',  ( 10.00000000000000000, -46.93287725819829603, 70.94007663282431508 ) ) ;
#2448=CYLINDRICAL_SURFACE ( 'NONE', #7639, 88.00000000000000000 ) ;
#2449=CIRCLE ( 'NONE', #2803, 88.00000000000000000 ) ;
#2450=DIRECTION ( 'NONE',  ( 0.000000000000000000, 0.000000000000000000, 1.000000000000000000 ) ) ;
#2451=DIRECTION ( 'NONE',  ( -1.000000000000000000, -0.000000000000000000, -0.000000000000000000 ) ) ;
#2455=EDGE_CURVE ( 'NONE', #19437, #14902, #18328, .T. ) ;
#2456=DIRECTION ( 'NONE',  ( 1.000000000000000000, -0.000000000000000000, 0.000000000000000000 ) ) ;
#2458=CARTESIAN_POINT ( 'NONE',  ( 10.00000000000000000, 92.49798535263880694, -0.7467976319023919007 ) ) ;
#2459=ORIENTED_EDGE ( 'NONE', *, *, #14476, .T. ) ;
#2460=CIRCLE ( 'NONE', #697, 44.99999999999999289 ) ;
#2462=AXIS2_PLACEMENT_3D ( 'NONE', #5259, #20502, #12091 ) ;
#2465=DIRECTION ( 'NONE',  ( 0.000000000000000000, -0.7880107536067145757, -0.6156614753256675066 ) ) ;
#2466=ORIENTED_EDGE ( 'NONE', *, *, #17407, .T. ) ;
#2469=CYLINDRICAL_SURFACE ( 'NONE', #6344, 88.00000000000000000 ) ;
#2470=EDGE_CURVE ( 'NONE', #5352, #5864, #17979, .T. ) ;
#2471=DIRECTION ( 'NONE',  ( 0.000000000000000000, 0.000000000000000000, 1.000000000000000000 ) ) ;
#2472=DIRECTION ( 'NONE',  ( -1.000000000000000000, -0.000000000000000000, 0.000000000000000000 ) ) ;
#2473=CYLINDRICAL_SURFACE ( 'NONE', #21740, 44.99999999999998579 ) ;
#2474=CARTESIAN_POINT ( 'NONE',  ( 5.000000000000002665, -76.53853822673953289, -43.42639941457193231 ) ) ;
#2475=CARTESIAN_POINT ( 'NONE',  ( 0.000000000000000000, -92.32475887865429343, 5.707354816230212791 ) ) ;
#2476=CARTESIAN_POINT ( 'NONE',  ( 10.00000000000000000, -8.134922360106683570, 84.67002113262478247 ) ) ;
#2477=FACE_OUTER_BOUND ( 'NONE', #20849, .T. ) ;
#2479=ORIENTED_EDGE ( 'NONE', *, *, #12825, .F. ) ;
#2480=DIRECTION ( 'NONE',  ( -1.000000000000000000, 0.000000000000000000, -0.000000000000000000 ) ) ;
#2482=EDGE_CURVE ( 'NONE', #9177, #4497, #7694, .T. ) ;
#2483=VERTEX_POINT ( 'NONE', #10894 ) ;
#2484=CARTESIAN_POINT ( 'NONE',  ( 0.000000000000000000, 45.60224695560681596, -80.47900393021679122 ) ) ;
#2487=VERTEX_POINT ( 'NONE', #14431 ) ;
#2488=EDGE_CURVE ( 'NONE', #18539, #8891, #4507, .T. ) ;
#2489=ORIENTED_EDGE ( 'NONE', *, *, #8914, .F. ) ;
#2490=ORIENTED_EDGE ( 'NONE', *, *, #4465, .F. ) ;
#2493=DIRECTION ( 'NONE',  ( -0.000000000000000000, 0.000000000000000000, 1.000000000000000000 ) ) ;
#2494=DIRECTION ( 'NONE',  ( -1.000000000000000000, 0.000000000000000000, 0.000000000000000000 ) ) ;
#2495=ORIENTED_EDGE ( 'NONE', *, *, #9757, .T. ) ;
#2496=CARTESIAN_POINT ( 'NONE',  ( 10.00000000000000000, 0.000000000000000000, 0.000000000000000000 ) ) ;
#2497=FACE_OUTER_BOUND ( 'NONE', #10740, .T. ) ;
#2501=ORIENTED_EDGE ( 'NONE', *, *, #11447, .F. ) ;
#2503=CARTESIAN_POINT ( 'NONE',  ( -10.00000000000000000, 0.000000000000000000, 0.000000000000000000 ) ) ;
#2506=CARTESIAN_POINT ( 'NONE',  ( 10.00000000000000000, -71.33759994382000968, 58.88447872958963814 ) ) ;
#2512=ORIENTED_EDGE ( 'NONE', *, *, #5125, .T. ) ;
#2513=ORIENTED_EDGE ( 'NONE', *, *, #10171, .T. ) ;
#2514=DIRECTION ( 'NONE',  ( -1.000000000000000000, 0.000000000000000000, 0.000000000000000000 ) ) ;
#2520=DIRECTION ( 'NONE',  ( 0.000000000000000000, 0.000000000000000000, 1.000000000000000000 ) ) ;
#2521=DIRECTION ( 'NONE',  ( -1.000000000000000000, 0.000000000000000000, -0.000000000000000000 ) ) ;
#2522=DIRECTION ( 'NONE',  ( -1.000000000000000000, 0.000000000000000000, -0.000000000000000000 ) ) ;
#2525=DIRECTION ( 'NONE',  ( -1.000000000000000000, -0.000000000000000000, -0.000000000000000000 ) ) ;
#2526=CARTESIAN_POINT ( 'NONE',  ( 5.000000000000002665, -86.77540292929691645, -14.62974526292806843 ) ) ;
#2527=VERTEX_POINT ( 'NONE', #21064 ) ;
#2528=EDGE_CURVE ( 'NONE', #19570, #6346, #5932, .T. ) ;
#2530=ORIENTED_EDGE ( 'NONE', *, *, #19083, .T. ) ;
#2532=EDGE_CURVE ( 'NONE', #13081, #1184, #18517, .T. ) ;
#2533=ORIENTED_EDGE ( 'NONE', *, *, #17724, .T. ) ;
#2534=DIRECTION ( 'NONE',  ( -1.000000000000000000, -0.000000000000000000, -0.000000000000000000 ) ) ;
#2535=AXIS2_PLACEMENT_3D ( 'NONE', #10098, #10424, #15181 ) ;
#2539=DIRECTION ( 'NONE',  ( 1.000000000000000000, 0.000000000000000000, -0.000000000000000000 ) ) ;
#2540=DIRECTION ( 'NONE',  ( -1.000000000000000000, -0.000000000000000000, -0.000000000000000000 ) ) ;
#2541=FACE_OUTER_BOUND ( 'NONE', #5263, .T. ) ;
#2542=CYLINDRICAL_SURFACE ( 'NONE', #8325, 92.50100000000000477 ) ;
#2543=DIRECTION ( 'NONE',  ( 0.000000000000000000, 0.3420201433256630508, 0.9396926207859105373 ) ) ;
#2544=CARTESIAN_POINT ( 'NONE',  ( 0.000000000000000000, -51.10509369859380513, -77.10190917907254970 ) ) ;
#2545=VECTOR ( 'NONE', #8853, 1000.000000000000000 ) ;
#2546=ORIENTED_EDGE ( 'NONE', *, *, #18243, .F. ) ;
#2547=CARTESIAN_POINT ( 'NONE',  ( 10.00000000000000000, 0.000000000000000000, 0.000000000000000000 ) ) ;
#2548=VECTOR ( 'NONE', #9148, 1000.000000000000000 ) ;
#2553=EDGE_CURVE ( 'NONE', #8941, #1477, #9190, .T. ) ;
#2554=DIRECTION ( 'NONE',  ( -1.000000000000000000, -0.000000000000000000, -0.000000000000000000 ) ) ;
#2556=DIRECTION ( 'NONE',  ( 0.000000000000000000, 0.000000000000000000, 1.000000000000000000 ) ) ;
#2557=ORIENTED_EDGE ( 'NONE', *, *, #5783, .F. ) ;
#2558=ORIENTED_EDGE ( 'NONE', *, *, #12606, .T. ) ;
#2560=DIRECTION ( 'NONE',  ( 1.000000000000000000, 0.000000000000000000, 0.000000000000000000 ) ) ;
#2567=CIRCLE ( 'NONE', #18812, 92.50100000000000477 ) ;
#2568=AXIS2_PLACEMENT_3D ( 'NONE', #3633, #17344, #20865 ) ;
#2569=CARTESIAN_POINT ( 'NONE',  ( 10.00000000000000000, -29.29369617358407041, -87.74003855418429509 ) ) ;
#2571=CARTESIAN_POINT ( 'NONE',  ( 0.000000000000000000, 0.000000000000000000, 0.000000000000000000 ) ) ;
#2572=DIRECTION ( 'NONE',  ( 0.000000000000000000, 0.000000000000000000, 1.000000000000000000 ) ) ;
#2575=EDGE_CURVE ( 'NONE', #9950, #16436, #6385, .T. ) ;
#2578=ORIENTED_EDGE ( 'NONE', *, *, #2584, .F. ) ;
#2581=ORIENTED_EDGE ( 'NONE', *, *, #10962, .T. ) ;
#2583=VECTOR ( 'NONE', #1825, 1000.000000000000000 ) ;
#2584=EDGE_CURVE ( 'NONE', #3353, #2487, #8028, .T. ) ;
#2587=ORIENTED_EDGE ( 'NONE', *, *, #16944, .T. ) ;
#2588=CIRCLE ( 'NONE', #4012, 44.99999999999999289 ) ;
#2590=AXIS2_PLACEMENT_3D ( 'NONE', #9742, #12952, #14726 ) ;
#2593=ORIENTED_EDGE ( 'NONE', *, *, #18545, .F. ) ;
#2594=DIRECTION ( 'NONE',  ( -1.000000000000000000, -0.000000000000000000, -0.000000000000000000 ) ) ;
#2598=AXIS2_PLACEMENT_3D ( 'NONE', #10779, #20952, #17751 ) ;
#2602=ADVANCED_FACE ( 'NONE', ( #18309 ), #5150, .F. ) ;
#2607=VERTEX_POINT ( 'NONE', #16736 ) ;
#2608=AXIS2_PLACEMENT_3D ( 'NONE', #21498, #9881, #19500 ) ;
#2609=EDGE_CURVE ( 'NONE', #18821, #2865, #6407, .T. ) ;
#2610=CYLINDRICAL_SURFACE ( 'NONE', #21852, 88.00000000000000000 ) ;
#2611=DIRECTION ( 'NONE',  ( -1.000000000000000000, -0.000000000000000000, -0.000000000000000000 ) ) ;
#2612=CARTESIAN_POINT ( 'NONE',  ( 10.00000000000000000, -27.87320266523616752, 88.20158487341750231 ) ) ;
#2613=VERTEX_POINT ( 'NONE', #11669 ) ;
#2615=ADVANCED_FACE ( 'NONE', ( #3485 ), #19834, .F. ) ;
#2617=EDGE_LOOP ( 'NONE', ( #18680, #16035, #2578, #11756 ) ) ;
#2619=VERTEX_POINT ( 'NONE', #4700 ) ;
#2620=AXIS2_PLACEMENT_3D ( 'NONE', #833, #7578, #5927 ) ;
#2622=ORIENTED_EDGE ( 'NONE', *, *, #13020, .T. ) ;
#2623=CYLINDRICAL_SURFACE ( 'NONE', #7273, 45.00000000000000000 ) ;
#2624=CIRCLE ( 'NONE', #18867, 88.00000000000000000 ) ;
#2625=VERTEX_POINT ( 'NONE', #1607 ) ;
#2626=LINE ( 'NONE', #2743, #1012 ) ;
#2627=CARTESIAN_POINT ( 'NONE',  ( 10.00000000000000000, 47.19205848891765243, 74.27590198428138990 ) ) ;
#2629=DIRECTION ( 'NONE',  ( 0.000000000000000000, 0.000000000000000000, 1.000000000000000000 ) ) ;
#2630=AXIS2_PLACEMENT_3D ( 'NONE', #3431, #21475, #11824 ) ;
#2633=DIRECTION ( 'NONE',  ( 0.000000000000000000, -0.9271838545667832054, -0.3746065934159225619 ) ) ;
#2636=DIRECTION ( 'NONE',  ( 1.000000000000000000, 0.000000000000000000, 0.000000000000000000 ) ) ;
#2637=CIRCLE ( 'NONE', #20283, 88.00000000000000000 ) ;
#2639=LINE ( 'NONE', #2526, #926 ) ;
#2640=ORIENTED_EDGE ( 'NONE', *, *, #20917, .T. ) ;
#2641=ORIENTED_EDGE ( 'NONE', *, *, #12685, .F. ) ;
#2642=ORIENTED_EDGE ( 'NONE', *, *, #14904, .T. ) ;
#2643=ORIENTED_EDGE ( 'NONE', *, *, #3209, .T. ) ;
#2645=AXIS2_PLACEMENT_3D ( 'NONE', #16197, #14535, #10778 ) ;
#2647=AXIS2_PLACEMENT_3D ( 'NONE', #16940, #5333, #8635 ) ;
#2649=ORIENTED_EDGE ( 'NONE', *, *, #6913, .F. ) ;
#2650=CARTESIAN_POINT ( 'NONE',  ( 10.00000000000000000, 0.000000000000000000, 0.000000000000000000 ) ) ;
#2651=DIRECTION ( 'NONE',  ( -1.000000000000000000, -0.000000000000000000, -0.000000000000000000 ) ) ;
#2652=AXIS2_PLACEMENT_3D ( 'NONE', #9795, #1422, #13223 ) ;
#2653=FACE_OUTER_BOUND ( 'NONE', #9378, .T. ) ;
#2654=DIRECTION ( 'NONE',  ( 0.000000000000000000, 0.000000000000000000, 1.000000000000000000 ) ) ;
#2658=LINE ( 'NONE', #12811, #13964 ) ;
#2660=CARTESIAN_POINT ( 'NONE',  ( 0.000000000000000000, 0.000000000000000000, 0.000000000000000000 ) ) ;
#2661=AXIS2_PLACEMENT_3D ( 'NONE', #4605, #21399, #6277 ) ;
#2662=VERTEX_POINT ( 'NONE', #5032 ) ;
#2667=AXIS2_PLACEMENT_3D ( 'NONE', #9173, #17369, #5659 ) ;
#2668=VERTEX_POINT ( 'NONE', #15190 ) ;
#2669=DIRECTION ( 'NONE',  ( 0.000000000000000000, 0.000000000000000000, 1.000000000000000000 ) ) ;
#2670=DIRECTION ( 'NONE',  ( 0.000000000000000000, 0.000000000000000000, 1.000000000000000000 ) ) ;
#2672=CARTESIAN_POINT ( 'NONE',  ( 10.00000000000000000, 81.55207211302045778, 24.17537951050201883 ) ) ;
#2673=ORIENTED_EDGE ( 'NONE', *, *, #13687, .F. ) ;
#2674=VERTEX_POINT ( 'NONE', #11768 ) ;
#2678=ORIENTED_EDGE ( 'NONE', *, *, #14481, .T. ) ;
#2679=VECTOR ( 'NONE', #19900, 1000.000000000000000 ) ;
#2684=CARTESIAN_POINT ( 'NONE',  ( 10.00000000000000000, 57.47876254627226444, -62.70072803846332476 ) ) ;
#2685=DIRECTION ( 'NONE',  ( 1.000000000000000000, 0.000000000000000000, 0.000000000000000000 ) ) ;
#2686=ADVANCED_FACE ( 'NONE', ( #12089 ), #13858, .F. ) ;
#2687=CARTESIAN_POINT ( 'NONE',  ( 10.00000000000000000, 0.000000000000000000, 0.000000000000000000 ) ) ;
#2688=CARTESIAN_POINT ( 'NONE',  ( 10.00000000000000000, -21.65267340503189430, -89.93106657554454841 ) ) ;
#2689=DIRECTION ( 'NONE',  ( 0.000000000000000000, 0.6946583704589983643, -0.7193398003386500816 ) ) ;
#2690=DIRECTION ( 'NONE',  ( -1.000000000000000000, 0.000000000000000000, 0.000000000000000000 ) ) ;
#2691=DIRECTION ( 'NONE',  ( 0.000000000000000000, 0.000000000000000000, 1.000000000000000000 ) ) ;
#2693=CARTESIAN_POINT ( 'NONE',  ( 10.00000000000000000, 78.83848282823974785, -48.38314403117421847 ) ) ;
#2695=CIRCLE ( 'NONE', #18250, 88.00000000000000000 ) ;
#2696=CIRCLE ( 'NONE', #12228, 44.99999999999998579 ) ;
#2697=DIRECTION ( 'NONE',  ( -1.000000000000000000, -0.000000000000000000, 0.000000000000000000 ) ) ;
#2698=ADVANCED_FACE ( 'NONE', ( #7026 ), #12313, .F. ) ;
#2701=ORIENTED_EDGE ( 'NONE', *, *, #7045, .F. ) ;
#2702=EDGE_CURVE ( 'NONE', #21564, #10277, #8437, .T. ) ;
#2703=ORIENTED_EDGE ( 'NONE', *, *, #2335, .F. ) ;
#2704=ORIENTED_EDGE ( 'NONE', *, *, #15351, .F. ) ;
#2705=ORIENTED_EDGE ( 'NONE', *, *, #3213, .T. ) ;
#2707=DIRECTION ( 'NONE',  ( 0.000000000000000000, 0.9848077530122084644, -0.1736481776669273336 ) ) ;
#2708=ORIENTED_EDGE ( 'NONE', *, *, #19121, .T. ) ;
#2709=CIRCLE ( 'NONE', #21764, 88.00000000000000000 ) ;
#2716=EDGE_CURVE ( 'NONE', #11894, #7808, #13356, .T. ) ;
#2718=VECTOR ( 'NONE', #866, 1000.000000000000000 ) ;
#2721=ORIENTED_EDGE ( 'NONE', *, *, #5400, .F. ) ;
#2723=LINE ( 'NONE', #4271, #19244 ) ;
#2725=DIRECTION ( 'NONE',  ( 1.000000000000000000, 0.000000000000000000, 0.000000000000000000 ) ) ;
#2726=ADVANCED_FACE ( 'NONE', ( #11988 ), #13643, .F. ) ;
#2727=ORIENTED_EDGE ( 'NONE', *, *, #13366, .T. ) ;
#2728=VECTOR ( 'NONE', #9045, 1000.000000000000000 ) ;
#2729=DIRECTION ( 'NONE',  ( 1.000000000000000000, 0.000000000000000000, 0.000000000000000000 ) ) ;
#2730=CIRCLE ( 'NONE', #3444, 92.50100000000000477 ) ;
#2731=DIRECTION ( 'NONE',  ( 1.000000000000000000, 0.000000000000000000, 0.000000000000000000 ) ) ;
#2732=ADVANCED_FACE ( 'NONE', ( #15292 ), #5578, .F. ) ;
#2733=AXIS2_PLACEMENT_3D ( 'NONE', #7058, #20200, #15437 ) ;
#2734=ORIENTED_EDGE ( 'NONE', *, *, #21329, .T. ) ;
#2736=EDGE_CURVE ( 'NONE', #18369, #7224, #4018, .T. ) ;
#2737=ORIENTED_EDGE ( 'NONE', *, *, #7207, .T. ) ;
#2738=EDGE_LOOP ( 'NONE', ( #17858, #2737, #11761, #13895 ) ) ;
#2739=ORIENTED_EDGE ( 'NONE', *, *, #13154, .T. ) ;
#2740=CARTESIAN_POINT ( 'NONE',  ( 10.00000000000000000, 9.646732466566502850, -84.51112348751837544 ) ) ;
#2743=CARTESIAN_POINT ( 'NONE',  ( 5.000000000000000000, -83.48638250753248258, 27.82128566055087049 ) ) ;
#2744=LINE ( 'NONE', #20975, #7241 ) ;
#2745=CARTESIAN_POINT ( 'NONE',  ( 10.00000000000000000, 0.000000000000000000, 0.000000000000000000 ) ) ;
#2746=DIRECTION ( 'NONE',  ( -1.000000000000000000, 0.000000000000000000, 0.000000000000000000 ) ) ;
#2747=AXIS2_PLACEMENT_3D ( 'NONE', #6989, #3983, #8950 ) ;
#2748=EDGE_CURVE ( 'NONE', #21192, #2262, #3226, .T. ) ;
#2751=CARTESIAN_POINT ( 'NONE',  ( 10.00000000000000000, -80.18694381077126820, 28.37681241246628616 ) ) ;
#2752=AXIS2_PLACEMENT_3D ( 'NONE', #5492, #406, #5380 ) ;
#2753=AXIS2_PLACEMENT_3D ( 'NONE', #6359, #15164, #14732 ) ;
#2754=CARTESIAN_POINT ( 'NONE',  ( 10.00000000000000000, -32.56745702629687855, -78.57830605990686479 ) ) ;
#2755=EDGE_CURVE ( 'NONE', #21410, #5809, #10645, .T. ) ;
#2757=DIRECTION ( 'NONE',  ( 1.000000000000000000, 0.000000000000000000, 0.000000000000000000 ) ) ;
#2763=CIRCLE ( 'NONE', #14769, 92.50100000000000477 ) ;
#2766=AXIS2_PLACEMENT_3D ( 'NONE', #19687, #9729, #4772 ) ;
#2767=AXIS2_PLACEMENT_3D ( 'NONE', #579, #11171, #6099 ) ;
#2768=EDGE_CURVE ( 'NONE', #4275, #19773, #7237, .T. ) ;
#2773=DIRECTION ( 'NONE',  ( 1.000000000000000000, 0.000000000000000000, 0.000000000000000000 ) ) ;
#2778=LINE ( 'NONE', #9274, #8020 ) ;
#2782=VECTOR ( 'NONE', #15658, 1000.000000000000000 ) ;
#2784=ORIENTED_EDGE ( 'NONE', *, *, #18493, .F. ) ;
#2785=AXIS2_PLACEMENT_3D ( 'NONE', #17244, #8840, #13472 ) ;
#2786=CARTESIAN_POINT ( 'NONE',  ( 10.00000000000000000, 0.000000000000000000, 0.000000000000000000 ) ) ;
#2787=EDGE_LOOP ( 'NONE', ( #17301, #12451, #2092, #4171 ) ) ;
#2789=DIRECTION ( 'NONE',  ( -1.000000000000000000, 0.000000000000000000, 0.000000000000000000 ) ) ;
#2790=DIRECTION ( 'NONE',  ( 0.000000000000000000, 0.6427876096865403621, -0.7660444431189772363 ) ) ;
#2792=FACE_OUTER_BOUND ( 'NONE', #3643, .T. ) ;
#2794=ORIENTED_EDGE ( 'NONE', *, *, #21494, .F. ) ;
#2796=VECTOR ( 'NONE', #21843, 1000.000000000000000 ) ;
#2797=CARTESIAN_POINT ( 'NONE',  ( 5.000000000000002665, 0.6609040254623512745, -87.99751818016873983 ) ) ;
#2798=ORIENTED_EDGE ( 'NONE', *, *, #16944, .F. ) ;
#2800=ORIENTED_EDGE ( 'NONE', *, *, #1906, .T. ) ;
#2803=AXIS2_PLACEMENT_3D ( 'NONE', #16773, #15215, #3408 ) ;
#2804=DIRECTION ( 'NONE',  ( -1.000000000000000000, -0.000000000000000000, -0.000000000000000000 ) ) ;
#2811=ORIENTED_EDGE ( 'NONE', *, *, #19488, .F. ) ;
#2813=AXIS2_PLACEMENT_3D ( 'NONE', #19697, #4667, #11404 ) ;
#2815=CIRCLE ( 'NONE', #15155, 92.50100000000000477 ) ;
#2817=DIRECTION ( 'NONE',  ( 0.000000000000000000, 0.000000000000000000, 1.000000000000000000 ) ) ;
#2818=EDGE_CURVE ( 'NONE', #18794, #17904, #17298, .T. ) ;
#2821=ORIENTED_EDGE ( 'NONE', *, *, #19984, .T. ) ;
#2822=EDGE_LOOP ( 'NONE', ( #5751, #7159, #11396, #1890 ) ) ;
#2823=ORIENTED_EDGE ( 'NONE', *, *, #7215, .T. ) ;
#2824=DIRECTION ( 'NONE',  ( 1.000000000000000000, 0.000000000000000000, 0.000000000000000000 ) ) ;
#2826=EDGE_LOOP ( 'NONE', ( #10289, #16219, #3929, #4299 ) ) ;
#2827=CARTESIAN_POINT ( 'NONE',  ( 0.000000000000000000, 77.39385041987151226, -35.28996114464630551 ) ) ;
#2828=LINE ( 'NONE', #16295, #18592 ) ;
#2829=LINE ( 'NONE', #17646, #17125 ) ;
#2830=CIRCLE ( 'NONE', #5653, 88.00000000000000000 ) ;
#2834=ORIENTED_EDGE ( 'NONE', *, *, #13831, .F. ) ;
#2835=DIRECTION ( 'NONE',  ( 1.000000000000000000, 0.000000000000000000, 0.000000000000000000 ) ) ;
#2836=CARTESIAN_POINT ( 'NONE',  ( 10.00000000000000000, 92.32475887865433606, -5.707354816229567973 ) ) ;
#2839=EDGE_LOOP ( 'NONE', ( #5345, #2376, #6902, #12220 ) ) ;
#2840=EDGE_CURVE ( 'NONE', #5619, #17311, #14287, .T. ) ;
#2841=DIRECTION ( 'NONE',  ( 1.000000000000000000, 0.000000000000000000, 0.000000000000000000 ) ) ;
#2845=CARTESIAN_POINT ( 'NONE',  ( 0.000000000000000000, -47.19205848891713373, -74.27590198428171675 ) ) ;
#2846=ORIENTED_EDGE ( 'NONE', *, *, #17293, .F. ) ;
#2848=EDGE_CURVE ( 'NONE', #17141, #10612, #19481, .T. ) ;
#2851=DIRECTION ( 'NONE',  ( 1.000000000000000000, -0.000000000000000000, -0.000000000000000000 ) ) ;
#2852=VERTEX_POINT ( 'NONE', #21364 ) ;
#2854=DIRECTION ( 'NONE',  ( -1.000000000000000000, -0.000000000000000000, -0.000000000000000000 ) ) ;
#2856=DIRECTION ( 'NONE',  ( 0.000000000000000000, 0.1391731009600657432, -0.9902680687415702510 ) ) ;
#2857=ADVANCED_FACE ( 'NONE', ( #5905 ), #6026, .F. ) ;
#2858=CARTESIAN_POINT ( 'NONE',  ( 10.00000000000000000, -11.59241532900687233, 87.23311244498734141 ) ) ;
#2861=EDGE_CURVE ( 'NONE', #5782, #5530, #20315, .T. ) ;
#2862=CARTESIAN_POINT ( 'NONE',  ( 0.000000000000000000, 89.12061559554332746, 24.77803214283573396 ) ) ;
#2864=ORIENTED_EDGE ( 'NONE', *, *, #8900, .T. ) ;
#2865=VERTEX_POINT ( 'NONE', #4134 ) ;
#2866=ORIENTED_EDGE ( 'NONE', *, *, #7314, .F. ) ;
#2868=ORIENTED_EDGE ( 'NONE', *, *, #4512, .F. ) ;
#2869=VERTEX_POINT ( 'NONE', #4345 ) ;
#2872=DIRECTION ( 'NONE',  ( -1.000000000000000000, -0.000000000000000000, -0.000000000000000000 ) ) ;
#2874=EDGE_CURVE ( 'NONE', #8708, #11578, #19382, .T. ) ;
#2875=CARTESIAN_POINT ( 'NONE',  ( 0.000000000000000000, 0.000000000000000000, 0.000000000000000000 ) ) ;
#2876=CARTESIAN_POINT ( 'NONE',  ( 0.000000000000000000, -8.134922360106683570, 84.67002113262478247 ) ) ;
#2877=CARTESIAN_POINT ( 'NONE',  ( 10.00000000000000000, 81.97107881582195432, 22.71412948308594437 ) ) ;
#2878=EDGE_CURVE ( 'NONE', #2527, #15117, #9102, .T. ) ;
#2879=DIRECTION ( 'NONE',  ( -1.000000000000000000, -0.000000000000000000, -0.000000000000000000 ) ) ;
#2880=CARTESIAN_POINT ( 'NONE',  ( 0.000000000000000000, 3.974475837766159980, -92.41557521768187655 ) ) ;
#2882=EDGE_CURVE ( 'NONE', #10824, #8047, #7247, .T. ) ;
#2883=VERTEX_POINT ( 'NONE', #9201 ) ;
#2884=EDGE_CURVE ( 'NONE', #1840, #19484, #17136, .T. ) ;
#2885=DIRECTION ( 'NONE',  ( 0.000000000000000000, 0.000000000000000000, 1.000000000000000000 ) ) ;
#2886=ORIENTED_EDGE ( 'NONE', *, *, #8646, .T. ) ;
#2887=ORIENTED_EDGE ( 'NONE', *, *, #3656, .F. ) ;
#2890=DIRECTION ( 'NONE',  ( -1.000000000000000000, -0.000000000000000000, -0.000000000000000000 ) ) ;
#2891=ORIENTED_EDGE ( 'NONE', *, *, #5684, .F. ) ;
#2892=DIRECTION ( 'NONE',  ( -1.000000000000000000, 0.000000000000000000, 0.000000000000000000 ) ) ;
#2893=ORIENTED_EDGE ( 'NONE', *, *, #6691, .F. ) ;
#2896=CARTESIAN_POINT ( 'NONE',  ( 0.000000000000000000, 15.32665449651924661, 91.22241316115426457 ) ) ;
#2897=ORIENTED_EDGE ( 'NONE', *, *, #18483, .T. ) ;
#2898=EDGE_LOOP ( 'NONE', ( #8789, #10979, #4690, #11709 ) ) ;
#2900=CYLINDRICAL_SURFACE ( 'NONE', #6693, 92.50100000000000477 ) ;
#2903=CARTESIAN_POINT ( 'NONE',  ( 10.00000000000000000, 68.36541360927188293, 50.60987712331726840 ) ) ;
#2904=DIRECTION ( 'NONE',  ( 0.000000000000000000, 0.8290375725550428454, -0.5591929034707450175 ) ) ;
#2905=DIRECTION ( 'NONE',  ( 0.000000000000000000, 0.000000000000000000, 1.000000000000000000 ) ) ;
#2906=DIRECTION ( 'NONE',  ( 0.000000000000000000, 0.000000000000000000, 1.000000000000000000 ) ) ;
#2907=DIRECTION ( 'NONE',  ( -1.000000000000000000, -0.000000000000000000, -0.000000000000000000 ) ) ;
#2909=VECTOR ( 'NONE', #12081, 1000.000000000000000 ) ;
#2910=VERTEX_POINT ( 'NONE', #5794 ) ;
#2911=AXIS2_PLACEMENT_3D ( 'NONE', #87, #19865, #6516 ) ;
#2912=EDGE_LOOP ( 'NONE', ( #12770, #8395, #17754, #1475 ) ) ;
#2913=CARTESIAN_POINT ( 'NONE',  ( 0.000000000000000000, 91.70173545986537533, -12.13370160539944287 ) ) ;
#2918=ORIENTED_EDGE ( 'NONE', *, *, #7029, .T. ) ;
#2919=AXIS2_PLACEMENT_3D ( 'NONE', #433, #19207, #4071 ) ;
#2920=ORIENTED_EDGE ( 'NONE', *, *, #4236, .T. ) ;
#2923=LINE ( 'NONE', #14753, #12525 ) ;
#2924=VECTOR ( 'NONE', #3901, 1000.000000000000000 ) ;
#2926=CIRCLE ( 'NONE', #5759, 44.99999999999999289 ) ;
#2927=CARTESIAN_POINT ( 'NONE',  ( 0.000000000000000000, 78.04699792498145428, 49.64978465107317618 ) ) ;
#2929=CARTESIAN_POINT ( 'NONE',  ( 0.000000000000000000, -41.21966518005896774, -82.80926399530329718 ) ) ;
#2933=CIRCLE ( 'NONE', #9994, 45.00000000000000711 ) ;
#2934=ADVANCED_FACE ( 'NONE', ( #12956 ), #19708, .F. ) ;
#2935=ORIENTED_EDGE ( 'NONE', *, *, #17047, .T. ) ;
#2936=DIRECTION ( 'NONE',  ( -1.000000000000000000, -0.000000000000000000, 0.000000000000000000 ) ) ;
#2939=VERTEX_POINT ( 'NONE', #15947 ) ;
#2940=EDGE_CURVE ( 'NONE', #13200, #733, #1252, .T. ) ;
#2942=DIRECTION ( 'NONE',  ( -1.000000000000000000, -0.000000000000000000, -0.000000000000000000 ) ) ;
#2945=CARTESIAN_POINT ( 'NONE',  ( 10.00000000000000000, -71.33759994381919967, -58.88447872959059026 ) ) ;
#2946=ORIENTED_EDGE ( 'NONE', *, *, #3423, .T. ) ;
#2948=VECTOR ( 'NONE', #308, 1000.000000000000000 ) ;
#2949=ORIENTED_EDGE ( 'NONE', *, *, #13942, .F. ) ;
#2952=ORIENTED_EDGE ( 'NONE', *, *, #7432, .T. ) ;
#2954=AXIS2_PLACEMENT_3D ( 'NONE', #9861, #11642, #4673 ) ;
#2957=DIRECTION ( 'NONE',  ( 0.000000000000000000, 0.000000000000000000, 1.000000000000000000 ) ) ;
#2958=AXIS2_PLACEMENT_3D ( 'NONE', #14858, #21595, #940 ) ;
#2959=EDGE_CURVE ( 'NONE', #6824, #17849, #13593, .T. ) ;
#2960=DIRECTION ( 'NONE',  ( -1.000000000000000000, -0.000000000000000000, 0.000000000000000000 ) ) ;
#2961=EDGE_CURVE ( 'NONE', #5897, #12371, #3358, .T. ) ;
#2962=LINE ( 'NONE', #18549, #10664 ) ;
#2963=DIRECTION ( 'NONE',  ( -1.000000000000000000, -0.000000000000000000, -0.000000000000000000 ) ) ;
#2964=CYLINDRICAL_SURFACE ( 'NONE', #10914, 92.50100000000000477 ) ;
#2965=AXIS2_PLACEMENT_3D ( 'NONE', #4016, #709, #10641 ) ;
#2968=CIRCLE ( 'NONE', #5799, 88.00000000000000000 ) ;
#2969=EDGE_LOOP ( 'NONE', ( #21371, #12356, #3685, #8578 ) ) ;
#2970=ORIENTED_EDGE ( 'NONE', *, *, #1086, .T. ) ;
#2972=EDGE_CURVE ( 'NONE', #9876, #1625, #4072, .T. ) ;
#2974=ORIENTED_EDGE ( 'NONE', *, *, #8864, .T. ) ;
#2975=ADVANCED_FACE ( 'NONE', ( #3342 ), #11737, .F. ) ;
#2976=CARTESIAN_POINT ( 'NONE',  ( 0.000000000000000000, 61.60362715319122628, -62.84101464466179721 ) ) ;
#2978=CARTESIAN_POINT ( 'NONE',  ( 0.000000000000000000, -45.60224695560626174, 80.47900393021710386 ) ) ;
#2980=FACE_OUTER_BOUND ( 'NONE', #7219, .T. ) ;
#2981=AXIS2_PLACEMENT_3D ( 'NONE', #4013, #8875, #17508 ) ;
#2982=ADVANCED_FACE ( 'NONE', ( #16826 ), #11530, .F. ) ;
#2983=CARTESIAN_POINT ( 'NONE',  ( 5.000000000000002665, -40.72878876293093242, -78.00747250042492453 ) ) ;
#2984=DIRECTION ( 'NONE',  ( 1.000000000000000000, 0.000000000000000000, -0.000000000000000000 ) ) ;
#2985=CYLINDRICAL_SURFACE ( 'NONE', #20700, 45.00000000000000000 ) ;
#2986=EDGE_CURVE ( 'NONE', #10498, #2910, #1962, .T. ) ;
#2987=AXIS2_PLACEMENT_3D ( 'NONE', #4892, #11636, #2192 ) ;
#2988=DIRECTION ( 'NONE',  ( 0.000000000000000000, 0.2756373558169998295, -0.9612616959383187831 ) ) ;
#2989=DIRECTION ( 'NONE',  ( 0.000000000000000000, 0.9993908270190956511, 0.03489949670250451497 ) ) ;
#2992=DIRECTION ( 'NONE',  ( 0.000000000000000000, 0.7880107536067233465, -0.6156614753256567374 ) ) ;
#2993=AXIS2_PLACEMENT_3D ( 'NONE', #2751, #11025, #12908 ) ;
#2995=ORIENTED_EDGE ( 'NONE', *, *, #8197, .F. ) ;
#2996=AXIS2_PLACEMENT_3D ( 'NONE', #1168, #17862, #12546 ) ;
#2998=EDGE_CURVE ( 'NONE', #5274, #9309, #4674, .T. ) ;
#3002=DIRECTION ( 'NONE',  ( -1.000000000000000000, -0.000000000000000000, -0.000000000000000000 ) ) ;
#3003=ORIENTED_EDGE ( 'NONE', *, *, #10497, .F. ) ;
#3004=EDGE_CURVE ( 'NONE', #1789, #8068, #20329, .T. ) ;
#3010=VECTOR ( 'NONE', #18406, 1000.000000000000000 ) ;
#3011=DIRECTION ( 'NONE',  ( 0.000000000000000000, 0.000000000000000000, 1.000000000000000000 ) ) ;
#3012=FACE_OUTER_BOUND ( 'NONE', #2826, .T. ) ;
#3015=DIRECTION ( 'NONE',  ( 0.000000000000000000, -0.3420201433256757073, 0.9396926207859058744 ) ) ;
#3016=AXIS2_PLACEMENT_3D ( 'NONE', #9863, #11413, #16710 ) ;
#3017=AXIS2_PLACEMENT_3D ( 'NONE', #5503, #15650, #16996 ) ;
#3018=CARTESIAN_POINT ( 'NONE',  ( 10.00000000000000000, -86.54587337002867287, -15.93147207947093946 ) ) ;
#3019=AXIS2_PLACEMENT_3D ( 'NONE', #12186, #11973, #20264 ) ;
#3021=AXIS2_PLACEMENT_3D ( 'NONE', #275, #59, #17068 ) ;
#3022=CARTESIAN_POINT ( 'NONE',  ( 0.000000000000000000, 18.94217447942559573, 85.93715160505956874 ) ) ;
#3025=CIRCLE ( 'NONE', #12536, 88.00000000000000000 ) ;
#3026=ADVANCED_FACE ( 'NONE', ( #6358 ), #19921, .F. ) ;
#3027=ORIENTED_EDGE ( 'NONE', *, *, #14112, .F. ) ;
#3028=VERTEX_POINT ( 'NONE', #36 ) ;
#3032=AXIS2_PLACEMENT_3D ( 'NONE', #3489, #9074, #10228 ) ;
#3033=CYLINDRICAL_SURFACE ( 'NONE', #21720, 44.99999999999999289 ) ;
#3034=AXIS2_PLACEMENT_3D ( 'NONE', #390, #3813, #13860 ) ;
#3035=ORIENTED_EDGE ( 'NONE', *, *, #17571, .F. ) ;
#3036=AXIS2_PLACEMENT_3D ( 'NONE', #9743, #18052, #2904 ) ;
#3037=VECTOR ( 'NONE', #12712, 1000.000000000000000 ) ;
#3038=ORIENTED_EDGE ( 'NONE', *, *, #11898, .F. ) ;
#3042=LINE ( 'NONE', #1483, #8653 ) ;
#3044=EDGE_CURVE ( 'NONE', #4876, #7568, #16085, .T. ) ;
#3045=FACE_OUTER_BOUND ( 'NONE', #4364, .T. ) ;
#3047=CARTESIAN_POINT ( 'NONE',  ( -10.00000000000000000, 0.000000000000000000, 0.000000000000000000 ) ) ;
#3048=DIRECTION ( 'NONE',  ( 0.000000000000000000, -0.8290375725550350738, -0.5591929034707566748 ) ) ;
#3052=ORIENTED_EDGE ( 'NONE', *, *, #21055, .T. ) ;
#3053=AXIS2_PLACEMENT_3D ( 'NONE', #11641, #7997, #4787 ) ;
#3054=FACE_OUTER_BOUND ( 'NONE', #19989, .T. ) ;
#3056=EDGE_LOOP ( 'NONE', ( #6134, #18407, #21026, #15954 ) ) ;
#3057=DIRECTION ( 'NONE',  ( 0.000000000000000000, 0.3420201433256631063, 0.9396926207859105373 ) ) ;
#3058=ORIENTED_EDGE ( 'NONE', *, *, #415, .T. ) ;
#3059=FACE_OUTER_BOUND ( 'NONE', #19879, .T. ) ;
#3061=VERTEX_POINT ( 'NONE', #11306 ) ;
#3063=ORIENTED_EDGE ( 'NONE', *, *, #14328, .T. ) ;
#3064=CIRCLE ( 'NONE', #21409, 45.00000000000000000 ) ;
#3066=ORIENTED_EDGE ( 'NONE', *, *, #13794, .T. ) ;
#3067=CARTESIAN_POINT ( 'NONE',  ( 10.00000000000000000, -84.80486432185219314, 36.94008646920367056 ) ) ;
#3068=AXIS2_PLACEMENT_3D ( 'NONE', #137, #20476, #13938 ) ;
#3069=ORIENTED_EDGE ( 'NONE', *, *, #15686, .F. ) ;
#3071=DIRECTION ( 'NONE',  ( -1.000000000000000000, 0.000000000000000000, 0.000000000000000000 ) ) ;
#3072=CARTESIAN_POINT ( 'NONE',  ( 0.000000000000000000, -65.83713140174687339, -58.39068529131263574 ) ) ;
#3077=CARTESIAN_POINT ( 'NONE',  ( -10.00000000000000000, 0.000000000000000000, 0.000000000000000000 ) ) ;
#3078=CARTESIAN_POINT ( 'NONE',  ( 10.00000000000000000, -83.35585896458606214, -16.94078559808036033 ) ) ;
#3079=CARTESIAN_POINT ( 'NONE',  ( 10.00000000000000000, 27.87320266523671819, -88.20158487341731757 ) ) ;
#3080=AXIS2_PLACEMENT_3D ( 'NONE', #15135, #10602, #12044 ) ;
#3082=AXIS2_PLACEMENT_3D ( 'NONE', #5719, #7810, #14329 ) ;
#3084=DIRECTION ( 'NONE',  ( -1.000000000000000000, -0.000000000000000000, -0.000000000000000000 ) ) ;
#3086=VERTEX_POINT ( 'NONE', #3130 ) ;
#3087=ORIENTED_EDGE ( 'NONE', *, *, #11259, .T. ) ;
#3088=ORIENTED_EDGE ( 'NONE', *, *, #422, .F. ) ;
#3091=DIRECTION ( 'NONE',  ( -1.000000000000000000, 0.000000000000000000, -0.000000000000000000 ) ) ;
#3093=ORIENTED_EDGE ( 'NONE', *, *, #3131, .T. ) ;
#3094=FACE_OUTER_BOUND ( 'NONE', #8793, .T. ) ;
#3095=AXIS2_PLACEMENT_3D ( 'NONE', #17633, #21045, #12413 ) ;
#3097=EDGE_CURVE ( 'NONE', #6505, #2865, #8323, .T. ) ;
#3098=DIRECTION ( 'NONE',  ( 1.000000000000000000, -0.000000000000000000, -0.000000000000000000 ) ) ;
#3099=CARTESIAN_POINT ( 'NONE',  ( 0.000000000000000000, 64.66851233300799606, -55.25552418572899427 ) ) ;
#3101=DIRECTION ( 'NONE',  ( 0.000000000000000000, 0.000000000000000000, 1.000000000000000000 ) ) ;
#3102=EDGE_CURVE ( 'NONE', #20413, #11578, #1629, .T. ) ;
#3103=CARTESIAN_POINT ( 'NONE',  ( 10.00000000000000000, 0.000000000000000000, 0.000000000000000000 ) ) ;
#3107=ORIENTED_EDGE ( 'NONE', *, *, #20938, .T. ) ;
#3108=ORIENTED_EDGE ( 'NONE', *, *, #13816, .T. ) ;
#3109=CARTESIAN_POINT ( 'NONE',  ( 10.00000000000000000, 2.208823992045340301, -85.03123271466934341 ) ) ;
#3111=ORIENTED_EDGE ( 'NONE', *, *, #10788, .T. ) ;
#3112=EDGE_CURVE ( 'NONE', #15636, #8019, #10622, .T. ) ;
#3114=DIRECTION ( 'NONE',  ( 0.000000000000000000, 0.000000000000000000, 1.000000000000000000 ) ) ;
#3115=ORIENTED_EDGE ( 'NONE', *, *, #17299, .T. ) ;
#3119=EDGE_LOOP ( 'NONE', ( #17057, #6468, #9490, #21620 ) ) ;
#3121=FACE_OUTER_BOUND ( 'NONE', #21077, .T. ) ;
#3124=DIRECTION ( 'NONE',  ( 0.000000000000000000, 0.1391731009600657987, -0.9902680687415702510 ) ) ;
#3125=VECTOR ( 'NONE', #14548, 1000.000000000000000 ) ;
#3126=CARTESIAN_POINT ( 'NONE',  ( 10.00000000000000000, 0.000000000000000000, 0.000000000000000000 ) ) ;
#3128=AXIS2_PLACEMENT_3D ( 'NONE', #1453, #13271, #20024 ) ;
#3129=FACE_OUTER_BOUND ( 'NONE', #7443, .T. ) ;
#3130=CARTESIAN_POINT ( 'NONE',  ( 0.000000000000000000, -15.32665449651985590, 91.22241316115413667 ) ) ;
#3131=EDGE_CURVE ( 'NONE', #2159, #15310, #218, .T. ) ;
#3132=CARTESIAN_POINT ( 'NONE',  ( -10.00000000000000000, 0.000000000000000000, 0.000000000000000000 ) ) ;
#3133=EDGE_LOOP ( 'NONE', ( #399, #724, #2117, #352 ) ) ;
#3136=CARTESIAN_POINT ( 'NONE',  ( 10.00000000000000000, 0.000000000000000000, 0.000000000000000000 ) ) ;
#3137=CIRCLE ( 'NONE', #17957, 92.50100000000000477 ) ;
#3138=DIRECTION ( 'NONE',  ( 0.000000000000000000, 0.000000000000000000, 1.000000000000000000 ) ) ;
#3139=VERTEX_POINT ( 'NONE', #11966 ) ;
#3140=CIRCLE ( 'NONE', #4201, 88.00000000000000000 ) ;
#3141=FACE_OUTER_BOUND ( 'NONE', #10285, .T. ) ;
#3143=ORIENTED_EDGE ( 'NONE', *, *, #4563, .F. ) ;
#3147=ORIENTED_EDGE ( 'NONE', *, *, #6494, .F. ) ;
#3150=CARTESIAN_POINT ( 'NONE',  ( 10.00000000000000000, 0.000000000000000000, 0.000000000000000000 ) ) ;
#3152=VECTOR ( 'NONE', #365, 1000.000000000000000 ) ;
#3154=CARTESIAN_POINT ( 'NONE',  ( 10.00000000000000000, -40.72878876293093242, -78.00747250042492453 ) ) ;
#3155=DIRECTION ( 'NONE',  ( 1.000000000000000000, 0.000000000000000000, 0.000000000000000000 ) ) ;
#3157=DIRECTION ( 'NONE',  ( 0.000000000000000000, -0.9945218953682722907, -0.1045284632676634906 ) ) ;
#3158=DIRECTION ( 'NONE',  ( 0.000000000000000000, 0.000000000000000000, 1.000000000000000000 ) ) ;
#3159=EDGE_CURVE ( 'NONE', #12184, #6987, #18169, .T. ) ;
#3160=AXIS2_PLACEMENT_3D ( 'NONE', #4474, #6698, #21491 ) ;
#3161=CIRCLE ( 'NONE', #15503, 88.00000000000000000 ) ;
#3162=ORIENTED_EDGE ( 'NONE', *, *, #10633, .F. ) ;
#3163=EDGE_CURVE ( 'NONE', #14101, #13181, #251, .T. ) ;
#3164=CIRCLE ( 'NONE', #5285, 88.00000000000000000 ) ;
#3165=DIRECTION ( 'NONE',  ( 1.000000000000000000, 0.000000000000000000, 0.000000000000000000 ) ) ;
#3166=DIRECTION ( 'NONE',  ( 0.000000000000000000, -0.8290375725550350738, -0.5591929034707566748 ) ) ;
#3167=ORIENTED_EDGE ( 'NONE', *, *, #7876, .T. ) ;
#3170=DIRECTION ( 'NONE',  ( 1.000000000000000000, -0.000000000000000000, -0.000000000000000000 ) ) ;
#3173=DIRECTION ( 'NONE',  ( -1.000000000000000000, -0.000000000000000000, -0.000000000000000000 ) ) ;
#3174=ORIENTED_EDGE ( 'NONE', *, *, #5865, .T. ) ;
#3175=CARTESIAN_POINT ( 'NONE',  ( 10.00000000000000000, 0.000000000000000000, 0.000000000000000000 ) ) ;
#3176=ORIENTED_EDGE ( 'NONE', *, *, #17732, .T. ) ;
#3177=ORIENTED_EDGE ( 'NONE', *, *, #18439, .F. ) ;
#3178=CIRCLE ( 'NONE', #13759, 88.00000000000000000 ) ;
#3181=EDGE_LOOP ( 'NONE', ( #21643, #21647, #3093, #2314 ) ) ;
#3182=CARTESIAN_POINT ( 'NONE',  ( 0.000000000000000000, 66.01871308925461790, 64.79170103523043167 ) ) ;
#3184=CARTESIAN_POINT ( 'NONE',  ( 10.00000000000000000, 9.646732466566502850, -84.51112348751837544 ) ) ;
#3185=CARTESIAN_POINT ( 'NONE',  ( 0.000000000000000000, 8.925965667928872804, 92.06933331948788179 ) ) ;
#3186=CARTESIAN_POINT ( 'NONE',  ( 10.00000000000000000, 61.33825423015778711, -69.23910433415882437 ) ) ;
#3188=DIRECTION ( 'NONE',  ( -1.000000000000000000, -0.000000000000000000, -0.000000000000000000 ) ) ;
#3192=DIRECTION ( 'NONE',  ( 0.000000000000000000, 0.000000000000000000, 1.000000000000000000 ) ) ;
#3194=ORIENTED_EDGE ( 'NONE', *, *, #19459, .F. ) ;
#3195=ORIENTED_EDGE ( 'NONE', *, *, #14599, .F. ) ;
#3196=ORIENTED_EDGE ( 'NONE', *, *, #17025, .T. ) ;
#3200=CYLINDRICAL_SURFACE ( 'NONE', #17740, 92.50100000000000477 ) ;
#3201=AXIS2_PLACEMENT_3D ( 'NONE', #21522, #6399, #12773 ) ;
#3202=CARTESIAN_POINT ( 'NONE',  ( 10.00000000000000000, 71.33759994381962599, 58.88447872959010709 ) ) ;
#3203=CYLINDRICAL_SURFACE ( 'NONE', #4688, 88.00000000000000000 ) ;
#3204=DIRECTION ( 'NONE',  ( 1.000000000000000000, 0.000000000000000000, 0.000000000000000000 ) ) ;
#3206=CARTESIAN_POINT ( 'NONE',  ( 10.00000000000000000, 0.000000000000000000, 0.000000000000000000 ) ) ;
#3207=CARTESIAN_POINT ( 'NONE',  ( 10.00000000000000000, 46.93287725819874368, -70.94007663282398823 ) ) ;
#3209=EDGE_CURVE ( 'NONE', #12163, #4259, #7239, .T. ) ;
#3211=DIRECTION ( 'NONE',  ( -1.000000000000000000, -0.000000000000000000, -0.000000000000000000 ) ) ;
#3212=ORIENTED_EDGE ( 'NONE', *, *, #19486, .F. ) ;
#3213=EDGE_CURVE ( 'NONE', #12268, #2625, #10048, .T. ) ;
#3214=VERTEX_POINT ( 'NONE', #8537 ) ;
#3217=DIRECTION ( 'NONE',  ( -1.000000000000000000, -0.000000000000000000, -0.000000000000000000 ) ) ;
#3218=EDGE_LOOP ( 'NONE', ( #15798, #14144, #4257, #3451 ) ) ;
#3226=CIRCLE ( 'NONE', #1461, 44.99999999999998579 ) ;
#3228=CARTESIAN_POINT ( 'NONE',  ( 10.00000000000000000, 61.71252885873465033, -58.53847642588533517 ) ) ;
#3232=DIRECTION ( 'NONE',  ( -1.000000000000000000, 0.000000000000000000, -0.000000000000000000 ) ) ;
#3238=CARTESIAN_POINT ( 'NONE',  ( 10.00000000000000000, 0.000000000000000000, 0.000000000000000000 ) ) ;
#3239=LINE ( 'NONE', #16833, #17998 ) ;
#3240=ORIENTED_EDGE ( 'NONE', *, *, #3893, .T. ) ;
#3246=ORIENTED_EDGE ( 'NONE', *, *, #4484, .F. ) ;
#3249=ORIENTED_EDGE ( 'NONE', *, *, #7613, .T. ) ;
#3251=DIRECTION ( 'NONE',  ( 0.000000000000000000, -0.9993908270190954291, -0.03489949670251119018 ) ) ;
#3252=ORIENTED_EDGE ( 'NONE', *, *, #13768, .F. ) ;
#3253=EDGE_CURVE ( 'NONE', #3881, #6503, #15821, .T. ) ;
#3254=AXIS2_PLACEMENT_3D ( 'NONE', #14479, #11043, #17794 ) ;
#3255=DIRECTION ( 'NONE',  ( 0.000000000000000000, 0.000000000000000000, 1.000000000000000000 ) ) ;
#3259=DIRECTION ( 'NONE',  ( -1.000000000000000000, -0.000000000000000000, 0.000000000000000000 ) ) ;
#3260=CARTESIAN_POINT ( 'NONE',  ( 10.00000000000000000, 0.000000000000000000, 0.000000000000000000 ) ) ;
#3265=EDGE_CURVE ( 'NONE', #15149, #8047, #12912, .T. ) ;
#3267=CYLINDRICAL_SURFACE ( 'NONE', #19957, 44.99999999999999289 ) ;
#3268=VERTEX_POINT ( 'NONE', #6098 ) ;
#3269=DIRECTION ( 'NONE',  ( 0.000000000000000000, 0.000000000000000000, 1.000000000000000000 ) ) ;
#3271=VECTOR ( 'NONE', #7961, 1000.000000000000000 ) ;
#3272=AXIS2_PLACEMENT_3D ( 'NONE', #8505, #18357, #3535 ) ;
#3274=DIRECTION ( 'NONE',  ( 1.000000000000000000, 0.000000000000000000, 0.000000000000000000 ) ) ;
#3277=CARTESIAN_POINT ( 'NONE',  ( 10.00000000000000000, -68.36541360927154187, -50.60987712331774446 ) ) ;
#3280=ORIENTED_EDGE ( 'NONE', *, *, #12179, .F. ) ;
#3282=EDGE_CURVE ( 'NONE', #3214, #16126, #5883, .T. ) ;
#3285=AXIS2_PLACEMENT_3D ( 'NONE', #20220, #6755, #18574 ) ;
#3290=EDGE_CURVE ( 'NONE', #282, #21704, #809, .T. ) ;
#3293=LINE ( 'NONE', #18547, #10846 ) ;
#3294=DIRECTION ( 'NONE',  ( 1.000000000000000000, 0.000000000000000000, 0.000000000000000000 ) ) ;
#3295=VECTOR ( 'NONE', #10853, 1000.000000000000000 ) ;
#3296=CARTESIAN_POINT ( 'NONE',  ( 10.00000000000000000, 0.000000000000000000, 0.000000000000000000 ) ) ;
#3297=EDGE_CURVE ( 'NONE', #15150, #481, #20716, .T. ) ;
#3301=CIRCLE ( 'NONE', #5056, 92.50100000000000477 ) ;
#3305=ORIENTED_EDGE ( 'NONE', *, *, #20447, .F. ) ;
#3307=ORIENTED_EDGE ( 'NONE', *, *, #11063, .T. ) ;
#3308=ORIENTED_EDGE ( 'NONE', *, *, #20133, .T. ) ;
#3310=ORIENTED_EDGE ( 'NONE', *, *, #1774, .F. ) ;
#3312=DIRECTION ( 'NONE',  ( 0.000000000000000000, -0.2756373558170062132, 0.9612616959383166737 ) ) ;
#3313=EDGE_CURVE ( 'NONE', #282, #17660, #2778, .T. ) ;
#3314=CIRCLE ( 'NONE', #15657, 45.00000000000000711 ) ;
#3317=CARTESIAN_POINT ( 'NONE',  ( 10.00000000000000000, -78.01214607583727911, -33.90124636420193838 ) ) ;
#3318=DIRECTION ( 'NONE',  ( 0.000000000000000000, -0.6427876096865299260, -0.7660444431189857850 ) ) ;
#3322=CARTESIAN_POINT ( 'NONE',  ( 0.000000000000000000, 2.208823992045340301, -85.03123271466934341 ) ) ;
#3323=ORIENTED_EDGE ( 'NONE', *, *, #7840, .F. ) ;
#3324=VERTEX_POINT ( 'NONE', #7428 ) ;
#3325=DIRECTION ( 'NONE',  ( -1.000000000000000000, 0.000000000000000000, 0.000000000000000000 ) ) ;
#3326=VERTEX_POINT ( 'NONE', #2339 ) ;
#3327=CARTESIAN_POINT ( 'NONE',  ( 10.00000000000000000, -77.39385041987125646, -35.28996114464684553 ) ) ;
#3328=ORIENTED_EDGE ( 'NONE', *, *, #20629, .T. ) ;
#3333=ORIENTED_EDGE ( 'NONE', *, *, #16380, .T. ) ;
#3335=AXIS2_PLACEMENT_3D ( 'NONE', #21027, #10856, #12194 ) ;
#3336=FACE_OUTER_BOUND ( 'NONE', #7486, .T. ) ;
#3337=DIRECTION ( 'NONE',  ( -1.000000000000000000, 0.000000000000000000, -0.000000000000000000 ) ) ;
#3338=DIRECTION ( 'NONE',  ( -1.000000000000000000, 0.000000000000000000, 0.000000000000000000 ) ) ;
#3341=CARTESIAN_POINT ( 'NONE',  ( 5.000000000000002665, 23.62010150527335028, -84.77081340225880979 ) ) ;
#3342=FACE_OUTER_BOUND ( 'NONE', #504, .T. ) ;
#3343=CARTESIAN_POINT ( 'NONE',  ( 5.000000000000000000, 78.80192417387927151, 39.16958956249325752 ) ) ;
#3344=CIRCLE ( 'NONE', #17808, 45.00000000000000000 ) ;
#3346=ORIENTED_EDGE ( 'NONE', *, *, #3253, .T. ) ;
#3347=CIRCLE ( 'NONE', #9034, 44.99999999999999289 ) ;
#3348=AXIS2_PLACEMENT_3D ( 'NONE', #17343, #20645, #13278 ) ;
#3349=CARTESIAN_POINT ( 'NONE',  ( 5.000000000000000000, -61.60362715319078575, 62.84101464466223774 ) ) ;
#3350=CARTESIAN_POINT ( 'NONE',  ( 0.000000000000000000, -15.51843147776295950, -83.63233659819665888 ) ) ;
#3353=VERTEX_POINT ( 'NONE', #5999 ) ;
#3357=ADVANCED_FACE ( 'NONE', ( #5767 ), #4110, .F. ) ;
#3358=CIRCLE ( 'NONE', #3016, 44.99999999999999289 ) ;
#3360=ORIENTED_EDGE ( 'NONE', *, *, #21249, .T. ) ;
#3362=DIRECTION ( 'NONE',  ( 0.000000000000000000, -0.8290375725550469532, 0.5591929034707392443 ) ) ;
#3363=AXIS2_PLACEMENT_3D ( 'NONE', #9186, #4227, #12723 ) ;
#3364=ORIENTED_EDGE ( 'NONE', *, *, #14710, .T. ) ;
#3365=CIRCLE ( 'NONE', #2645, 44.99999999999998579 ) ;
#3370=CARTESIAN_POINT ( 'NONE',  ( 10.00000000000000000, 51.10509369859433804, 77.10190917907216601 ) ) ;
#3371=DIRECTION ( 'NONE',  ( 0.000000000000000000, 0.000000000000000000, 1.000000000000000000 ) ) ;
#3373=AXIS2_PLACEMENT_3D ( 'NONE', #14640, #14859, #4810 ) ;
#3376=EDGE_CURVE ( 'NONE', #17660, #12864, #1317, .T. ) ;
#3379=VECTOR ( 'NONE', #12607, 1000.000000000000000 ) ;
#3381=EDGE_CURVE ( 'NONE', #2483, #1347, #943, .T. ) ;
#3382=DIRECTION ( 'NONE',  ( 0.000000000000000000, -0.9848077530122062440, -0.1736481776669404620 ) ) ;
#3384=ORIENTED_EDGE ( 'NONE', *, *, #9576, .F. ) ;
#3388=DIRECTION ( 'NONE',  ( -1.000000000000000000, -0.000000000000000000, -0.000000000000000000 ) ) ;
#3389=ORIENTED_EDGE ( 'NONE', *, *, #12322, .F. ) ;
#3390=EDGE_CURVE ( 'NONE', #2869, #13770, #2709, .T. ) ;
#3392=EDGE_CURVE ( 'NONE', #16153, #2852, #4873, .T. ) ;
#3393=ORIENTED_EDGE ( 'NONE', *, *, #15717, .T. ) ;
#3394=EDGE_CURVE ( 'NONE', #12590, #9562, #7647, .T. ) ;
#3395=DIRECTION ( 'NONE',  ( 0.000000000000000000, 0.000000000000000000, 1.000000000000000000 ) ) ;
#3396=ORIENTED_EDGE ( 'NONE', *, *, #1122, .T. ) ;
#3397=DIRECTION ( 'NONE',  ( -1.000000000000000000, 0.000000000000000000, -0.000000000000000000 ) ) ;
#3398=EDGE_CURVE ( 'NONE', #15174, #1347, #16682, .T. ) ;
#3400=CARTESIAN_POINT ( 'NONE',  ( 0.000000000000000000, 51.10509369859540385, -77.10190917907144126 ) ) ;
#3403=CARTESIAN_POINT ( 'NONE',  ( 10.00000000000000000, 57.06999622551805373, 66.98518889142101784 ) ) ;
#3404=AXIS2_PLACEMENT_3D ( 'NONE', #21359, #19703, #14616 ) ;
#3405=AXIS2_PLACEMENT_3D ( 'NONE', #7930, #19756, #14784 ) ;
#3406=DIRECTION ( 'NONE',  ( 1.000000000000000000, -0.000000000000000000, -0.000000000000000000 ) ) ;
#3407=DIRECTION ( 'NONE',  ( -1.000000000000000000, -0.000000000000000000, -0.000000000000000000 ) ) ;
#3408=DIRECTION ( 'NONE',  ( 0.000000000000000000, 0.000000000000000000, 1.000000000000000000 ) ) ;
#3412=CARTESIAN_POINT ( 'NONE',  ( 0.000000000000000000, 3.974475837764924968, 92.41557521768191918 ) ) ;
#3415=ORIENTED_EDGE ( 'NONE', *, *, #331, .T. ) ;
#3416=CARTESIAN_POINT ( 'NONE',  ( 10.00000000000000000, -74.39348546125016526, -54.97312363261490731 ) ) ;
#3418=EDGE_CURVE ( 'NONE', #15453, #16302, #21057, .T. ) ;
#3420=VERTEX_POINT ( 'NONE', #15029 ) ;
#3423=EDGE_CURVE ( 'NONE', #19711, #18608, #11612, .T. ) ;
#3424=VERTEX_POINT ( 'NONE', #13369 ) ;
#3427=AXIS2_PLACEMENT_3D ( 'NONE', #10166, #13471, #6978 ) ;
#3430=CARTESIAN_POINT ( 'NONE',  ( 5.000000000000002665, -46.07110168784768689, -74.97635353408431058 ) ) ;
#3431=CARTESIAN_POINT ( 'NONE',  ( 10.00000000000000000, -31.15801000616779248, -79.14775961996421927 ) ) ;
#3432=VECTOR ( 'NONE', #7502, 1000.000000000000000 ) ;
#3433=CARTESIAN_POINT ( 'NONE',  ( 10.00000000000000000, 84.33453774737672859, -11.08490790852044405 ) ) ;
#3434=CYLINDRICAL_SURFACE ( 'NONE', #2785, 92.50100000000000477 ) ;
#3435=ORIENTED_EDGE ( 'NONE', *, *, #3394, .T. ) ;
#3436=ADVANCED_FACE ( 'NONE', ( #18364 ), #12929, .F. ) ;
#3437=DIRECTION ( 'NONE',  ( 0.000000000000000000, -0.1391731009600517543, -0.9902680687415721383 ) ) ;
#3441=CIRCLE ( 'NONE', #960, 92.50099999999999056 ) ;
#3442=DIRECTION ( 'NONE',  ( 0.000000000000000000, 0.000000000000000000, 1.000000000000000000 ) ) ;
#3444=AXIS2_PLACEMENT_3D ( 'NONE', #13651, #20402, #10650 ) ;
#3445=DIRECTION ( 'NONE',  ( -1.000000000000000000, -0.000000000000000000, -0.000000000000000000 ) ) ;
#3446=ORIENTED_EDGE ( 'NONE', *, *, #15120, .F. ) ;
#3447=ORIENTED_EDGE ( 'NONE', *, *, #2961, .F. ) ;
#3448=AXIS2_PLACEMENT_3D ( 'NONE', #16884, #18441, #5386 ) ;
#3451=ORIENTED_EDGE ( 'NONE', *, *, #20161, .T. ) ;
#3452=CARTESIAN_POINT ( 'NONE',  ( 10.00000000000000000, 74.74361964203228581, 40.60271866773572214 ) ) ;
#3455=CARTESIAN_POINT ( 'NONE',  ( 0.000000000000000000, 0.000000000000000000, 100.0000000000000000 ) ) ;
#3457=CARTESIAN_POINT ( 'NONE',  ( 10.00000000000000000, -23.10190250628894404, 89.56973317806591695 ) ) ;
#3459=AXIS2_PLACEMENT_3D ( 'NONE', #8314, #21785, #14829 ) ;
#3461=AXIS2_PLACEMENT_3D ( 'NONE', #19402, #1167, #7908 ) ;
#3462=ORIENTED_EDGE ( 'NONE', *, *, #11942, .T. ) ;
#3463=AXIS2_PLACEMENT_3D ( 'NONE', #4576, #20150, #6245 ) ;
#3465=CARTESIAN_POINT ( 'NONE',  ( 10.00000000000000000, 23.62010150527335028, -84.77081340225880979 ) ) ;
#3467=CARTESIAN_POINT ( 'NONE',  ( 10.00000000000000000, -9.646732466564730046, -84.51112348751858860 ) ) ;
#3470=CIRCLE ( 'NONE', #1359, 88.00000000000000000 ) ;
#3471=EDGE_LOOP ( 'NONE', ( #21241, #8326, #18674, #13746 ) ) ;
#3472=DIRECTION ( 'NONE',  ( 1.000000000000000000, 0.000000000000000000, 0.000000000000000000 ) ) ;
#3473=VERTEX_POINT ( 'NONE', #6328 ) ;
#3474=ORIENTED_EDGE ( 'NONE', *, *, #6090, .F. ) ;
#3475=CARTESIAN_POINT ( 'NONE',  ( 10.00000000000000000, 0.000000000000000000, 0.000000000000000000 ) ) ;
#3476=AXIS2_PLACEMENT_3D ( 'NONE', #13054, #13384, #21670 ) ;
#3477=DIRECTION ( 'NONE',  ( 0.000000000000000000, 0.000000000000000000, 1.000000000000000000 ) ) ;
#3478=AXIS2_PLACEMENT_3D ( 'NONE', #7429, #14259, #15822 ) ;
#3479=VERTEX_POINT ( 'NONE', #21657 ) ;
#3480=FACE_OUTER_BOUND ( 'NONE', #17737, .T. ) ;
#3481=DIRECTION ( 'NONE',  ( 0.000000000000000000, 0.000000000000000000, -1.000000000000000000 ) ) ;
#3482=DIRECTION ( 'NONE',  ( 0.000000000000000000, 0.000000000000000000, 1.000000000000000000 ) ) ;
#3485=FACE_OUTER_BOUND ( 'NONE', #20052, .T. ) ;
#3486=VERTEX_POINT ( 'NONE', #6210 ) ;
#3487=DIRECTION ( 'NONE',  ( -1.000000000000000000, -0.000000000000000000, 0.000000000000000000 ) ) ;
#3488=AXIS2_PLACEMENT_3D ( 'NONE', #7718, #11140, #17889 ) ;
#3489=CARTESIAN_POINT ( 'NONE',  ( 10.00000000000000000, 0.000000000000000000, 0.000000000000000000 ) ) ;
#3490=ADVANCED_FACE ( 'NONE', ( #9939 ), #4545, .F. ) ;
#3493=AXIS2_PLACEMENT_3D ( 'NONE', #18206, #11010, #5945 ) ;
#3499=EDGE_CURVE ( 'NONE', #9108, #13997, #4485, .T. ) ;
#3500=DIRECTION ( 'NONE',  ( 1.000000000000000000, 0.000000000000000000, 0.000000000000000000 ) ) ;
#3502=ORIENTED_EDGE ( 'NONE', *, *, #10695, .F. ) ;
#3503=DIRECTION ( 'NONE',  ( -1.000000000000000000, -0.000000000000000000, 0.000000000000000000 ) ) ;
#3504=ORIENTED_EDGE ( 'NONE', *, *, #2335, .T. ) ;
#3505=EDGE_CURVE ( 'NONE', #12778, #11100, #19788, .T. ) ;
#3506=DIRECTION ( 'NONE',  ( -1.000000000000000000, -0.000000000000000000, -0.000000000000000000 ) ) ;
#3507=VECTOR ( 'NONE', #13222, 1000.000000000000000 ) ;
#3508=CYLINDRICAL_SURFACE ( 'NONE', #7217, 92.50100000000000477 ) ;
#3510=CARTESIAN_POINT ( 'NONE',  ( 10.00000000000000000, 5.479102470011647519, -87.82926298292107958 ) ) ;
#3511=CIRCLE ( 'NONE', #21510, 92.50100000000000477 ) ;
#3512=AXIS2_PLACEMENT_3D ( 'NONE', #19768, #4630, #18108 ) ;
#3513=DIRECTION ( 'NONE',  ( -1.000000000000000000, 0.000000000000000000, -0.000000000000000000 ) ) ;
#3514=CYLINDRICAL_SURFACE ( 'NONE', #2733, 88.00000000000000000 ) ;
#3516=DIRECTION ( 'NONE',  ( 0.000000000000000000, 0.000000000000000000, 1.000000000000000000 ) ) ;
#3518=EDGE_CURVE ( 'NONE', #16436, #15664, #16478, .T. ) ;
#3522=VERTEX_POINT ( 'NONE', #10052 ) ;
#3523=EDGE_CURVE ( 'NONE', #5168, #14060, #12236, .T. ) ;
#3524=CARTESIAN_POINT ( 'NONE',  ( -10.00000000000000000, 0.000000000000000000, 0.000000000000000000 ) ) ;
#3525=VERTEX_POINT ( 'NONE', #16354 ) ;
#3526=AXIS2_PLACEMENT_3D ( 'NONE', #3896, #14059, #10301 ) ;
#3528=CIRCLE ( 'NONE', #6364, 88.00000000000000000 ) ;
#3531=ORIENTED_EDGE ( 'NONE', *, *, #19424, .T. ) ;
#3532=EDGE_CURVE ( 'NONE', #9814, #16595, #16118, .T. ) ;
#3533=CARTESIAN_POINT ( 'NONE',  ( 10.00000000000000000, -82.02147376274642454, -42.76579056660944644 ) ) ;
#3534=ORIENTED_EDGE ( 'NONE', *, *, #7952, .F. ) ;
#3535=DIRECTION ( 'NONE',  ( 0.000000000000000000, 0.000000000000000000, -1.000000000000000000 ) ) ;
#3538=CYLINDRICAL_SURFACE ( 'NONE', #7512, 44.99999999999999289 ) ;
#3543=DIRECTION ( 'NONE',  ( 0.000000000000000000, 0.000000000000000000, 1.000000000000000000 ) ) ;
#3544=VERTEX_POINT ( 'NONE', #13705 ) ;
#3545=DIRECTION ( 'NONE',  ( 0.000000000000000000, -0.9993908270190959842, 0.03489949670249112984 ) ) ;
#3552=CARTESIAN_POINT ( 'NONE',  ( 10.00000000000000000, -81.32027326007897727, 44.08455690949027428 ) ) ;
#3554=ORIENTED_EDGE ( 'NONE', *, *, #14704, .F. ) ;
#3557=CARTESIAN_POINT ( 'NONE',  ( 0.000000000000000000, 87.44637528609661103, 9.855528870798920593 ) ) ;
#3559=EDGE_CURVE ( 'NONE', #17337, #1046, #15403, .T. ) ;
#3560=CARTESIAN_POINT ( 'NONE',  ( 10.00000000000000000, 87.58454185039441597, 8.540961822681984117 ) ) ;
#3561=DIRECTION ( 'NONE',  ( -1.000000000000000000, -0.000000000000000000, 0.000000000000000000 ) ) ;
#3562=CYLINDRICAL_SURFACE ( 'NONE', #11415, 44.99999999999999289 ) ;
#3563=AXIS2_PLACEMENT_3D ( 'NONE', #18629, #16637, #4934 ) ;
#3564=DIRECTION ( 'NONE',  ( -1.000000000000000000, 0.000000000000000000, 0.000000000000000000 ) ) ;
#3565=EDGE_CURVE ( 'NONE', #4256, #19013, #6972, .T. ) ;
#3566=EDGE_CURVE ( 'NONE', #17521, #12476, #11939, .T. ) ;
#3571=ORIENTED_EDGE ( 'NONE', *, *, #5967, .F. ) ;
#3573=CYLINDRICAL_SURFACE ( 'NONE', #17647, 44.99999999999998579 ) ;
#3574=ORIENTED_EDGE ( 'NONE', *, *, #17274, .T. ) ;
#3576=ORIENTED_EDGE ( 'NONE', *, *, #21090, .T. ) ;
#3577=ORIENTED_EDGE ( 'NONE', *, *, #4325, .F. ) ;
#3578=DIRECTION ( 'NONE',  ( 0.000000000000000000, -0.8987940462991711454, 0.4383711467890689661 ) ) ;
#3580=ORIENTED_EDGE ( 'NONE', *, *, #133, .F. ) ;
#3581=VERTEX_POINT ( 'NONE', #18690 ) ;
#3583=DIRECTION ( 'NONE',  ( 0.000000000000000000, -0.7431448254773861395, -0.6691306063588670083 ) ) ;
#3584=DIRECTION ( 'NONE',  ( 1.000000000000000000, 0.000000000000000000, 0.000000000000000000 ) ) ;
#3587=CARTESIAN_POINT ( 'NONE',  ( 10.00000000000000000, -37.96946988134224910, 76.11510229470846411 ) ) ;
#3589=DIRECTION ( 'NONE',  ( 0.000000000000000000, 0.4694715627858855322, 0.8829475928589297640 ) ) ;
#3590=CARTESIAN_POINT ( 'NONE',  ( 10.00000000000000000, 0.000000000000000000, 0.000000000000000000 ) ) ;
#3592=FACE_OUTER_BOUND ( 'NONE', #449, .T. ) ;
#3597=CARTESIAN_POINT ( 'NONE',  ( 10.00000000000000000, -79.66702613806754130, -29.80527447819517661 ) ) ;
#3598=FACE_OUTER_BOUND ( 'NONE', #15071, .T. ) ;
#3599=VERTEX_POINT ( 'NONE', #6759 ) ;
#3600=ORIENTED_EDGE ( 'NONE', *, *, #10002, .F. ) ;
#3601=ORIENTED_EDGE ( 'NONE', *, *, #11119, .F. ) ;
#3605=DIRECTION ( 'NONE',  ( -1.000000000000000000, 0.000000000000000000, -0.000000000000000000 ) ) ;
#3606=FACE_OUTER_BOUND ( 'NONE', #14526, .T. ) ;
#3608=EDGE_CURVE ( 'NONE', #14246, #15239, #18788, .T. ) ;
#3609=CARTESIAN_POINT ( 'NONE',  ( 10.00000000000000000, -3.728035544475628793, -84.97818067823773447 ) ) ;
#3610=CARTESIAN_POINT ( 'NONE',  ( 10.00000000000000000, -67.05625154133410604, -63.71729851637880415 ) ) ;
#3611=CARTESIAN_POINT ( 'NONE',  ( 10.00000000000000000, -90.32141448704669529, -19.96189084378313794 ) ) ;
#3613=CYLINDRICAL_SURFACE ( 'NONE', #1148, 44.99999999999999289 ) ;
#3614=ORIENTED_EDGE ( 'NONE', *, *, #3297, .T. ) ;
#3615=EDGE_CURVE ( 'NONE', #13385, #17227, #7311, .T. ) ;
#3618=CARTESIAN_POINT ( 'NONE',  ( 10.00000000000000000, 86.66425444033919234, 32.33793443156426406 ) ) ;
#3619=AXIS2_PLACEMENT_3D ( 'NONE', #15109, #3407, #16885 ) ;
#3622=CARTESIAN_POINT ( 'NONE',  ( 10.00000000000000000, -84.33453774737651543, -11.08490790852216534 ) ) ;
#3623=ORIENTED_EDGE ( 'NONE', *, *, #20532, .F. ) ;
#3624=DIRECTION ( 'NONE',  ( 1.000000000000000000, 0.000000000000000000, 0.000000000000000000 ) ) ;
#3625=ORIENTED_EDGE ( 'NONE', *, *, #10450, .F. ) ;
#3626=AXIS2_PLACEMENT_3D ( 'NONE', #13701, #15784, #10697 ) ;
#3627=ORIENTED_EDGE ( 'NONE', *, *, #19984, .F. ) ;
#3630=CIRCLE ( 'NONE', #8222, 88.00000000000000000 ) ;
#3633=CARTESIAN_POINT ( 'NONE',  ( 0.000000000000000000, 0.000000000000000000, 0.000000000000000000 ) ) ;
#3635=ADVANCED_FACE ( 'NONE', ( #13 ), #5418, .F. ) ;
#3637=DIRECTION ( 'NONE',  ( 1.000000000000000000, 0.000000000000000000, 0.000000000000000000 ) ) ;
#3638=CARTESIAN_POINT ( 'NONE',  ( 0.000000000000000000, -92.49798535263880694, 0.7467976319017535225 ) ) ;
#3640=DIRECTION ( 'NONE',  ( -1.000000000000000000, 0.000000000000000000, 0.000000000000000000 ) ) ;
#3641=DIRECTION ( 'NONE',  ( 0.000000000000000000, 0.000000000000000000, 1.000000000000000000 ) ) ;
#3643=EDGE_LOOP ( 'NONE', ( #20257, #12651, #11816, #19041 ) ) ;
#3644=CARTESIAN_POINT ( 'NONE',  ( 10.00000000000000000, -35.34277389771474986, -85.48288328206420772 ) ) ;
#3647=ORIENTED_EDGE ( 'NONE', *, *, #21065, .F. ) ;
#3648=VECTOR ( 'NONE', #1130, 1000.000000000000000 ) ;
#3649=EDGE_LOOP ( 'NONE', ( #12915, #6031, #12301, #821 ) ) ;
#3651=DIRECTION ( 'NONE',  ( 1.000000000000000000, 0.000000000000000000, 0.000000000000000000 ) ) ;
#3652=ORIENTED_EDGE ( 'NONE', *, *, #5534, .T. ) ;
#3653=ORIENTED_EDGE ( 'NONE', *, *, #11912, .F. ) ;
#3654=DIRECTION ( 'NONE',  ( 1.000000000000000000, 0.000000000000000000, 0.000000000000000000 ) ) ;
#3655=AXIS2_PLACEMENT_3D ( 'NONE', #7264, #15644, #20424 ) ;
#3656=EDGE_CURVE ( 'NONE', #21588, #2240, #21421, .T. ) ;
#3659=ADVANCED_FACE ( 'NONE', ( #11826 ), #18578, .F. ) ;
#3660=DIRECTION ( 'NONE',  ( 1.000000000000000000, 0.000000000000000000, 0.000000000000000000 ) ) ;
#3662=ADVANCED_FACE ( 'NONE', ( #10811 ), #15791, .F. ) ;
#3663=CARTESIAN_POINT ( 'NONE',  ( 10.00000000000000000, -92.32475887865419395, -5.707354816231494432 ) ) ;
#3665=DIRECTION ( 'NONE',  ( -1.000000000000000000, 0.000000000000000000, 0.000000000000000000 ) ) ;
#3668=DIRECTION ( 'NONE',  ( 1.000000000000000000, 0.000000000000000000, 0.000000000000000000 ) ) ;
#3669=CARTESIAN_POINT ( 'NONE',  ( 10.00000000000000000, 0.000000000000000000, 0.000000000000000000 ) ) ;
#3671=EDGE_CURVE ( 'NONE', #6675, #9108, #2311, .T. ) ;
#3672=AXIS2_PLACEMENT_3D ( 'NONE', #19832, #19733, #3048 ) ;
#3673=EDGE_CURVE ( 'NONE', #10178, #21331, #18965, .T. ) ;
#3674=CARTESIAN_POINT ( 'NONE',  ( 0.000000000000000000, 78.83848282823907994, 48.38314403117527718 ) ) ;
#3675=CIRCLE ( 'NONE', #10377, 44.99999999999999289 ) ;
#3676=DIRECTION ( 'NONE',  ( -1.000000000000000000, -0.000000000000000000, 0.000000000000000000 ) ) ;
#3677=EDGE_LOOP ( 'NONE', ( #18265, #3534, #11480, #2970 ) ) ;
#3679=ORIENTED_EDGE ( 'NONE', *, *, #16912, .F. ) ;
#3680=CIRCLE ( 'NONE', #15683, 92.50100000000000477 ) ;
#3681=EDGE_CURVE ( 'NONE', #419, #14686, #7505, .T. ) ;
#3682=VERTEX_POINT ( 'NONE', #16116 ) ;
#3683=CARTESIAN_POINT ( 'NONE',  ( 10.00000000000000000, 0.000000000000000000, 0.000000000000000000 ) ) ;
#3684=EDGE_LOOP ( 'NONE', ( #21184, #12645, #131, #12882 ) ) ;
#3685=ORIENTED_EDGE ( 'NONE', *, *, #11267, .F. ) ;
#3687=FACE_OUTER_BOUND ( 'NONE', #8467, .T. ) ;
#3688=CIRCLE ( 'NONE', #15690, 92.50100000000001899 ) ;
#3689=EDGE_CURVE ( 'NONE', #15117, #3028, #17909, .T. ) ;
#3692=CIRCLE ( 'NONE', #14263, 45.00000000000000711 ) ;
#3693=CARTESIAN_POINT ( 'NONE',  ( 0.000000000000000000, -32.56745702629792305, 78.57830605990643846 ) ) ;
#3695=DIRECTION ( 'NONE',  ( 0.000000000000000000, 0.000000000000000000, 1.000000000000000000 ) ) ;
#3696=CARTESIAN_POINT ( 'NONE',  ( 5.000000000000000000, -69.74988376403980794, -53.65588238863408321 ) ) ;
#3698=ORIENTED_EDGE ( 'NONE', *, *, #16892, .T. ) ;
#3700=EDGE_LOOP ( 'NONE', ( #4972, #4505, #15095, #8829 ) ) ;
#3701=EDGE_CURVE ( 'NONE', #15534, #12050, #5857, .T. ) ;
#3702=DIRECTION ( 'NONE',  ( 0.000000000000000000, -0.9702957262759939194, -0.2419218955996776110 ) ) ;
#3704=VECTOR ( 'NONE', #9367, 1000.000000000000000 ) ;
#3705=CARTESIAN_POINT ( 'NONE',  ( 0.000000000000000000, -78.83848282823873888, -48.38314403117582430 ) ) ;
#3706=CIRCLE ( 'NONE', #8302, 45.00000000000000000 ) ;
#3707=DIRECTION ( 'NONE',  ( 1.000000000000000000, 0.000000000000000000, 0.000000000000000000 ) ) ;
#3709=AXIS2_PLACEMENT_3D ( 'NONE', #13670, #198, #12226 ) ;
#3710=EDGE_CURVE ( 'NONE', #14716, #935, #14237, .T. ) ;
#3711=( NAMED_UNIT ( * ) PLANE_ANGLE_UNIT ( ) SI_UNIT ( $, .RADIAN. ) );
#3712=CIRCLE ( 'NONE', #9343, 92.50100000000000477 ) ;
#3713=ORIENTED_EDGE ( 'NONE', *, *, #4161, .F. ) ;
#3714=ORIENTED_EDGE ( 'NONE', *, *, #11129, .T. ) ;
#3717=AXIS2_PLACEMENT_3D ( 'NONE', #8373, #10456, #16986 ) ;
#3719=FACE_OUTER_BOUND ( 'NONE', #8769, .T. ) ;
#3720=CARTESIAN_POINT ( 'NONE',  ( 10.00000000000000000, -81.55207211302061410, -24.17537951050148592 ) ) ;
#3721=DIRECTION ( 'NONE',  ( 1.000000000000000000, -0.000000000000000000, 0.000000000000000000 ) ) ;
#3722=FACE_OUTER_BOUND ( 'NONE', #2898, .T. ) ;
#3724=CARTESIAN_POINT ( 'NONE',  ( 10.00000000000000000, -41.87002153499162915, 74.04114219178029543 ) ) ;
#3727=AXIS2_PLACEMENT_3D ( 'NONE', #2786, #17807, #2885 ) ;
#3729=CIRCLE ( 'NONE', #543, 92.50099999999999056 ) ;
#3730=VERTEX_POINT ( 'NONE', #20985 ) ;
#3731=AXIS2_PLACEMENT_3D ( 'NONE', #3047, #13311, #21392 ) ;
#3732=CYLINDRICAL_SURFACE ( 'NONE', #19740, 44.99999999999998579 ) ;
#3733=VECTOR ( 'NONE', #7493, 1000.000000000000000 ) ;
#3736=DIRECTION ( 'NONE',  ( -1.000000000000000000, -0.000000000000000000, -0.000000000000000000 ) ) ;
#3737=ORIENTED_EDGE ( 'NONE', *, *, #17458, .F. ) ;
#3738=CARTESIAN_POINT ( 'NONE',  ( 0.000000000000000000, 35.18804927320529430, 80.65854690202691302 ) ) ;
#3740=DIRECTION ( 'NONE',  ( 0.000000000000000000, 0.000000000000000000, 1.000000000000000000 ) ) ;
#3743=AXIS2_PLACEMENT_3D ( 'NONE', #6438, #1448, #1780 ) ;
#3744=CIRCLE ( 'NONE', #11153, 88.00000000000000000 ) ;
#3746=CIRCLE ( 'NONE', #6895, 92.50100000000003320 ) ;
#3748=DIRECTION ( 'NONE',  ( 1.000000000000000000, 0.000000000000000000, 0.000000000000000000 ) ) ;
#3749=CARTESIAN_POINT ( 'NONE',  ( 10.00000000000000000, -92.49798535263880694, 0.7467976319017460840 ) ) ;
#3750=CARTESIAN_POINT ( 'NONE',  ( 0.000000000000000000, 64.95266917914399585, -59.37298010462904330 ) ) ;
#3751=DIRECTION ( 'NONE',  ( -1.000000000000000000, 0.000000000000000000, 0.000000000000000000 ) ) ;
#3752=DIRECTION ( 'NONE',  ( 1.000000000000000000, 0.000000000000000000, -0.000000000000000000 ) ) ;
#3755=DIRECTION ( 'NONE',  ( -1.000000000000000000, 0.000000000000000000, -0.000000000000000000 ) ) ;
#3756=AXIS2_PLACEMENT_3D ( 'NONE', #5971, #17784, #9370 ) ;
#3757=ORIENTED_EDGE ( 'NONE', *, *, #7331, .T. ) ;
#3759=CARTESIAN_POINT ( 'NONE',  ( 0.000000000000000000, 46.07110168784820559, 74.97635353408399794 ) ) ;
#3760=EDGE_LOOP ( 'NONE', ( #9907, #5309, #17574, #7653 ) ) ;
#3762=ORIENTED_EDGE ( 'NONE', *, *, #21240, .T. ) ;
#3763=ORIENTED_EDGE ( 'NONE', *, *, #18395, .F. ) ;
#3764=FACE_OUTER_BOUND ( 'NONE', #13632, .T. ) ;
#3765=ORIENTED_EDGE ( 'NONE', *, *, #3940, .T. ) ;
#3766=ORIENTED_EDGE ( 'NONE', *, *, #20288, .T. ) ;
#3768=FACE_OUTER_BOUND ( 'NONE', #3181, .T. ) ;
#3772=VECTOR ( 'NONE', #11024, 1000.000000000000000 ) ;
#3773=DIRECTION ( 'NONE',  ( 0.000000000000000000, -0.3420201433256569445, -0.9396926207859126468 ) ) ;
#3775=DIRECTION ( 'NONE',  ( -1.000000000000000000, -0.000000000000000000, 0.000000000000000000 ) ) ;
#3777=CARTESIAN_POINT ( 'NONE',  ( 5.000000000000002665, 18.94217447942673971, -85.93715160505934136 ) ) ;
#3778=CARTESIAN_POINT ( 'NONE',  ( 10.00000000000000000, -3.728035544476815399, 84.97818067823770605 ) ) ;
#3779=DIRECTION ( 'NONE',  ( 0.000000000000000000, 0.000000000000000000, -1.000000000000000000 ) ) ;
#3780=DIRECTION ( 'NONE',  ( 0.000000000000000000, 8.943463253924873884E-15, -1.000000000000000000 ) ) ;
#3781=ORIENTED_EDGE ( 'NONE', *, *, #20367, .T. ) ;
#3785=AXIS2_PLACEMENT_3D ( 'NONE', #4272, #2725, #7919 ) ;
#3786=ADVANCED_FACE ( 'NONE', ( #4292 ), #3970, .F. ) ;
#3787=AXIS2_PLACEMENT_3D ( 'NONE', #14561, #19864, #12907 ) ;
#3789=ADVANCED_FACE ( 'NONE', ( #15678 ), #7616, .F. ) ;
#3790=DIRECTION ( 'NONE',  ( 0.000000000000000000, 0.000000000000000000, 1.000000000000000000 ) ) ;
#3792=CARTESIAN_POINT ( 'NONE',  ( 10.00000000000000000, -36.60317927562525853, -76.78148674856802813 ) ) ;
#3793=EDGE_LOOP ( 'NONE', ( #6220, #9218, #19397, #10336 ) ) ;
#3794=CARTESIAN_POINT ( 'NONE',  ( 0.000000000000000000, 0.000000000000000000, 0.000000000000000000 ) ) ;
#3795=VERTEX_POINT ( 'NONE', #7404 ) ;
#3801=CARTESIAN_POINT ( 'NONE',  ( 5.000000000000002665, -85.54350296776095774, -20.64725405482940346 ) ) ;
#3802=CYLINDRICAL_SURFACE ( 'NONE', #5187, 45.00000000000000000 ) ;
#3804=DIRECTION ( 'NONE',  ( 1.000000000000000000, 0.000000000000000000, 0.000000000000000000 ) ) ;
#3805=CIRCLE ( 'NONE', #16147, 88.00000000000000000 ) ;
#3806=LINE ( 'NONE', #3370, #5099 ) ;
#3807=AXIS2_PLACEMENT_3D ( 'NONE', #9414, #17514, #1040 ) ;
#3809=EDGE_CURVE ( 'NONE', #15239, #8355, #4849, .T. ) ;
#3811=VERTEX_POINT ( 'NONE', #16332 ) ;
#3812=AXIS2_PLACEMENT_3D ( 'NONE', #5224, #11962, #13829 ) ;
#3813=DIRECTION ( 'NONE',  ( -1.000000000000000000, -0.000000000000000000, -0.000000000000000000 ) ) ;
#3814=ORIENTED_EDGE ( 'NONE', *, *, #14224, .F. ) ;
#3815=DIRECTION ( 'NONE',  ( 0.000000000000000000, -0.7431448254773861395, -0.6691306063588671194 ) ) ;
#3816=EDGE_LOOP ( 'NONE', ( #15457, #471, #2459, #20302 ) ) ;
#3817=CIRCLE ( 'NONE', #5589, 88.00000000000000000 ) ;
#3819=CARTESIAN_POINT ( 'NONE',  ( 5.000000000000000000, -64.95266917914358373, 59.37298010462950515 ) ) ;
#3820=AXIS2_PLACEMENT_3D ( 'NONE', #8008, #9754, #9968 ) ;
#3821=AXIS2_PLACEMENT_3D ( 'NONE', #8279, #6745, #1973 ) ;
#3823=AXIS2_PLACEMENT_3D ( 'NONE', #11940, #15238, #113 ) ;
#3825=ORIENTED_EDGE ( 'NONE', *, *, #9183, .F. ) ;
#3828=CARTESIAN_POINT ( 'NONE',  ( 10.00000000000000000, 0.000000000000000000, 0.000000000000000000 ) ) ;
#3830=EDGE_CURVE ( 'NONE', #286, #7680, #20021, .T. ) ;
#3831=DIRECTION ( 'NONE',  ( 1.000000000000000000, 0.000000000000000000, 0.000000000000000000 ) ) ;
#3832=CARTESIAN_POINT ( 'NONE',  ( 10.00000000000000000, -51.10509369859380513, -77.10190917907254970 ) ) ;
#3833=CARTESIAN_POINT ( 'NONE',  ( 10.00000000000000000, 67.05625154133453236, 63.71729851637834940 ) ) ;
#3834=EDGE_CURVE ( 'NONE', #7150, #14716, #10139, .T. ) ;
#3836=DIRECTION ( 'NONE',  ( 0.000000000000000000, 0.000000000000000000, -1.000000000000000000 ) ) ;
#3838=AXIS2_PLACEMENT_3D ( 'NONE', #12611, #19360, #7976 ) ;
#3840=EDGE_CURVE ( 'NONE', #12932, #173, #614, .T. ) ;
#3843=AXIS2_PLACEMENT_3D ( 'NONE', #7506, #16001, #4195 ) ;
#3844=EDGE_CURVE ( 'NONE', #17747, #14422, #7942, .T. ) ;
#3845=DIRECTION ( 'NONE',  ( 1.000000000000000000, 0.000000000000000000, 0.000000000000000000 ) ) ;
#3846=DIRECTION ( 'NONE',  ( -1.000000000000000000, -0.000000000000000000, -0.000000000000000000 ) ) ;
#3847=LINE ( 'NONE', #7158, #8716 ) ;
#3849=LINE ( 'NONE', #7387, #2782 ) ;
#3850=ORIENTED_EDGE ( 'NONE', *, *, #567, .T. ) ;
#3851=CARTESIAN_POINT ( 'NONE',  ( 0.000000000000000000, -68.93609746931198856, 54.69748134696436637 ) ) ;
#3853=ORIENTED_EDGE ( 'NONE', *, *, #5147, .F. ) ;
#3854=CIRCLE ( 'NONE', #5975, 44.99999999999999289 ) ;
#3856=DIRECTION ( 'NONE',  ( 0.000000000000000000, 0.000000000000000000, 1.000000000000000000 ) ) ;
#3858=CYLINDRICAL_SURFACE ( 'NONE', #17247, 44.99999999999999289 ) ;
#3860=DIRECTION ( 'NONE',  ( 0.000000000000000000, -0.9271838545667832054, -0.3746065934159226729 ) ) ;
#3863=DIRECTION ( 'NONE',  ( -1.000000000000000000, 0.000000000000000000, 0.000000000000000000 ) ) ;
#3864=CARTESIAN_POINT ( 'NONE',  ( 10.00000000000000000, 0.000000000000000000, 0.000000000000000000 ) ) ;
#3869=AXIS2_PLACEMENT_3D ( 'NONE', #13165, #15051, #9856 ) ;
#3871=ORIENTED_EDGE ( 'NONE', *, *, #3253, .F. ) ;
#3873=CARTESIAN_POINT ( 'NONE',  ( 0.000000000000000000, 91.70173545986517638, 12.13370160540072007 ) ) ;
#3874=VERTEX_POINT ( 'NONE', #13023 ) ;
#3876=VERTEX_POINT ( 'NONE', #4731 ) ;
#3877=LINE ( 'NONE', #10609, #10611 ) ;
#3878=ORIENTED_EDGE ( 'NONE', *, *, #16757, .T. ) ;
#3880=CARTESIAN_POINT ( 'NONE',  ( 10.00000000000000000, 0.000000000000000000, 0.000000000000000000 ) ) ;
#3881=VERTEX_POINT ( 'NONE', #6185 ) ;
#3882=CIRCLE ( 'NONE', #6730, 92.50100000000000477 ) ;
#3886=DIRECTION ( 'NONE',  ( 0.000000000000000000, 0.000000000000000000, 1.000000000000000000 ) ) ;
#3887=EDGE_CURVE ( 'NONE', #18262, #20717, #7328, .T. ) ;
#3891=CARTESIAN_POINT ( 'NONE',  ( 10.00000000000000000, 84.33453774737657227, 11.08490790852157559 ) ) ;
#3893=EDGE_CURVE ( 'NONE', #14902, #13159, #4148, .T. ) ;
#3895=DIRECTION ( 'NONE',  ( 0.000000000000000000, 0.000000000000000000, 1.000000000000000000 ) ) ;
#3896=CARTESIAN_POINT ( 'NONE',  ( 0.000000000000000000, 0.000000000000000000, 0.000000000000000000 ) ) ;
#3897=ORIENTED_EDGE ( 'NONE', *, *, #20464, .F. ) ;
#3898=CARTESIAN_POINT ( 'NONE',  ( 10.00000000000000000, 84.90234713953985590, 5.175025661884123274 ) ) ;
#3901=DIRECTION ( 'NONE',  ( -1.000000000000000000, 0.000000000000000000, 0.000000000000000000 ) ) ;
#3902=ORIENTED_EDGE ( 'NONE', *, *, #3947, .F. ) ;
#3903=ORIENTED_EDGE ( 'NONE', *, *, #16774, .F. ) ;
#3904=CARTESIAN_POINT ( 'NONE',  ( 0.000000000000000000, 0.000000000000000000, 0.000000000000000000 ) ) ;
#3905=CARTESIAN_POINT ( 'NONE',  ( 10.00000000000000000, -82.02147376274702140, 42.76579056660835221 ) ) ;
#3906=DIRECTION ( 'NONE',  ( 0.000000000000000000, 0.000000000000000000, 1.000000000000000000 ) ) ;
#3908=EDGE_CURVE ( 'NONE', #3086, #11509, #16503, .T. ) ;
#3909=ADVANCED_FACE ( 'NONE', ( #9806 ), #16563, .F. ) ;
#3910=DIRECTION ( 'NONE',  ( 0.000000000000000000, 0.000000000000000000, 1.000000000000000000 ) ) ;
#3911=EDGE_CURVE ( 'NONE', #16436, #1002, #10484, .T. ) ;
#3912=CIRCLE ( 'NONE', #730, 44.99999999999998579 ) ;
#3913=DIRECTION ( 'NONE',  ( -1.000000000000000000, -0.000000000000000000, -0.000000000000000000 ) ) ;
#3914=DIRECTION ( 'NONE',  ( 0.000000000000000000, 0.000000000000000000, 1.000000000000000000 ) ) ;
#3916=EDGE_CURVE ( 'NONE', #6987, #20717, #7829, .T. ) ;
#3918=CARTESIAN_POINT ( 'NONE',  ( 10.00000000000000000, 48.19312842678472464, 70.09002648625214249 ) ) ;
#3919=ORIENTED_EDGE ( 'NONE', *, *, #7740, .T. ) ;
#3920=EDGE_CURVE ( 'NONE', #14961, #4926, #3441, .T. ) ;
#3926=DIRECTION ( 'NONE',  ( -1.000000000000000000, -0.000000000000000000, -0.000000000000000000 ) ) ;
#3927=ORIENTED_EDGE ( 'NONE', *, *, #12529, .F. ) ;
#3929=ORIENTED_EDGE ( 'NONE', *, *, #9598, .T. ) ;
#3930=ORIENTED_EDGE ( 'NONE', *, *, #8929, .F. ) ;
#3932=CARTESIAN_POINT ( 'NONE',  ( 10.00000000000000000, 70.37753541436022431, -60.02863908169562279 ) ) ;
#3936=DIRECTION ( 'NONE',  ( 0.000000000000000000, 0.9993908270190957621, -0.03489949670249752750 ) ) ;
#3937=EDGE_CURVE ( 'NONE', #14715, #2438, #1329, .T. ) ;
#3938=FACE_OUTER_BOUND ( 'NONE', #3816, .T. ) ;
#3940=EDGE_CURVE ( 'NONE', #21516, #19466, #829, .T. ) ;
#3941=CYLINDRICAL_SURFACE ( 'NONE', #5393, 44.99999999999999289 ) ;
#3943=EDGE_LOOP ( 'NONE', ( #2513, #71, #17681, #8299 ) ) ;
#3944=CARTESIAN_POINT ( 'NONE',  ( 0.000000000000000000, 51.18896083639267403, 71.57995730992199412 ) ) ;
#3945=DIRECTION ( 'NONE',  ( -1.000000000000000000, -0.000000000000000000, -0.000000000000000000 ) ) ;
#3947=EDGE_CURVE ( 'NONE', #17904, #17373, #269, .T. ) ;
#3948=ORIENTED_EDGE ( 'NONE', *, *, #10439, .T. ) ;
#3949=CARTESIAN_POINT ( 'NONE',  ( 0.000000000000000000, 73.32282170386848463, 48.65967342042804944 ) ) ;
#3950=ORIENTED_EDGE ( 'NONE', *, *, #18037, .F. ) ;
#3954=ORIENTED_EDGE ( 'NONE', *, *, #4350, .F. ) ;
#3955=ORIENTED_EDGE ( 'NONE', *, *, #8246, .F. ) ;
#3958=EDGE_CURVE ( 'NONE', #7513, #2166, #6984, .T. ) ;
#3959=ORIENTED_EDGE ( 'NONE', *, *, #10613, .F. ) ;
#3961=CARTESIAN_POINT ( 'NONE',  ( 5.000000000000002665, -0.6609040254617754018, 87.99751818016873983 ) ) ;
#3963=DIRECTION ( 'NONE',  ( 0.000000000000000000, 0.000000000000000000, 1.000000000000000000 ) ) ;
#3964=AXIS2_PLACEMENT_3D ( 'NONE', #10312, #18942, #18506 ) ;
#3966=EDGE_CURVE ( 'NONE', #10355, #21543, #630, .T. ) ;
#3968=CARTESIAN_POINT ( 'NONE',  ( 5.000000000000000000, 61.60362715319035942, 62.84101464466265696 ) ) ;
#3969=CIRCLE ( 'NONE', #17395, 44.99999999999999289 ) ;
#3970=CYLINDRICAL_SURFACE ( 'NONE', #21071, 88.00000000000000000 ) ;
#3972=ORIENTED_EDGE ( 'NONE', *, *, #17562, .F. ) ;
#3974=ORIENTED_EDGE ( 'NONE', *, *, #8383, .F. ) ;
#3976=VERTEX_POINT ( 'NONE', #17857 ) ;
#3977=ORIENTED_EDGE ( 'NONE', *, *, #14096, .T. ) ;
#3978=CARTESIAN_POINT ( 'NONE',  ( 0.000000000000000000, -74.39348546125087580, 54.97312363261390544 ) ) ;
#3979=EDGE_LOOP ( 'NONE', ( #16898, #19968, #21454, #19203 ) ) ;
#3981=CIRCLE ( 'NONE', #5756, 92.50100000000000477 ) ;
#3982=EDGE_CURVE ( 'NONE', #10882, #8096, #11210, .T. ) ;
#3983=DIRECTION ( 'NONE',  ( 1.000000000000000000, 0.000000000000000000, 0.000000000000000000 ) ) ;
#3984=CIRCLE ( 'NONE', #5050, 92.50100000000000477 ) ;
#3985=ORIENTED_EDGE ( 'NONE', *, *, #2455, .T. ) ;
#3986=LINE ( 'NONE', #12595, #11818 ) ;
#3987=FACE_OUTER_BOUND ( 'NONE', #10743, .T. ) ;
#3990=CARTESIAN_POINT ( 'NONE',  ( 0.000000000000000000, 0.000000000000000000, 0.000000000000000000 ) ) ;
#3991=DIRECTION ( 'NONE',  ( 1.000000000000000000, 0.000000000000000000, 0.000000000000000000 ) ) ;
#3992=CARTESIAN_POINT ( 'NONE',  ( 10.00000000000000000, -46.93287725819731548, -70.94007663282492615 ) ) ;
#3993=CARTESIAN_POINT ( 'NONE',  ( 10.00000000000000000, 0.000000000000000000, 0.000000000000000000 ) ) ;
#3995=ORIENTED_EDGE ( 'NONE', *, *, #20133, .F. ) ;
#3996=VECTOR ( 'NONE', #15935, 1000.000000000000000 ) ;
#3997=LINE ( 'NONE', #14261, #19976 ) ;
#3998=CIRCLE ( 'NONE', #12820, 44.99999999999998579 ) ;
#4001=CIRCLE ( 'NONE', #6846, 88.00000000000000000 ) ;
#4004=DIRECTION ( 'NONE',  ( 1.000000000000000000, 0.000000000000000000, 0.000000000000000000 ) ) ;
#4006=VECTOR ( 'NONE', #15851, 1000.000000000000000 ) ;
#4007=CARTESIAN_POINT ( 'NONE',  ( 0.000000000000000000, 87.58454185039441597, 8.540961822681984117 ) ) ;
#4008=ORIENTED_EDGE ( 'NONE', *, *, #8300, .T. ) ;
#4009=VERTEX_POINT ( 'NONE', #5924 ) ;
#4012=AXIS2_PLACEMENT_3D ( 'NONE', #6113, #12833, #2465 ) ;
#4013=CARTESIAN_POINT ( 'NONE',  ( 0.000000000000000000, 0.000000000000000000, 0.000000000000000000 ) ) ;
#4014=DIRECTION ( 'NONE',  ( -1.000000000000000000, 0.000000000000000000, -0.000000000000000000 ) ) ;
#4016=CARTESIAN_POINT ( 'NONE',  ( 0.000000000000000000, 0.000000000000000000, 0.000000000000000000 ) ) ;
#4018=LINE ( 'NONE', #171, #9212 ) ;
#4019=EDGE_LOOP ( 'NONE', ( #9121, #15605, #9238, #18507 ) ) ;
#4020=CARTESIAN_POINT ( 'NONE',  ( 0.000000000000000000, -81.97107881582211064, 22.71412948308539370 ) ) ;
#4021=AXIS2_PLACEMENT_3D ( 'NONE', #2496, #14426, #12430 ) ;
#4023=CARTESIAN_POINT ( 'NONE',  ( 0.000000000000000000, 51.10509369859433804, 77.10190917907216601 ) ) ;
#4026=EDGE_CURVE ( 'NONE', #6084, #18142, #732, .T. ) ;
#4028=ORIENTED_EDGE ( 'NONE', *, *, #15407, .T. ) ;
#4029=SURFACE_STYLE_FILL_AREA ( #12326 ) ;
#4030=CIRCLE ( 'NONE', #16388, 92.50100000000000477 ) ;
#4031=ORIENTED_EDGE ( 'NONE', *, *, #2207, .T. ) ;
#4033=AXIS2_PLACEMENT_3D ( 'NONE', #2122, #15590, #14145 ) ;
#4034=ORIENTED_EDGE ( 'NONE', *, *, #5288, .T. ) ;
#4035=DIRECTION ( 'NONE',  ( 0.000000000000000000, 0.000000000000000000, 1.000000000000000000 ) ) ;
#4039=VECTOR ( 'NONE', #16846, 1000.000000000000000 ) ;
#4040=CARTESIAN_POINT ( 'NONE',  ( 0.000000000000000000, 82.02147376274670876, 42.76579056660889933 ) ) ;
#4041=CARTESIAN_POINT ( 'NONE',  ( 5.000000000000000000, -75.87763420127801339, -44.57111876559802255 ) ) ;
#4043=CARTESIAN_POINT ( 'NONE',  ( 0.000000000000000000, -72.58367602204218372, 49.75550195834843237 ) ) ;
#4044=VECTOR ( 'NONE', #13393, 1000.000000000000000 ) ;
#4046=EDGE_CURVE ( 'NONE', #12634, #15915, #7574, .T. ) ;
#4049=CIRCLE ( 'NONE', #20978, 92.50099999999999056 ) ;
#4053=DIRECTION ( 'NONE',  ( 0.000000000000000000, 0.000000000000000000, 1.000000000000000000 ) ) ;
#4057=CARTESIAN_POINT ( 'NONE',  ( 0.000000000000000000, 0.000000000000000000, 0.000000000000000000 ) ) ;
#4059=EDGE_CURVE ( 'NONE', #7682, #12369, #1058, .T. ) ;
#4060=EDGE_LOOP ( 'NONE', ( #8800, #13133, #16514, #2587 ) ) ;
#4066=VERTEX_POINT ( 'NONE', #18477 ) ;
#4067=CARTESIAN_POINT ( 'NONE',  ( 10.00000000000000000, -45.60224695560514618, -80.47900393021774335 ) ) ;
#4068=VERTEX_POINT ( 'NONE', #13487 ) ;
#4069=CARTESIAN_POINT ( 'NONE',  ( 0.000000000000000000, 61.60362715319035942, 62.84101464466265696 ) ) ;
#4071=DIRECTION ( 'NONE',  ( 0.000000000000000000, 0.000000000000000000, 1.000000000000000000 ) ) ;
#4072=CIRCLE ( 'NONE', #15711, 88.00000000000000000 ) ;
#4074=AXIS2_PLACEMENT_3D ( 'NONE', #5668, #903, #21138 ) ;
#4075=CYLINDRICAL_SURFACE ( 'NONE', #815, 92.50100000000000477 ) ;
#4076=AXIS2_PLACEMENT_3D ( 'NONE', #12012, #7145, #1847 ) ;
#4079=CYLINDRICAL_SURFACE ( 'NONE', #14923, 44.99999999999998579 ) ;
#4080=DIRECTION ( 'NONE',  ( 0.000000000000000000, -0.4067366430757887730, -0.9135454576426059736 ) ) ;
#4081=CYLINDRICAL_SURFACE ( 'NONE', #18873, 44.99999999999998579 ) ;
#4082=DIRECTION ( 'NONE',  ( 0.000000000000000000, 0.000000000000000000, 1.000000000000000000 ) ) ;
#4083=EDGE_CURVE ( 'NONE', #21518, #1477, #12973, .T. ) ;
#4084=DIRECTION ( 'NONE',  ( 0.000000000000000000, 0.000000000000000000, 1.000000000000000000 ) ) ;
#4085=AXIS2_PLACEMENT_3D ( 'NONE', #3150, #2824, #19826 ) ;
#4086=EDGE_CURVE ( 'NONE', #21782, #5377, #11584, .T. ) ;
#4088=DIRECTION ( 'NONE',  ( -1.000000000000000000, -0.000000000000000000, -0.000000000000000000 ) ) ;
#4090=CIRCLE ( 'NONE', #3032, 100.0000000000000000 ) ;
#4091=VERTEX_POINT ( 'NONE', #1793 ) ;
#4092=VECTOR ( 'NONE', #19603, 1000.000000000000000 ) ;
#4093=AXIS2_PLACEMENT_3D ( 'NONE', #6806, #20390, #7022 ) ;
#4096=EDGE_CURVE ( 'NONE', #9115, #18608, #15088, .T. ) ;
#4098=ORIENTED_EDGE ( 'NONE', *, *, #3313, .F. ) ;
#4102=CYLINDRICAL_SURFACE ( 'NONE', #14188, 92.50100000000000477 ) ;
#4103=CARTESIAN_POINT ( 'NONE',  ( 10.00000000000000000, 81.83745710415318797, -32.35167097270070258 ) ) ;
#4104=CYLINDRICAL_SURFACE ( 'NONE', #20925, 44.99999999999998579 ) ;
#4105=AXIS2_PLACEMENT_3D ( 'NONE', #5643, #12370, #17353 ) ;
#4106=DIRECTION ( 'NONE',  ( 0.000000000000000000, 0.8290375725550428454, -0.5591929034707450175 ) ) ;
#4108=AXIS2_PLACEMENT_3D ( 'NONE', #13830, #13727, #12171 ) ;
#4109=CYLINDRICAL_SURFACE ( 'NONE', #17852, 44.99999999999999289 ) ;
#4110=CYLINDRICAL_SURFACE ( 'NONE', #6264, 92.50100000000000477 ) ;
#4111=DIRECTION ( 'NONE',  ( 1.000000000000000000, 0.000000000000000000, 0.000000000000000000 ) ) ;
#4112=ADVANCED_FACE ( 'NONE', ( #18591 ), #9850, .F. ) ;
#4113=ORIENTED_EDGE ( 'NONE', *, *, #15420, .T. ) ;
#4115=DIRECTION ( 'NONE',  ( 1.000000000000000000, 0.000000000000000000, 0.000000000000000000 ) ) ;
#4116=CARTESIAN_POINT ( 'NONE',  ( 10.00000000000000000, 84.79630770241077187, 6.691460262316813790 ) ) ;
#4117=CARTESIAN_POINT ( 'NONE',  ( 10.00000000000000000, -74.39348546125016526, -54.97312363261490731 ) ) ;
#4119=EDGE_LOOP ( 'NONE', ( #13160, #10114, #16005, #20641 ) ) ;
#4120=CIRCLE ( 'NONE', #16468, 88.00000000000000000 ) ;
#4121=DIRECTION ( 'NONE',  ( -1.000000000000000000, 0.000000000000000000, 0.000000000000000000 ) ) ;
#4126=ORIENTED_EDGE ( 'NONE', *, *, #17274, .F. ) ;
#4127=CARTESIAN_POINT ( 'NONE',  ( 0.000000000000000000, 0.000000000000000000, 0.000000000000000000 ) ) ;
#4128=DIRECTION ( 'NONE',  ( 0.000000000000000000, 0.7431448254773953543, -0.6691306063588567943 ) ) ;
#4131=CARTESIAN_POINT ( 'NONE',  ( 0.000000000000000000, 46.89573839703386682, -79.73220629831438089 ) ) ;
#4132=CARTESIAN_POINT ( 'NONE',  ( 10.00000000000000000, 21.31452625070926743, 82.34610137166127686 ) ) ;
#4133=CARTESIAN_POINT ( 'NONE',  ( -10.00000000000000000, 0.000000000000000000, 0.000000000000000000 ) ) ;
#4134=CARTESIAN_POINT ( 'NONE',  ( 0.000000000000000000, 41.89587599971545018, 77.38692120905484728 ) ) ;
#4136=AXIS2_PLACEMENT_3D ( 'NONE', #13044, #21769, #8186 ) ;
#4138=ORIENTED_EDGE ( 'NONE', *, *, #584, .F. ) ;
#4139=AXIS2_PLACEMENT_3D ( 'NONE', #8836, #17778, #4080 ) ;
#4140=CARTESIAN_POINT ( 'NONE',  ( 0.000000000000000000, 3.728035544476225649, 84.97818067823770605 ) ) ;
#4142=DIRECTION ( 'NONE',  ( -1.000000000000000000, -0.000000000000000000, -0.000000000000000000 ) ) ;
#4145=DIRECTION ( 'NONE',  ( 0.000000000000000000, -0.1391731009600725710, 0.9902680687415692518 ) ) ;
#4146=ORIENTED_EDGE ( 'NONE', *, *, #19774, .F. ) ;
#4148=CIRCLE ( 'NONE', #6282, 44.99999999999999289 ) ;
#4150=VERTEX_POINT ( 'NONE', #8526 ) ;
#4152=ORIENTED_EDGE ( 'NONE', *, *, #17106, .F. ) ;
#4154=CARTESIAN_POINT ( 'NONE',  ( 10.00000000000000000, 81.97107881582226696, -22.71412948308482171 ) ) ;
#4155=ORIENTED_EDGE ( 'NONE', *, *, #9092, .F. ) ;
#4159=LINE ( 'NONE', #14204, #19179 ) ;
#4161=EDGE_CURVE ( 'NONE', #6607, #7559, #19912, .T. ) ;
#4162=ORIENTED_EDGE ( 'NONE', *, *, #7045, .T. ) ;
#4164=CIRCLE ( 'NONE', #977, 44.99999999999998579 ) ;
#4167=AXIS2_PLACEMENT_3D ( 'NONE', #18975, #15317, #8807 ) ;
#4168=CIRCLE ( 'NONE', #982, 92.50100000000000477 ) ;
#4169=EDGE_CURVE ( 'NONE', #4447, #6087, #4164, .T. ) ;
#4170=CARTESIAN_POINT ( 'NONE',  ( 10.00000000000000000, 0.000000000000000000, 0.000000000000000000 ) ) ;
#4171=ORIENTED_EDGE ( 'NONE', *, *, #13221, .T. ) ;
#4172=DIRECTION ( 'NONE',  ( -1.000000000000000000, -0.000000000000000000, -0.000000000000000000 ) ) ;
#4173=ORIENTED_EDGE ( 'NONE', *, *, #1262, .F. ) ;
#4175=ORIENTED_EDGE ( 'NONE', *, *, #8531, .F. ) ;
#4178=DIRECTION ( 'NONE',  ( 0.000000000000000000, 0.9271838545667883125, -0.3746065934159096833 ) ) ;
#4181=CIRCLE ( 'NONE', #16534, 88.00000000000000000 ) ;
#4182=DIRECTION ( 'NONE',  ( 0.000000000000000000, -0.5877852522924797984, 0.8090169943749424553 ) ) ;
#4186=CIRCLE ( 'NONE', #7019, 44.99999999999998579 ) ;
#4187=DIRECTION ( 'NONE',  ( 0.000000000000000000, 0.000000000000000000, 1.000000000000000000 ) ) ;
#4188=CARTESIAN_POINT ( 'NONE',  ( 0.000000000000000000, 0.000000000000000000, 0.000000000000000000 ) ) ;
#4192=DIRECTION ( 'NONE',  ( 1.000000000000000000, 0.000000000000000000, 0.000000000000000000 ) ) ;
#4193=EDGE_CURVE ( 'NONE', #9671, #17337, #10499, .T. ) ;
#4195=DIRECTION ( 'NONE',  ( 0.000000000000000000, 1.063963731932441790E-14, -1.000000000000000000 ) ) ;
#4196=ADVANCED_FACE ( 'NONE', ( #13161 ), #6674, .F. ) ;
#4197=CYLINDRICAL_SURFACE ( 'NONE', #15048, 92.50100000000000477 ) ;
#4200=VERTEX_POINT ( 'NONE', #11729 ) ;
#4201=AXIS2_PLACEMENT_3D ( 'NONE', #8912, #19194, #15770 ) ;
#4202=ORIENTED_EDGE ( 'NONE', *, *, #1218, .T. ) ;
#4203=EDGE_CURVE ( 'NONE', #6246, #20166, #8399, .T. ) ;
#4204=ORIENTED_EDGE ( 'NONE', *, *, #18162, .F. ) ;
#4208=EDGE_LOOP ( 'NONE', ( #19197, #7078, #18584, #1612 ) ) ;
#4209=DIRECTION ( 'NONE',  ( -1.000000000000000000, 0.000000000000000000, -0.000000000000000000 ) ) ;
#4211=CIRCLE ( 'NONE', #11970, 92.50100000000000477 ) ;
#4213=DIRECTION ( 'NONE',  ( 1.000000000000000000, 0.000000000000000000, 0.000000000000000000 ) ) ;
#4214=AXIS2_PLACEMENT_3D ( 'NONE', #14523, #10880, #19609 ) ;
#4215=CARTESIAN_POINT ( 'NONE',  ( 0.000000000000000000, 84.19736439813806328, 38.30455363800960811 ) ) ;
#4219=DIRECTION ( 'NONE',  ( 0.000000000000000000, 0.000000000000000000, 1.000000000000000000 ) ) ;
#4221=ORIENTED_EDGE ( 'NONE', *, *, #3523, .F. ) ;
#4222=CARTESIAN_POINT ( 'NONE',  ( 10.00000000000000000, -83.48638250753209888, -27.82128566055197538 ) ) ;
#4223=CARTESIAN_POINT ( 'NONE',  ( 10.00000000000000000, 0.000000000000000000, 0.000000000000000000 ) ) ;
#4225=CARTESIAN_POINT ( 'NONE',  ( 0.000000000000000000, 21.31452625071037943, -82.34610137166097843 ) ) ;
#4227=DIRECTION ( 'NONE',  ( -1.000000000000000000, 0.000000000000000000, 0.000000000000000000 ) ) ;
#4228=ORIENTED_EDGE ( 'NONE', *, *, #12409, .F. ) ;
#4233=DIRECTION ( 'NONE',  ( 0.000000000000000000, 0.8660254037844397068, -0.4999999999999980016 ) ) ;
#4236=EDGE_CURVE ( 'NONE', #21231, #935, #11928, .T. ) ;
#4237=DIRECTION ( 'NONE',  ( -1.000000000000000000, 0.000000000000000000, 0.000000000000000000 ) ) ;
#4238=FACE_OUTER_BOUND ( 'NONE', #4721, .T. ) ;
#4239=ADVANCED_FACE ( 'NONE', ( #3768 ), #10392, .F. ) ;
#4240=CYLINDRICAL_SURFACE ( 'NONE', #10047, 88.00000000000000000 ) ;
#4241=CARTESIAN_POINT ( 'NONE',  ( 10.00000000000000000, 0.000000000000000000, 0.000000000000000000 ) ) ;
#4242=FACE_OUTER_BOUND ( 'NONE', #9294, .T. ) ;
#4243=CARTESIAN_POINT ( 'NONE',  ( -10.00000000000000000, 0.000000000000000000, 0.000000000000000000 ) ) ;
#4247=EDGE_CURVE ( 'NONE', #17357, #12772, #8754, .T. ) ;
#4248=AXIS2_PLACEMENT_3D ( 'NONE', #12823, #9511, #4554 ) ;
#4251=ORIENTED_EDGE ( 'NONE', *, *, #7043, .F. ) ;
#4253=ORIENTED_EDGE ( 'NONE', *, *, #9866, .F. ) ;
#4255=CYLINDRICAL_SURFACE ( 'NONE', #2107, 92.50100000000000477 ) ;
#4256=VERTEX_POINT ( 'NONE', #20566 ) ;
#4257=ORIENTED_EDGE ( 'NONE', *, *, #18133, .T. ) ;
#4259=VERTEX_POINT ( 'NONE', #19023 ) ;
#4261=FACE_BOUND ( 'NONE', #11573, .T. ) ;
#4263=ORIENTED_EDGE ( 'NONE', *, *, #5454, .F. ) ;
#4264=CARTESIAN_POINT ( 'NONE',  ( 10.00000000000000000, 0.000000000000000000, 0.000000000000000000 ) ) ;
#4266=DIRECTION ( 'NONE',  ( 0.000000000000000000, 0.000000000000000000, 1.000000000000000000 ) ) ;
#4269=VERTEX_POINT ( 'NONE', #13719 ) ;
#4270=DIRECTION ( 'NONE',  ( -1.000000000000000000, 0.000000000000000000, 0.000000000000000000 ) ) ;
#4271=CARTESIAN_POINT ( 'NONE',  ( 5.000000000000000000, -57.06999622551850138, 66.98518889142063415 ) ) ;
#4272=CARTESIAN_POINT ( 'NONE',  ( 0.000000000000000000, 0.000000000000000000, 0.000000000000000000 ) ) ;
#4274=CARTESIAN_POINT ( 'NONE',  ( 0.000000000000000000, -39.87723064937174655, 83.46401306393555330 ) ) ;
#4275=VERTEX_POINT ( 'NONE', #10505 ) ;
#4276=DIRECTION ( 'NONE',  ( 0.000000000000000000, 0.3420201433256693235, -0.9396926207859080948 ) ) ;
#4277=ORIENTED_EDGE ( 'NONE', *, *, #9581, .T. ) ;
#4278=ORIENTED_EDGE ( 'NONE', *, *, #14484, .F. ) ;
#4279=EDGE_CURVE ( 'NONE', #2625, #3525, #20404, .T. ) ;
#4280=ORIENTED_EDGE ( 'NONE', *, *, #7355, .F. ) ;
#4284=CARTESIAN_POINT ( 'NONE',  ( 10.00000000000000000, 84.19736439813806328, 38.30455363800960811 ) ) ;
#4289=DIRECTION ( 'NONE',  ( -1.000000000000000000, -0.000000000000000000, -0.000000000000000000 ) ) ;
#4290=CARTESIAN_POINT ( 'NONE',  ( 10.00000000000000000, 29.29369617358468858, 87.74003855418408193 ) ) ;
#4291=DIRECTION ( 'NONE',  ( -1.000000000000000000, -0.000000000000000000, -0.000000000000000000 ) ) ;
#4292=FACE_OUTER_BOUND ( 'NONE', #8195, .T. ) ;
#4293=CYLINDRICAL_SURFACE ( 'NONE', #14792, 44.99999999999998579 ) ;
#4294=DIRECTION ( 'NONE',  ( 0.000000000000000000, 0.000000000000000000, 1.000000000000000000 ) ) ;
#4296=ORIENTED_EDGE ( 'NONE', *, *, #5671, .F. ) ;
#4299=ORIENTED_EDGE ( 'NONE', *, *, #18242, .T. ) ;
#4300=EDGE_CURVE ( 'NONE', #49, #5950, #5935, .T. ) ;
#4301=ORIENTED_EDGE ( 'NONE', *, *, #14507, .F. ) ;
#4303=VECTOR ( 'NONE', #10637, 1000.000000000000000 ) ;
#4304=ORIENTED_EDGE ( 'NONE', *, *, #3656, .T. ) ;
#4306=CARTESIAN_POINT ( 'NONE',  ( 0.000000000000000000, -77.39385041987173963, 35.28996114464576550 ) ) ;
#4308=DIRECTION ( 'NONE',  ( 0.000000000000000000, 0.000000000000000000, 1.000000000000000000 ) ) ;
#4311=CARTESIAN_POINT ( 'NONE',  ( 0.000000000000000000, 61.71252885873388294, 58.53847642588613809 ) ) ;
#4312=DIRECTION ( 'NONE',  ( 0.000000000000000000, 0.000000000000000000, 1.000000000000000000 ) ) ;
#4315=AXIS2_PLACEMENT_3D ( 'NONE', #20246, #5109, #20143 ) ;
#4317=EDGE_CURVE ( 'NONE', #21664, #14408, #10288, .T. ) ;
#4322=CARTESIAN_POINT ( 'NONE',  ( 10.00000000000000000, 31.15801000616834315, 79.14775961996400611 ) ) ;
#4325=EDGE_CURVE ( 'NONE', #6904, #12778, #9446, .T. ) ;
#4326=EDGE_CURVE ( 'NONE', #2438, #6675, #2763, .T. ) ;
#4327=LINE ( 'NONE', #17605, #4900 ) ;
#4328=VERTEX_POINT ( 'NONE', #568 ) ;
#4333=VECTOR ( 'NONE', #1334, 1000.000000000000000 ) ;
#4335=VERTEX_POINT ( 'NONE', #3557 ) ;
#4338=AXIS2_PLACEMENT_3D ( 'NONE', #2875, #18130, #9270 ) ;
#4339=VECTOR ( 'NONE', #10368, 1000.000000000000000 ) ;
#4343=CARTESIAN_POINT ( 'NONE',  ( 10.00000000000000000, 0.000000000000000000, 0.000000000000000000 ) ) ;
#4344=FACE_OUTER_BOUND ( 'NONE', #16758, .T. ) ;
#4345=CARTESIAN_POINT ( 'NONE',  ( 10.00000000000000000, -73.32282170386882569, 48.65967342042752364 ) ) ;
#4350=EDGE_CURVE ( 'NONE', #8942, #21012, #3470, .T. ) ;
#4351=DIRECTION ( 'NONE',  ( 1.000000000000000000, 0.000000000000000000, 0.000000000000000000 ) ) ;
#4352=AXIS2_PLACEMENT_3D ( 'NONE', #8488, #20097, #21853 ) ;
#4355=CARTESIAN_POINT ( 'NONE',  ( 0.000000000000000000, 52.34334029047981574, -76.26670130689429072 ) ) ;
#4356=VECTOR ( 'NONE', #14348, 1000.000000000000000 ) ;
#4357=CYLINDRICAL_SURFACE ( 'NONE', #1758, 44.99999999999998579 ) ;
#4362=ORIENTED_EDGE ( 'NONE', *, *, #7850, .T. ) ;
#4363=EDGE_CURVE ( 'NONE', #6056, #15522, #21808, .T. ) ;
#4364=EDGE_LOOP ( 'NONE', ( #9900, #9756, #21495, #2533 ) ) ;
#4365=ORIENTED_EDGE ( 'NONE', *, *, #7836, .T. ) ;
#4366=CARTESIAN_POINT ( 'NONE',  ( 0.000000000000000000, -17.64925110578526812, 86.21197095186339254 ) ) ;
#4367=CARTESIAN_POINT ( 'NONE',  ( 10.00000000000000000, 78.01214607583800387, -33.90124636420030413 ) ) ;
#4368=ORIENTED_EDGE ( 'NONE', *, *, #8818, .F. ) ;
#4369=EDGE_CURVE ( 'NONE', #11040, #13984, #12993, .T. ) ;
#4371=CARTESIAN_POINT ( 'NONE',  ( 10.00000000000000000, 71.33759994382042180, -58.88447872958914786 ) ) ;
#4374=CARTESIAN_POINT ( 'NONE',  ( 0.000000000000000000, 0.000000000000000000, 0.000000000000000000 ) ) ;
#4378=ADVANCED_FACE ( 'NONE', ( #18022 ), #9589, .F. ) ;
#4379=AXIS2_PLACEMENT_3D ( 'NONE', #7468, #19287, #14310 ) ;
#4380=LINE ( 'NONE', #11330, #16582 ) ;
#4381=LINE ( 'NONE', #19410, #1964 ) ;
#4383=ADVANCED_FACE ( 'NONE', ( #9165 ), #19233, .F. ) ;
#4388=DIRECTION ( 'NONE',  ( 1.000000000000000000, 0.000000000000000000, 0.000000000000000000 ) ) ;
#4390=DIRECTION ( 'NONE',  ( -1.000000000000000000, -0.000000000000000000, -0.000000000000000000 ) ) ;
#4392=ORIENTED_EDGE ( 'NONE', *, *, #7869, .T. ) ;
#4395=DIRECTION ( 'NONE',  ( -1.000000000000000000, 0.000000000000000000, 0.000000000000000000 ) ) ;
#4396=VECTOR ( 'NONE', #1030, 1000.000000000000000 ) ;
#4397=EDGE_LOOP ( 'NONE', ( #5760, #17278, #1072, #17639 ) ) ;
#4398=DIRECTION ( 'NONE',  ( 0.000000000000000000, -0.7880107536067275653, 0.6156614753256510753 ) ) ;
#4399=DIRECTION ( 'NONE',  ( 0.000000000000000000, 0.2756373558169997184, -0.9612616959383185611 ) ) ;
#4400=DIRECTION ( 'NONE',  ( -1.000000000000000000, 0.000000000000000000, 0.000000000000000000 ) ) ;
#4404=DIRECTION ( 'NONE',  ( 0.000000000000000000, 0.7880107536067190166, 0.6156614753256620665 ) ) ;
#4405=EDGE_CURVE ( 'NONE', #9323, #1046, #20884, .T. ) ;
#4410=AXIS2_PLACEMENT_3D ( 'NONE', #12360, #647, #14228 ) ;
#4412=ORIENTED_EDGE ( 'NONE', *, *, #1218, .F. ) ;
#4413=ORIENTED_EDGE ( 'NONE', *, *, #6950, .T. ) ;
#4415=ORIENTED_EDGE ( 'NONE', *, *, #6650, .F. ) ;
#4416=AXIS2_PLACEMENT_3D ( 'NONE', #21155, #4461, #12741 ) ;
#4417=CIRCLE ( 'NONE', #4786, 92.50100000000000477 ) ;
#4419=AXIS2_PLACEMENT_3D ( 'NONE', #15876, #9124, #4266 ) ;
#4420=ORIENTED_EDGE ( 'NONE', *, *, #16251, .T. ) ;
#4423=ORIENTED_EDGE ( 'NONE', *, *, #2528, .T. ) ;
#4424=DIRECTION ( 'NONE',  ( -1.000000000000000000, 0.000000000000000000, 0.000000000000000000 ) ) ;
#4425=CARTESIAN_POINT ( 'NONE',  ( 0.000000000000000000, -52.34334029047821701, -76.26670130689538496 ) ) ;
#4430=CIRCLE ( 'NONE', #5843, 44.99999999999999289 ) ;
#4431=CYLINDRICAL_SURFACE ( 'NONE', #14674, 88.00000000000000000 ) ;
#4433=CARTESIAN_POINT ( 'NONE',  ( 0.000000000000000000, 19.83954325428771881, -82.71385593638672162 ) ) ;
#4435=AXIS2_PLACEMENT_3D ( 'NONE', #13318, #4941, #11675 ) ;
#4438=AXIS2_PLACEMENT_3D ( 'NONE', #18945, #3804, #5146 ) ;
#4439=CYLINDRICAL_SURFACE ( 'NONE', #11143, 88.00000000000000000 ) ;
#4440=ORIENTED_EDGE ( 'NONE', *, *, #19607, .T. ) ;
#4441=EDGE_CURVE ( 'NONE', #15239, #2267, #10514, .T. ) ;
#4442=CYLINDRICAL_SURFACE ( 'NONE', #10878, 44.99999999999999289 ) ;
#4445=DIRECTION ( 'NONE',  ( 0.000000000000000000, -0.2079116908177664480, 0.9781476007338041345 ) ) ;
#4447=VERTEX_POINT ( 'NONE', #12481 ) ;
#4449=EDGE_CURVE ( 'NONE', #21353, #12424, #17941, .T. ) ;
#4450=CARTESIAN_POINT ( 'NONE',  ( 10.00000000000000000, -45.60224695560626174, 80.47900393021710386 ) ) ;
#4451=ORIENTED_EDGE ( 'NONE', *, *, #17967, .T. ) ;
#4452=AXIS2_PLACEMENT_3D ( 'NONE', #3322, #5095, #21663 ) ;
#4453=ORIENTED_EDGE ( 'NONE', *, *, #9757, .F. ) ;
#4455=CARTESIAN_POINT ( 'NONE',  ( 0.000000000000000000, 2.481790431839256517, 92.46770094066594936 ) ) ;
#4457=CARTESIAN_POINT ( 'NONE',  ( 5.000000000000002665, -24.89070495400677530, -84.40647372620527733 ) ) ;
#4459=CARTESIAN_POINT ( 'NONE',  ( 10.00000000000000000, 82.02147376274669455, 42.76579056660889933 ) ) ;
#4461=DIRECTION ( 'NONE',  ( 1.000000000000000000, 0.000000000000000000, 0.000000000000000000 ) ) ;
#4462=DIRECTION ( 'NONE',  ( -1.000000000000000000, 0.000000000000000000, 0.000000000000000000 ) ) ;
#4463=ADVANCED_FACE ( 'NONE', ( #19549 ), #10936, .F. ) ;
#4465=EDGE_CURVE ( 'NONE', #20877, #15560, #16882, .T. ) ;
#4466=ORIENTED_EDGE ( 'NONE', *, *, #10419, .F. ) ;
#4467=LINE ( 'NONE', #2693, #16440 ) ;
#4468=EDGE_CURVE ( 'NONE', #13478, #21353, #3817, .T. ) ;
#4469=EDGE_LOOP ( 'NONE', ( #19467, #8016, #2581, #20382 ) ) ;
#4470=AXIS2_PLACEMENT_3D ( 'NONE', #6521, #3084, #11478 ) ;
#4471=VECTOR ( 'NONE', #15705, 1000.000000000000000 ) ;
#4472=DIRECTION ( 'NONE',  ( 0.000000000000000000, -0.8660254037844432595, 0.4999999999999918954 ) ) ;
#4474=CARTESIAN_POINT ( 'NONE',  ( 0.000000000000000000, 0.000000000000000000, 0.000000000000000000 ) ) ;
#4475=ORIENTED_EDGE ( 'NONE', *, *, #15927, .F. ) ;
#4478=ORIENTED_EDGE ( 'NONE', *, *, #11468, .T. ) ;
#4480=EDGE_LOOP ( 'NONE', ( #14543, #18450, #20484, #15425 ) ) ;
#4481=DIRECTION ( 'NONE',  ( -1.000000000000000000, 0.000000000000000000, 0.000000000000000000 ) ) ;
#4484=EDGE_CURVE ( 'NONE', #14902, #20191, #5984, .T. ) ;
#4485=CIRCLE ( 'NONE', #4136, 44.99999999999999289 ) ;
#4487=CARTESIAN_POINT ( 'NONE',  ( 10.00000000000000000, 0.000000000000000000, 0.000000000000000000 ) ) ;
#4488=AXIS2_PLACEMENT_3D ( 'NONE', #9342, #5943, #10790 ) ;
#4489=DIRECTION ( 'NONE',  ( 0.000000000000000000, 0.000000000000000000, 1.000000000000000000 ) ) ;
#4490=CARTESIAN_POINT ( 'NONE',  ( 10.00000000000000000, 87.44637528609661103, 9.855528870798920593 ) ) ;
#4491=AXIS2_PLACEMENT_3D ( 'NONE', #16914, #11, #10487 ) ;
#4494=DIRECTION ( 'NONE',  ( 0.000000000000000000, -0.5877852522924797984, 0.8090169943749425663 ) ) ;
#4495=ADVANCED_FACE ( 'NONE', ( #881 ), #7841, .F. ) ;
#4497=VERTEX_POINT ( 'NONE', #12920 ) ;
#4499=ORIENTED_EDGE ( 'NONE', *, *, #14040, .F. ) ;
#4502=AXIS2_PLACEMENT_3D ( 'NONE', #609, #15953, #21262 ) ;
#4503=DIRECTION ( 'NONE',  ( -1.000000000000000000, -0.000000000000000000, -0.000000000000000000 ) ) ;
#4504=AXIS2_PLACEMENT_3D ( 'NONE', #17952, #12633, #9203 ) ;
#4505=ORIENTED_EDGE ( 'NONE', *, *, #8779, .F. ) ;
#4507=CIRCLE ( 'NONE', #7332, 92.50100000000000477 ) ;
#4508=EDGE_CURVE ( 'NONE', #4068, #20507, #1213, .T. ) ;
#4509=ORIENTED_EDGE ( 'NONE', *, *, #4847, .F. ) ;
#4510=ORIENTED_EDGE ( 'NONE', *, *, #2609, .T. ) ;
#4511=CYLINDRICAL_SURFACE ( 'NONE', #17473, 44.99999999999998579 ) ;
#4512=EDGE_CURVE ( 'NONE', #17030, #13577, #11596, .T. ) ;
#4513=ORIENTED_EDGE ( 'NONE', *, *, #4894, .F. ) ;
#4515=LINE ( 'NONE', #14668, #16039 ) ;
#4516=FACE_OUTER_BOUND ( 'NONE', #6701, .T. ) ;
#4517=EDGE_CURVE ( 'NONE', #5352, #1972, #1706, .T. ) ;
#4518=DIRECTION ( 'NONE',  ( 1.000000000000000000, 0.000000000000000000, 0.000000000000000000 ) ) ;
#4522=CARTESIAN_POINT ( 'NONE',  ( 10.00000000000000000, 84.12297548659721258, 32.40974838672968872 ) ) ;
#4524=CIRCLE ( 'NONE', #16866, 44.99999999999999289 ) ;
#4525=CARTESIAN_POINT ( 'NONE',  ( 0.000000000000000000, -52.96496548042899377, 66.55750800669339640 ) ) ;
#4528=DIRECTION ( 'NONE',  ( 0.000000000000000000, 0.000000000000000000, -1.000000000000000000 ) ) ;
#4529=ORIENTED_EDGE ( 'NONE', *, *, #11108, .T. ) ;
#4530=ORIENTED_EDGE ( 'NONE', *, *, #20039, .F. ) ;
#4531=ORIENTED_EDGE ( 'NONE', *, *, #9320, .T. ) ;
#4532=VECTOR ( 'NONE', #3091, 1000.000000000000000 ) ;
#4533=EDGE_LOOP ( 'NONE', ( #21623, #16487, #3115, #21701 ) ) ;
#4534=CIRCLE ( 'NONE', #18659, 88.00000000000000000 ) ;
#4535=VECTOR ( 'NONE', #6668, 1000.000000000000000 ) ;
#4537=ORIENTED_EDGE ( 'NONE', *, *, #17011, .F. ) ;
#4538=CARTESIAN_POINT ( 'NONE',  ( -10.00000000000000000, 0.000000000000000000, 0.000000000000000000 ) ) ;
#4539=VERTEX_POINT ( 'NONE', #2976 ) ;
#4540=LINE ( 'NONE', #7959, #9233 ) ;
#4542=DIRECTION ( 'NONE',  ( 1.000000000000000000, 0.000000000000000000, 0.000000000000000000 ) ) ;
#4543=FACE_OUTER_BOUND ( 'NONE', #18434, .T. ) ;
#4545=CYLINDRICAL_SURFACE ( 'NONE', #13659, 44.99999999999999289 ) ;
#4546=CARTESIAN_POINT ( 'NONE',  ( 0.000000000000000000, 41.89587599971653731, -77.38692120905427885 ) ) ;
#4547=VECTOR ( 'NONE', #11018, 1000.000000000000000 ) ;
#4549=ORIENTED_EDGE ( 'NONE', *, *, #15717, .F. ) ;
#4550=AXIS2_PLACEMENT_3D ( 'NONE', #19986, #21744, #9690 ) ;
#4554=DIRECTION ( 'NONE',  ( 0.000000000000000000, 0.000000000000000000, 1.000000000000000000 ) ) ;
#4556=CARTESIAN_POINT ( 'NONE',  ( 10.00000000000000000, 81.32027326007924728, -44.08455690948972716 ) ) ;
#4557=ORIENTED_EDGE ( 'NONE', *, *, #14901, .T. ) ;
#4558=ORIENTED_EDGE ( 'NONE', *, *, #9027, .F. ) ;
#4560=VECTOR ( 'NONE', #21468, 1000.000000000000000 ) ;
#4561=CARTESIAN_POINT ( 'NONE',  ( 10.00000000000000000, 2.208823992044147033, 85.03123271466937183 ) ) ;
#4563=EDGE_CURVE ( 'NONE', #8013, #12830, #1541, .T. ) ;
#4564=CIRCLE ( 'NONE', #12674, 45.00000000000000711 ) ;
#4567=AXIS2_PLACEMENT_3D ( 'NONE', #10785, #19299, #5828 ) ;
#4568=LINE ( 'NONE', #21248, #14801 ) ;
#4569=CARTESIAN_POINT ( 'NONE',  ( 10.00000000000000000, -56.35896156214997887, 73.34918167666290856 ) ) ;
#4571=LINE ( 'NONE', #11303, #6234 ) ;
#4572=CARTESIAN_POINT ( 'NONE',  ( -10.00000000000000000, 0.000000000000000000, 0.000000000000000000 ) ) ;
#4573=EDGE_CURVE ( 'NONE', #215, #18043, #7358, .T. ) ;
#4575=CARTESIAN_POINT ( 'NONE',  ( 5.000000000000000000, 41.89587599971545728, 77.38692120905484728 ) ) ;
#4576=CARTESIAN_POINT ( 'NONE',  ( 10.00000000000000000, 0.000000000000000000, 0.000000000000000000 ) ) ;
#4584=CARTESIAN_POINT ( 'NONE',  ( 10.00000000000000000, -41.21966518006011881, 82.80926399530274296 ) ) ;
#4587=VERTEX_POINT ( 'NONE', #4859 ) ;
#4588=EDGE_CURVE ( 'NONE', #17903, #536, #16675, .T. ) ;
#4589=ADVANCED_FACE ( 'NONE', ( #19780 ), #16908, .F. ) ;
#4590=VERTEX_POINT ( 'NONE', #6320 ) ;
#4591=DIRECTION ( 'NONE',  ( -1.000000000000000000, 0.000000000000000000, -0.000000000000000000 ) ) ;
#4592=CARTESIAN_POINT ( 'NONE',  ( 10.00000000000000000, 83.03980459022454852, 18.42770452393382641 ) ) ;
#4594=EDGE_CURVE ( 'NONE', #13601, #19313, #10876, .T. ) ;
#4599=DIRECTION ( 'NONE',  ( -1.000000000000000000, -0.000000000000000000, -0.000000000000000000 ) ) ;
#4601=UNCERTAINTY_MEASURE_WITH_UNIT (LENGTH_MEASURE( 1.000000000000000082E-05 ), #13982, 'distance_accuracy_value', 'NONE');
#4602=VERTEX_POINT ( 'NONE', #13135 ) ;
#4605=CARTESIAN_POINT ( 'NONE',  ( 10.00000000000000000, -19.83954325428713972, 82.71385593638686373 ) ) ;
#4606=VERTEX_POINT ( 'NONE', #14690 ) ;
#4607=EDGE_CURVE ( 'NONE', #10469, #6016, #4181, .T. ) ;
#4608=FACE_OUTER_BOUND ( 'NONE', #1949, .T. ) ;
#4609=ORIENTED_EDGE ( 'NONE', *, *, #16020, .T. ) ;
#4611=AXIS2_PLACEMENT_3D ( 'NONE', #13108, #14550, #19967 ) ;
#4612=FACE_OUTER_BOUND ( 'NONE', #4974, .T. ) ;
#4616=EDGE_CURVE ( 'NONE', #18424, #20435, #310, .T. ) ;
#4617=ORIENTED_EDGE ( 'NONE', *, *, #14306, .F. ) ;
#4618=EDGE_CURVE ( 'NONE', #21664, #12163, #14396, .T. ) ;
#4619=DIRECTION ( 'NONE',  ( 0.000000000000000000, -0.9271838545667908660, 0.3746065934159030775 ) ) ;
#4621=DIRECTION ( 'NONE',  ( 0.000000000000000000, 0.000000000000000000, 1.000000000000000000 ) ) ;
#4623=VECTOR ( 'NONE', #14869, 1000.000000000000000 ) ;
#4628=CARTESIAN_POINT ( 'NONE',  ( 10.00000000000000000, -75.45728100697571961, -39.26051685139143643 ) ) ;
#4629=DIRECTION ( 'NONE',  ( 0.000000000000000000, 0.000000000000000000, 1.000000000000000000 ) ) ;
#4630=DIRECTION ( 'NONE',  ( 1.000000000000000000, 0.000000000000000000, 0.000000000000000000 ) ) ;
#4631=ADVANCED_FACE ( 'NONE', ( #11708 ), #8179, .F. ) ;
#4632=FACE_OUTER_BOUND ( 'NONE', #968, .T. ) ;
#4634=CYLINDRICAL_SURFACE ( 'NONE', #5891, 88.00000000000000000 ) ;
#4635=ORIENTED_EDGE ( 'NONE', *, *, #16480, .T. ) ;
#4636=EDGE_LOOP ( 'NONE', ( #13059, #9089, #11310, #18154 ) ) ;
#4637=ADVANCED_FACE ( 'NONE', ( #10040 ), #8398, .F. ) ;
#4639=ORIENTED_EDGE ( 'NONE', *, *, #13137, .T. ) ;
#4642=DIRECTION ( 'NONE',  ( 0.000000000000000000, 0.4067366430757947127, 0.9135454576426031981 ) ) ;
#4644=ORIENTED_EDGE ( 'NONE', *, *, #8153, .T. ) ;
#4645=CYLINDRICAL_SURFACE ( 'NONE', #4676, 88.00000000000000000 ) ;
#4651=DIRECTION ( 'NONE',  ( 1.000000000000000000, 0.000000000000000000, 0.000000000000000000 ) ) ;
#4652=EDGE_LOOP ( 'NONE', ( #20468, #1561, #16123, #11956 ) ) ;
#4653=DIRECTION ( 'NONE',  ( -1.000000000000000000, -0.000000000000000000, 0.000000000000000000 ) ) ;
#4654=EDGE_LOOP ( 'NONE', ( #1675, #1836, #12399, #18449 ) ) ;
#4655=EDGE_CURVE ( 'NONE', #5100, #10149, #9833, .T. ) ;
#4656=ORIENTED_EDGE ( 'NONE', *, *, #20306, .T. ) ;
#4657=AXIS2_PLACEMENT_3D ( 'NONE', #1634, #14789, #1516 ) ;
#4658=CARTESIAN_POINT ( 'NONE',  ( 5.000000000000002665, -87.58454185039434492, -8.540961822682595184 ) ) ;
#4659=CARTESIAN_POINT ( 'NONE',  ( 0.000000000000000000, -51.10509369859486384, 77.10190917907182495 ) ) ;
#4660=VERTEX_POINT ( 'NONE', #431 ) ;
#4667=DIRECTION ( 'NONE',  ( 1.000000000000000000, 0.000000000000000000, 0.000000000000000000 ) ) ;
#4668=AXIS2_PLACEMENT_3D ( 'NONE', #5544, #13827, #7422 ) ;
#4670=CARTESIAN_POINT ( 'NONE',  ( 0.000000000000000000, 36.39558101400249512, -80.12091913260344711 ) ) ;
#4672=DIRECTION ( 'NONE',  ( 0.000000000000000000, -0.8660254037844328234, -0.5000000000000101030 ) ) ;
#4673=DIRECTION ( 'NONE',  ( 0.000000000000000000, 0.000000000000000000, 1.000000000000000000 ) ) ;
#4674=LINE ( 'NONE', #16500, #18546 ) ;
#4675=FACE_OUTER_BOUND ( 'NONE', #14571, .T. ) ;
#4676=AXIS2_PLACEMENT_3D ( 'NONE', #11373, #8074, #18126 ) ;
#4679=ORIENTED_EDGE ( 'NONE', *, *, #2609, .F. ) ;
#4680=CARTESIAN_POINT ( 'NONE',  ( 10.00000000000000000, -86.66425444033941972, 32.33793443156368852 ) ) ;
#4681=CARTESIAN_POINT ( 'NONE',  ( 10.00000000000000000, 46.89573839703386682, -79.73220629831438089 ) ) ;
#4682=CIRCLE ( 'NONE', #17753, 44.99999999999998579 ) ;
#4683=ORIENTED_EDGE ( 'NONE', *, *, #13285, .T. ) ;
#4685=ORIENTED_EDGE ( 'NONE', *, *, #5196, .F. ) ;
#4687=VERTEX_POINT ( 'NONE', #3533 ) ;
#4688=AXIS2_PLACEMENT_3D ( 'NONE', #6539, #16680, #6757 ) ;
#4689=ORIENTED_EDGE ( 'NONE', *, *, #13797, .F. ) ;
#4690=ORIENTED_EDGE ( 'NONE', *, *, #11627, .F. ) ;
#4691=CARTESIAN_POINT ( 'NONE',  ( 10.00000000000000000, -12.90135963484022241, -87.04915231966658951 ) ) ;
#4693=AXIS2_PLACEMENT_3D ( 'NONE', #10307, #15278, #4806 ) ;
#4696=LINE ( 'NONE', #9886, #7683 ) ;
#4697=CARTESIAN_POINT ( 'NONE',  ( 10.00000000000000000, 75.27139873020959726, -53.76477968147737840 ) ) ;
#4698=DIRECTION ( 'NONE',  ( 0.000000000000000000, 0.000000000000000000, 1.000000000000000000 ) ) ;
#4699=DIRECTION ( 'NONE',  ( 0.000000000000000000, 0.8987940462991680368, -0.4383711467890752389 ) ) ;
#4700=CARTESIAN_POINT ( 'NONE',  ( 0.000000000000000000, 90.63195040374210976, -18.50093422002330712 ) ) ;
#4702=VERTEX_POINT ( 'NONE', #5308 ) ;
#4704=VECTOR ( 'NONE', #13094, 1000.000000000000000 ) ;
#4705=CIRCLE ( 'NONE', #20188, 92.50099999999999056 ) ;
#4706=DIRECTION ( 'NONE',  ( 1.000000000000000000, 0.000000000000000000, 0.000000000000000000 ) ) ;
#4707=ADVANCED_FACE ( 'NONE', ( #1866 ), #3858, .F. ) ;
#4708=ORIENTED_EDGE ( 'NONE', *, *, #13116, .F. ) ;
#4710=ORIENTED_EDGE ( 'NONE', *, *, #5001, .T. ) ;
#4712=CARTESIAN_POINT ( 'NONE',  ( 10.00000000000000000, -33.95793648385871677, 86.04239391577979745 ) ) ;
#4713=DIRECTION ( 'NONE',  ( -1.000000000000000000, -0.000000000000000000, -0.000000000000000000 ) ) ;
#4715=EDGE_CURVE ( 'NONE', #3420, #9395, #16554, .T. ) ;
#4716=DIRECTION ( 'NONE',  ( 0.000000000000000000, -0.6427876096865458022, 0.7660444431189726844 ) ) ;
#4717=CIRCLE ( 'NONE', #16002, 88.00000000000000000 ) ;
#4718=ORIENTED_EDGE ( 'NONE', *, *, #18091, .F. ) ;
#4721=EDGE_LOOP ( 'NONE', ( #16674, #15934, #18281, #664 ) ) ;
#4722=ADVANCED_FACE ( 'NONE', ( #17232 ), #12359, .F. ) ;
#4723=LINE ( 'NONE', #16763, #2796 ) ;
#4724=DIRECTION ( 'NONE',  ( 0.000000000000000000, -0.1391731009600517821, -0.9902680687415721383 ) ) ;
#4727=CARTESIAN_POINT ( 'NONE',  ( 10.00000000000000000, -46.93287725819731548, -70.94007663282492615 ) ) ;
#4728=CIRCLE ( 'NONE', #7915, 88.00000000000000000 ) ;
#4730=CARTESIAN_POINT ( 'NONE',  ( 10.00000000000000000, 0.000000000000000000, 0.000000000000000000 ) ) ;
#4731=CARTESIAN_POINT ( 'NONE',  ( 10.00000000000000000, -79.38136668499764426, 37.98155635597287016 ) ) ;
#4735=CARTESIAN_POINT ( 'NONE',  ( 10.00000000000000000, -80.18694381077088451, -28.37681241246736974 ) ) ;
#4737=EDGE_CURVE ( 'NONE', #10766, #16126, #16901, .T. ) ;
#4739=VECTOR ( 'NONE', #10776, 1000.000000000000000 ) ;
#4740=ORIENTED_EDGE ( 'NONE', *, *, #12559, .F. ) ;
#4741=EDGE_CURVE ( 'NONE', #14101, #21516, #7378, .T. ) ;
#4744=ORIENTED_EDGE ( 'NONE', *, *, #456, .F. ) ;
#4745=VERTEX_POINT ( 'NONE', #8830 ) ;
#4746=VERTEX_POINT ( 'NONE', #17447 ) ;
#4748=CARTESIAN_POINT ( 'NONE',  ( 0.000000000000000000, -25.56104204395359503, 81.12843256239655432 ) ) ;
#4749=AXIS2_PLACEMENT_3D ( 'NONE', #4572, #18054, #2905 ) ;
#4752=CIRCLE ( 'NONE', #10386, 92.50100000000000477 ) ;
#4753=CARTESIAN_POINT ( 'NONE',  ( 5.000000000000002665, -85.22372865846278955, -21.92979875759713693 ) ) ;
#4754=ADVANCED_FACE ( 'NONE', ( #18776 ), #103, .F. ) ;
#4755=CARTESIAN_POINT ( 'NONE',  ( 10.00000000000000000, 0.000000000000000000, 0.000000000000000000 ) ) ;
#4758=AXIS2_PLACEMENT_3D ( 'NONE', #1190, #2854, #18004 ) ;
#4759=EDGE_CURVE ( 'NONE', #15531, #13465, #3137, .T. ) ;
#4761=DIRECTION ( 'NONE',  ( 0.000000000000000000, -0.9945218953682742891, 0.1045284632676436315 ) ) ;
#4763=CARTESIAN_POINT ( 'NONE',  ( 10.00000000000000000, 0.000000000000000000, 0.000000000000000000 ) ) ;
#4764=CIRCLE ( 'NONE', #11467, 92.50099999999999056 ) ;
#4766=AXIS2_PLACEMENT_3D ( 'NONE', #11806, #21746, #1318 ) ;
#4768=AXIS2_PLACEMENT_3D ( 'NONE', #19182, #12654, #17977 ) ;
#4769=ORIENTED_EDGE ( 'NONE', *, *, #4512, .T. ) ;
#4770=DIRECTION ( 'NONE',  ( 0.000000000000000000, 0.000000000000000000, 1.000000000000000000 ) ) ;
#4771=ORIENTED_EDGE ( 'NONE', *, *, #15554, .F. ) ;
#4772=DIRECTION ( 'NONE',  ( 0.000000000000000000, 0.9945218953682737340, -0.1045284632676505149 ) ) ;
#4774=ORIENTED_EDGE ( 'NONE', *, *, #6086, .T. ) ;
#4775=CIRCLE ( 'NONE', #1953, 44.99999999999998579 ) ;
#4777=EDGE_CURVE ( 'NONE', #12008, #10332, #1725, .T. ) ;
#4778=CARTESIAN_POINT ( 'NONE',  ( 10.00000000000000000, 0.000000000000000000, 0.000000000000000000 ) ) ;
#4779=EDGE_LOOP ( 'NONE', ( #18375, #1967, #367, #1207 ) ) ;
#4781=CYLINDRICAL_SURFACE ( 'NONE', #13934, 88.00000000000000000 ) ;
#4782=EDGE_CURVE ( 'NONE', #6246, #9931, #17263, .T. ) ;
#4783=DIRECTION ( 'NONE',  ( -1.000000000000000000, -0.000000000000000000, -0.000000000000000000 ) ) ;
#4784=FACE_OUTER_BOUND ( 'NONE', #3056, .T. ) ;
#4786=AXIS2_PLACEMENT_3D ( 'NONE', #9132, #10787, #10679 ) ;
#4787=DIRECTION ( 'NONE',  ( 0.000000000000000000, 0.8987940462991680368, -0.4383711467890752389 ) ) ;
#4788=ADVANCED_FACE ( 'NONE', ( #645 ), #6066, .F. ) ;
#4790=CIRCLE ( 'NONE', #16443, 44.99999999999999289 ) ;
#4791=EDGE_CURVE ( 'NONE', #4066, #6505, #12298, .T. ) ;
#4792=DIRECTION ( 'NONE',  ( -1.000000000000000000, 0.000000000000000000, -0.000000000000000000 ) ) ;
#4793=DIRECTION ( 'NONE',  ( -1.000000000000000000, 0.000000000000000000, -0.000000000000000000 ) ) ;
#4794=CYLINDRICAL_SURFACE ( 'NONE', #2753, 45.00000000000000000 ) ;
#4795=CIRCLE ( 'NONE', #19962, 92.50100000000000477 ) ;
#4796=ORIENTED_EDGE ( 'NONE', *, *, #128, .T. ) ;
#4801=CARTESIAN_POINT ( 'NONE',  ( 10.00000000000000000, -46.93287725819829603, 70.94007663282431508 ) ) ;
#4802=AXIS2_PLACEMENT_3D ( 'NONE', #10980, #9419, #17954 ) ;
#4804=CIRCLE ( 'NONE', #8683, 44.99999999999999289 ) ;
#4806=DIRECTION ( 'NONE',  ( 0.000000000000000000, -0.8987940462991618196, -0.4383711467890877289 ) ) ;
#4808=ORIENTED_EDGE ( 'NONE', *, *, #2528, .F. ) ;
#4810=DIRECTION ( 'NONE',  ( 0.000000000000000000, 0.4694715627858855322, 0.8829475928589297640 ) ) ;
#4812=DIRECTION ( 'NONE',  ( 0.000000000000000000, 0.000000000000000000, 1.000000000000000000 ) ) ;
#4814=DIRECTION ( 'NONE',  ( 0.000000000000000000, 0.000000000000000000, -1.000000000000000000 ) ) ;
#4815=CARTESIAN_POINT ( 'NONE',  ( 10.00000000000000000, -27.87320266523496315, -88.20158487341788600 ) ) ;
#4817=DIRECTION ( 'NONE',  ( 1.000000000000000000, -0.000000000000000000, -0.000000000000000000 ) ) ;
#4819=CIRCLE ( 'NONE', #20684, 88.00000000000000000 ) ;
#4822=CIRCLE ( 'NONE', #13119, 92.50099999999999056 ) ;
#4824=FACE_OUTER_BOUND ( 'NONE', #10229, .T. ) ;
#4827=ORIENTED_EDGE ( 'NONE', *, *, #1345, .T. ) ;
#4828=DIRECTION ( 'NONE',  ( 0.000000000000000000, 0.000000000000000000, 1.000000000000000000 ) ) ;
#4829=CARTESIAN_POINT ( 'NONE',  ( 10.00000000000000000, 0.000000000000000000, 0.000000000000000000 ) ) ;
#4830=ORIENTED_EDGE ( 'NONE', *, *, #831, .T. ) ;
#4831=CARTESIAN_POINT ( 'NONE',  ( 0.000000000000000000, -64.66851233300690183, -55.25552418573029456 ) ) ;
#4833=EDGE_LOOP ( 'NONE', ( #5985, #20046, #6965, #4969 ) ) ;
#4835=ORIENTED_EDGE ( 'NONE', *, *, #14481, .F. ) ;
#4836=DIRECTION ( 'NONE',  ( 0.000000000000000000, 0.000000000000000000, 1.000000000000000000 ) ) ;
#4839=CARTESIAN_POINT ( 'NONE',  ( 5.000000000000000000, 47.19205848891868271, -74.27590198428072199 ) ) ;
#4843=DIRECTION ( 'NONE',  ( -1.000000000000000000, -0.000000000000000000, -0.000000000000000000 ) ) ;
#4844=FILL_AREA_STYLE_COLOUR ( '', #20928 ) ;
#4845=DIRECTION ( 'NONE',  ( 1.000000000000000000, 0.000000000000000000, 0.000000000000000000 ) ) ;
#4847=EDGE_CURVE ( 'NONE', #20877, #13006, #859, .T. ) ;
#4849=CIRCLE ( 'NONE', #15785, 92.50100000000003320 ) ;
#4850=CARTESIAN_POINT ( 'NONE',  ( 0.000000000000000000, -81.34229909304657724, -33.57723005635448743 ) ) ;
#4852=CIRCLE ( 'NONE', #278, 88.00000000000000000 ) ;
#4854=ORIENTED_EDGE ( 'NONE', *, *, #13738, .F. ) ;
#4856=ORIENTED_EDGE ( 'NONE', *, *, #8828, .T. ) ;
#4858=VERTEX_POINT ( 'NONE', #4069 ) ;
#4859=CARTESIAN_POINT ( 'NONE',  ( 10.00000000000000000, -41.89587599971492438, -77.38692120905515992 ) ) ;
#4861=VERTEX_POINT ( 'NONE', #17556 ) ;
#4862=DIRECTION ( 'NONE',  ( 1.000000000000000000, 0.000000000000000000, 0.000000000000000000 ) ) ;
#4864=CIRCLE ( 'NONE', #16848, 44.99999999999999289 ) ;
#4865=EDGE_CURVE ( 'NONE', #17077, #1435, #7719, .T. ) ;
#4867=CIRCLE ( 'NONE', #14382, 88.00000000000000000 ) ;
#4868=DIRECTION ( 'NONE',  ( -1.000000000000000000, 0.000000000000000000, 0.000000000000000000 ) ) ;
#4869=EDGE_CURVE ( 'NONE', #4687, #11658, #12680, .T. ) ;
#4870=DIRECTION ( 'NONE',  ( -1.000000000000000000, -0.000000000000000000, -0.000000000000000000 ) ) ;
#4871=FACE_OUTER_BOUND ( 'NONE', #10991, .T. ) ;
#4873=LINE ( 'NONE', #19675, #1662 ) ;
#4874=CIRCLE ( 'NONE', #3812, 45.00000000000000711 ) ;
#4875=DIRECTION ( 'NONE',  ( -1.000000000000000000, 0.000000000000000000, -0.000000000000000000 ) ) ;
#4876=VERTEX_POINT ( 'NONE', #14343 ) ;
#4877=CARTESIAN_POINT ( 'NONE',  ( 5.000000000000000000, 57.06999622551897033, -66.98518889142023625 ) ) ;
#4878=EDGE_CURVE ( 'NONE', #2527, #19897, #20070, .T. ) ;
#4879=AXIS2_PLACEMENT_3D ( 'NONE', #20115, #18355, #4642 ) ;
#4881=ORIENTED_EDGE ( 'NONE', *, *, #15035, .T. ) ;
#4882=CIRCLE ( 'NONE', #19338, 44.99999999999999289 ) ;
#4883=ORIENTED_EDGE ( 'NONE', *, *, #21501, .F. ) ;
#4884=EDGE_CURVE ( 'NONE', #7563, #508, #7030, .T. ) ;
#4887=CARTESIAN_POINT ( 'NONE',  ( 0.000000000000000000, 48.19312842678564834, -70.09002648625148879 ) ) ;
#4888=ORIENTED_EDGE ( 'NONE', *, *, #5449, .F. ) ;
#4889=VERTEX_POINT ( 'NONE', #12456 ) ;
#4890=CARTESIAN_POINT ( 'NONE',  ( 10.00000000000000000, -2.481790431838652111, -92.46770094066596357 ) ) ;
#4891=ORIENTED_EDGE ( 'NONE', *, *, #4086, .T. ) ;
#4892=CARTESIAN_POINT ( 'NONE',  ( 10.00000000000000000, 0.000000000000000000, 0.000000000000000000 ) ) ;
#4894=EDGE_CURVE ( 'NONE', #15140, #21168, #2626, .T. ) ;
#4895=CARTESIAN_POINT ( 'NONE',  ( 5.000000000000000000, -36.39558101400082535, -80.12091913260421450 ) ) ;
#4898=CARTESIAN_POINT ( 'NONE',  ( 10.00000000000000000, 23.62010150527222052, 84.77081340225913664 ) ) ;
#4900=VECTOR ( 'NONE', #19253, 1000.000000000000000 ) ;
#4901=CIRCLE ( 'NONE', #18663, 45.00000000000000000 ) ;
#4904=CARTESIAN_POINT ( 'NONE',  ( 0.000000000000000000, -76.53853822674008711, 43.42639941457088781 ) ) ;
#4905=ORIENTED_EDGE ( 'NONE', *, *, #20306, .F. ) ;
#4907=CIRCLE ( 'NONE', #12655, 44.99999999999998579 ) ;
#4908=ADVANCED_FACE ( 'NONE', ( #972 ), #19527, .F. ) ;
#4913=CIRCLE ( 'NONE', #10896, 92.50100000000000477 ) ;
#4919=ORIENTED_EDGE ( 'NONE', *, *, #4096, .T. ) ;
#4921=ORIENTED_EDGE ( 'NONE', *, *, #8271, .T. ) ;
#4923=ORIENTED_EDGE ( 'NONE', *, *, #17207, .T. ) ;
#4925=CARTESIAN_POINT ( 'NONE',  ( 0.000000000000000000, -85.54350296776095774, -20.64725405482940346 ) ) ;
#4926=VERTEX_POINT ( 'NONE', #3182 ) ;
#4927=ORIENTED_EDGE ( 'NONE', *, *, #9577, .T. ) ;
#4929=FACE_OUTER_BOUND ( 'NONE', #5475, .T. ) ;
#4930=DIRECTION ( 'NONE',  ( -1.000000000000000000, -0.000000000000000000, -0.000000000000000000 ) ) ;
#4931=FACE_OUTER_BOUND ( 'NONE', #20528, .T. ) ;
#4933=DIRECTION ( 'NONE',  ( 1.000000000000000000, 0.000000000000000000, 0.000000000000000000 ) ) ;
#4934=DIRECTION ( 'NONE',  ( 0.000000000000000000, -0.4694715627858798146, -0.8829475928589327616 ) ) ;
#4938=ORIENTED_EDGE ( 'NONE', *, *, #20938, .F. ) ;
#4939=AXIS2_PLACEMENT_3D ( 'NONE', #520, #15976, #10901 ) ;
#4940=LINE ( 'NONE', #14973, #5303 ) ;
#4941=DIRECTION ( 'NONE',  ( -1.000000000000000000, 0.000000000000000000, 0.000000000000000000 ) ) ;
#4942=EDGE_LOOP ( 'NONE', ( #13003, #11622, #9695, #4413 ) ) ;
#4944=ORIENTED_EDGE ( 'NONE', *, *, #969, .T. ) ;
#4950=ORIENTED_EDGE ( 'NONE', *, *, #11770, .T. ) ;
#4952=DIRECTION ( 'NONE',  ( 0.000000000000000000, -0.6946583704589885944, -0.7193398003386594075 ) ) ;
#4953=ORIENTED_EDGE ( 'NONE', *, *, #5987, .F. ) ;
#4954=FACE_OUTER_BOUND ( 'NONE', #19775, .T. ) ;
#4955=CARTESIAN_POINT ( 'NONE',  ( 0.000000000000000000, 0.000000000000000000, 0.000000000000000000 ) ) ;
#4956=DIRECTION ( 'NONE',  ( -1.000000000000000000, -0.000000000000000000, 0.000000000000000000 ) ) ;
#4957=CARTESIAN_POINT ( 'NONE',  ( 5.000000000000002665, -76.53853822674008711, 43.42639941457088781 ) ) ;
#4959=CARTESIAN_POINT ( 'NONE',  ( 10.00000000000000000, 0.000000000000000000, 0.000000000000000000 ) ) ;
#4960=DIRECTION ( 'NONE',  ( -1.000000000000000000, -0.000000000000000000, -0.000000000000000000 ) ) ;
#4961=FACE_OUTER_BOUND ( 'NONE', #12921, .T. ) ;
#4963=AXIS2_PLACEMENT_3D ( 'NONE', #8968, #18930, #585 ) ;
#4964=CARTESIAN_POINT ( 'NONE',  ( 10.00000000000000000, 0.000000000000000000, 0.000000000000000000 ) ) ;
#4967=EDGE_CURVE ( 'NONE', #21786, #15480, #11262, .T. ) ;
#4969=ORIENTED_EDGE ( 'NONE', *, *, #14359, .T. ) ;
#4970=VERTEX_POINT ( 'NONE', #14667 ) ;
#4971=EDGE_CURVE ( 'NONE', #17333, #7568, #20456, .T. ) ;
#4972=ORIENTED_EDGE ( 'NONE', *, *, #10099, .F. ) ;
#4973=DIRECTION ( 'NONE',  ( -1.000000000000000000, 0.000000000000000000, 0.000000000000000000 ) ) ;
#4974=EDGE_LOOP ( 'NONE', ( #13444, #1755, #21066, #12056 ) ) ;
#4975=FACE_OUTER_BOUND ( 'NONE', #15482, .T. ) ;
#4977=CARTESIAN_POINT ( 'NONE',  ( 10.00000000000000000, 0.000000000000000000, 0.000000000000000000 ) ) ;
#4978=DIRECTION ( 'NONE',  ( 0.000000000000000000, 0.000000000000000000, 1.000000000000000000 ) ) ;
#4979=DIRECTION ( 'NONE',  ( 0.000000000000000000, 0.000000000000000000, 1.000000000000000000 ) ) ;
#4980=DIRECTION ( 'NONE',  ( 1.000000000000000000, 0.000000000000000000, 0.000000000000000000 ) ) ;
#4981=LINE ( 'NONE', #11502, #7702 ) ;
#4985=ORIENTED_EDGE ( 'NONE', *, *, #4971, .F. ) ;
#4989=DIRECTION ( 'NONE',  ( -1.000000000000000000, -0.000000000000000000, 0.000000000000000000 ) ) ;
#4991=ORIENTED_EDGE ( 'NONE', *, *, #851, .F. ) ;
#4992=PRODUCT_CONTEXT ( 'NONE', #1204, 'mechanical' ) ;
#4993=DIRECTION ( 'NONE',  ( 0.000000000000000000, 0.000000000000000000, 1.000000000000000000 ) ) ;
#4997=CARTESIAN_POINT ( 'NONE',  ( 10.00000000000000000, 61.60362715319122628, -62.84101464466179721 ) ) ;
#5001=EDGE_CURVE ( 'NONE', #4259, #14855, #18098, .T. ) ;
#5003=CARTESIAN_POINT ( 'NONE',  ( 10.00000000000000000, -64.66851233300764079, 55.25552418572942059 ) ) ;
#5005=EDGE_CURVE ( 'NONE', #7352, #19098, #4723, .T. ) ;
#5006=EDGE_CURVE ( 'NONE', #11182, #11054, #6406, .T. ) ;
#5007=ADVANCED_FACE ( 'NONE', ( #4954 ), #6294, .F. ) ;
#5008=CARTESIAN_POINT ( 'NONE',  ( 10.00000000000000000, 0.000000000000000000, 0.000000000000000000 ) ) ;
#5010=ADVANCED_FACE ( 'NONE', ( #14994 ), #18331, .F. ) ;
#5011=DIRECTION ( 'NONE',  ( 1.000000000000000000, 0.000000000000000000, 0.000000000000000000 ) ) ;
#5013=CARTESIAN_POINT ( 'NONE',  ( 0.000000000000000000, 84.80486432185243473, -36.94008646920313055 ) ) ;
#5014=ORIENTED_EDGE ( 'NONE', *, *, #15695, .F. ) ;
#5018=VECTOR ( 'NONE', #21574, 1000.000000000000000 ) ;
#5020=ORIENTED_EDGE ( 'NONE', *, *, #18910, .T. ) ;
#5023=EDGE_LOOP ( 'NONE', ( #1078, #4679, #10655, #17133 ) ) ;
#5026=DIRECTION ( 'NONE',  ( -1.000000000000000000, -0.000000000000000000, 0.000000000000000000 ) ) ;
#5030=FACE_OUTER_BOUND ( 'NONE', #14932, .T. ) ;
#5031=EDGE_CURVE ( 'NONE', #21500, #5074, #1400, .T. ) ;
#5032=CARTESIAN_POINT ( 'NONE',  ( 10.00000000000000000, -91.49386717542212466, -13.61276130277086693 ) ) ;
#5033=ORIENTED_EDGE ( 'NONE', *, *, #16809, .T. ) ;
#5035=DIRECTION ( 'NONE',  ( -1.000000000000000000, -0.000000000000000000, 0.000000000000000000 ) ) ;
#5036=AXIS2_PLACEMENT_3D ( 'NONE', #1545, #9709, #11608 ) ;
#5038=ORIENTED_EDGE ( 'NONE', *, *, #16407, .F. ) ;
#5039=CARTESIAN_POINT ( 'NONE',  ( 5.000000000000000000, -60.65279801375385915, 63.75921967137595914 ) ) ;
#5041=AXIS2_PLACEMENT_3D ( 'NONE', #6431, #6094, #18028 ) ;
#5044=DIRECTION ( 'NONE',  ( -1.000000000000000000, -0.000000000000000000, -0.000000000000000000 ) ) ;
#5045=ORIENTED_EDGE ( 'NONE', *, *, #7645, .F. ) ;
#5047=DIRECTION ( 'NONE',  ( -1.000000000000000000, 0.000000000000000000, 0.000000000000000000 ) ) ;
#5049=VERTEX_POINT ( 'NONE', #15430 ) ;
#5050=AXIS2_PLACEMENT_3D ( 'NONE', #19347, #4213, #9271 ) ;
#5052=ORIENTED_EDGE ( 'NONE', *, *, #21568, .T. ) ;
#5054=EDGE_LOOP ( 'NONE', ( #5784, #16281, #10069, #3462 ) ) ;
#5056=AXIS2_PLACEMENT_3D ( 'NONE', #21301, #4518, #2856 ) ;
#5059=DIRECTION ( 'NONE',  ( -1.000000000000000000, -0.000000000000000000, -0.000000000000000000 ) ) ;
#5060=EDGE_CURVE ( 'NONE', #6638, #935, #10548, .T. ) ;
#5061=CARTESIAN_POINT ( 'NONE',  ( 0.000000000000000000, 31.15801000616942673, -79.14775961996359399 ) ) ;
#5062=VECTOR ( 'NONE', #12088, 1000.000000000000000 ) ;
#5063=AXIS2_PLACEMENT_3D ( 'NONE', #14996, #16556, #21846 ) ;
#5065=CYLINDRICAL_SURFACE ( 'NONE', #12087, 88.00000000000000000 ) ;
#5066=AXIS2_PLACEMENT_3D ( 'NONE', #16957, #3472, #1708 ) ;
#5067=EDGE_CURVE ( 'NONE', #13354, #14952, #21844, .T. ) ;
#5069=CYLINDRICAL_SURFACE ( 'NONE', #4766, 44.99999999999999289 ) ;
#5070=DIRECTION ( 'NONE',  ( 0.000000000000000000, 0.9993908270190955401, 0.03489949670250440394 ) ) ;
#5071=ORIENTED_EDGE ( 'NONE', *, *, #3565, .F. ) ;
#5072=AXIS2_PLACEMENT_3D ( 'NONE', #4727, #1747, #2957 ) ;
#5073=CARTESIAN_POINT ( 'NONE',  ( 5.000000000000002665, 40.72878876293257377, -78.00747250042405767 ) ) ;
#5074=VERTEX_POINT ( 'NONE', #20309 ) ;
#5079=AXIS2_PLACEMENT_3D ( 'NONE', #12946, #7987, #1244 ) ;
#5081=DIRECTION ( 'NONE',  ( -1.000000000000000000, 0.000000000000000000, 0.000000000000000000 ) ) ;
#5082=ORIENTED_EDGE ( 'NONE', *, *, #9306, .F. ) ;
#5083=FACE_OUTER_BOUND ( 'NONE', #1147, .T. ) ;
#5084=CARTESIAN_POINT ( 'NONE',  ( 10.00000000000000000, 66.01871308925461790, 64.79170103523043167 ) ) ;
#5085=VECTOR ( 'NONE', #19082, 1000.000000000000000 ) ;
#5086=DIRECTION ( 'NONE',  ( -1.000000000000000000, -0.000000000000000000, -0.000000000000000000 ) ) ;
#5087=LINE ( 'NONE', #15234, #15059 ) ;
#5088=CARTESIAN_POINT ( 'NONE',  ( 0.000000000000000000, 0.000000000000000000, 0.000000000000000000 ) ) ;
#5092=ORIENTED_EDGE ( 'NONE', *, *, #5910, .F. ) ;
#5095=DIRECTION ( 'NONE',  ( 1.000000000000000000, 0.000000000000000000, 0.000000000000000000 ) ) ;
#5099=VECTOR ( 'NONE', #15400, 1000.000000000000000 ) ;
#5100=VERTEX_POINT ( 'NONE', #12509 ) ;
#5103=ORIENTED_EDGE ( 'NONE', *, *, #6598, .F. ) ;
#5106=DIRECTION ( 'NONE',  ( 0.000000000000000000, 0.2756373558169932236, 0.9612616959383206705 ) ) ;
#5109=DIRECTION ( 'NONE',  ( -1.000000000000000000, -0.000000000000000000, -0.000000000000000000 ) ) ;
#5110=CARTESIAN_POINT ( 'NONE',  ( 10.00000000000000000, 0.000000000000000000, 0.000000000000000000 ) ) ;
#5111=CARTESIAN_POINT ( 'NONE',  ( 10.00000000000000000, -85.05652083079337444, 0.7600687895857258791 ) ) ;
#5114=FACE_OUTER_BOUND ( 'NONE', #4060, .T. ) ;
#5116=DIRECTION ( 'NONE',  ( 1.000000000000000000, 0.000000000000000000, 0.000000000000000000 ) ) ;
#5117=CIRCLE ( 'NONE', #12494, 92.50100000000000477 ) ;
#5119=ORIENTED_EDGE ( 'NONE', *, *, #11721, .F. ) ;
#5121=VECTOR ( 'NONE', #11693, 1000.000000000000000 ) ;
#5123=AXIS2_PLACEMENT_3D ( 'NONE', #5956, #21196, #4182 ) ;
#5125=EDGE_CURVE ( 'NONE', #8987, #6547, #195, .T. ) ;
#5126=DIRECTION ( 'NONE',  ( -1.000000000000000000, -0.000000000000000000, 0.000000000000000000 ) ) ;
#5128=CYLINDRICAL_SURFACE ( 'NONE', #18904, 44.99999999999999289 ) ;
#5130=VERTEX_POINT ( 'NONE', #799 ) ;
#5131=DIRECTION ( 'NONE',  ( -1.000000000000000000, 0.000000000000000000, 0.000000000000000000 ) ) ;
#5133=AXIS2_PLACEMENT_3D ( 'NONE', #16277, #17723, #7553 ) ;
#5134=CIRCLE ( 'NONE', #1253, 45.00000000000000000 ) ;
#5137=CARTESIAN_POINT ( 'NONE',  ( 10.00000000000000000, -19.83954325428713972, 82.71385593638686373 ) ) ;
#5138=CIRCLE ( 'NONE', #19246, 44.99999999999999289 ) ;
#5142=EDGE_CURVE ( 'NONE', #6401, #845, #11792, .T. ) ;
#5143=CARTESIAN_POINT ( 'NONE',  ( 10.00000000000000000, 90.63195040374210976, -18.50093422002330712 ) ) ;
#5144=CARTESIAN_POINT ( 'NONE',  ( 10.00000000000000000, 25.56104204395415991, -81.12843256239638379 ) ) ;
#5145=ADVANCED_FACE ( 'NONE', ( #7545 ), #14277, .F. ) ;
#5146=DIRECTION ( 'NONE',  ( 0.000000000000000000, 0.8987940462991651502, 0.4383711467890813451 ) ) ;
#5147=EDGE_CURVE ( 'NONE', #15286, #5049, #4211, .T. ) ;
#5148=DIRECTION ( 'NONE',  ( -1.000000000000000000, 0.000000000000000000, 0.000000000000000000 ) ) ;
#5150=CYLINDRICAL_SURFACE ( 'NONE', #5335, 44.99999999999998579 ) ;
#5151=ADVANCED_FACE ( 'NONE', ( #1739 ), #2469, .F. ) ;
#5152=VERTEX_POINT ( 'NONE', #16985 ) ;
#5155=VERTEX_POINT ( 'NONE', #15208 ) ;
#5158=CARTESIAN_POINT ( 'NONE',  ( 10.00000000000000000, 0.000000000000000000, 0.000000000000000000 ) ) ;
#5160=CIRCLE ( 'NONE', #7626, 44.99999999999999289 ) ;
#5161=ORIENTED_EDGE ( 'NONE', *, *, #12886, .T. ) ;
#5163=DIRECTION ( 'NONE',  ( -1.000000000000000000, -0.000000000000000000, -0.000000000000000000 ) ) ;
#5165=CYLINDRICAL_SURFACE ( 'NONE', #6053, 92.50100000000000477 ) ;
#5166=EDGE_CURVE ( 'NONE', #52, #1120, #15137, .T. ) ;
#5168=VERTEX_POINT ( 'NONE', #5378 ) ;
#5171=ORIENTED_EDGE ( 'NONE', *, *, #8361, .T. ) ;
#5172=CYLINDRICAL_SURFACE ( 'NONE', #21508, 88.00000000000000000 ) ;
#5175=AXIS2_PLACEMENT_3D ( 'NONE', #1673, #8412, #15142 ) ;
#5176=CARTESIAN_POINT ( 'NONE',  ( 0.000000000000000000, -36.39558101400191248, 80.12091913260368869 ) ) ;
#5179=ADVANCED_FACE ( 'NONE', ( #3719 ), #5172, .F. ) ;
#5180=DIRECTION ( 'NONE',  ( 0.000000000000000000, 0.000000000000000000, 1.000000000000000000 ) ) ;
#5181=DIRECTION ( 'NONE',  ( 0.000000000000000000, 0.000000000000000000, -1.000000000000000000 ) ) ;
#5182=CARTESIAN_POINT ( 'NONE',  ( 10.00000000000000000, 0.000000000000000000, 0.000000000000000000 ) ) ;
#5184=EDGE_CURVE ( 'NONE', #301, #9696, #14446, .T. ) ;
#5185=VERTEX_POINT ( 'NONE', #15541 ) ;
#5187=AXIS2_PLACEMENT_3D ( 'NONE', #13966, #10316, #13528 ) ;
#5196=EDGE_CURVE ( 'NONE', #21331, #10498, #4568, .T. ) ;
#5197=ORIENTED_EDGE ( 'NONE', *, *, #17037, .T. ) ;
#5198=DIRECTION ( 'NONE',  ( 1.000000000000000000, 0.000000000000000000, 0.000000000000000000 ) ) ;
#5200=CYLINDRICAL_SURFACE ( 'NONE', #1146, 88.00000000000000000 ) ;
#5205=CIRCLE ( 'NONE', #12241, 88.00000000000000000 ) ;
#5206=CARTESIAN_POINT ( 'NONE',  ( 10.00000000000000000, 83.03980459022454852, 18.42770452393382641 ) ) ;
#5207=ORIENTED_EDGE ( 'NONE', *, *, #1262, .T. ) ;
#5210=ORIENTED_EDGE ( 'NONE', *, *, #4655, .T. ) ;
#5211=AXIS2_PLACEMENT_3D ( 'NONE', #12756, #17529, #20839 ) ;
#5215=VECTOR ( 'NONE', #2690, 1000.000000000000000 ) ;
#5217=ORIENTED_EDGE ( 'NONE', *, *, #2414, .T. ) ;
#5220=DIRECTION ( 'NONE',  ( 0.000000000000000000, 0.000000000000000000, 1.000000000000000000 ) ) ;
#5222=CARTESIAN_POINT ( 'NONE',  ( 0.000000000000000000, 86.54587337002878655, 15.93147207947034971 ) ) ;
#5223=DIRECTION ( 'NONE',  ( -1.000000000000000000, 0.000000000000000000, 0.000000000000000000 ) ) ;
#5224=CARTESIAN_POINT ( 'NONE',  ( 0.000000000000000000, 57.47876254627143311, 62.70072803846409215 ) ) ;
#5225=FACE_OUTER_BOUND ( 'NONE', #13660, .T. ) ;
#5228=DIRECTION ( 'NONE',  ( -1.000000000000000000, -0.000000000000000000, -0.000000000000000000 ) ) ;
#5231=AXIS2_PLACEMENT_3D ( 'NONE', #4487, #1061, #7800 ) ;
#5235=DIRECTION ( 'NONE',  ( -1.000000000000000000, -0.000000000000000000, 0.000000000000000000 ) ) ;
#5237=ADVANCED_FACE ( 'NONE', ( #3012 ), #16379, .F. ) ;
#5239=ORIENTED_EDGE ( 'NONE', *, *, #18772, .T. ) ;
#5241=VECTOR ( 'NONE', #19441, 1000.000000000000000 ) ;
#5243=CARTESIAN_POINT ( 'NONE',  ( 10.00000000000000000, -81.55207211302061410, -24.17537951050148592 ) ) ;
#5244=VERTEX_POINT ( 'NONE', #4455 ) ;
#5245=AXIS2_PLACEMENT_3D ( 'NONE', #14708, #21455, #6337 ) ;
#5246=ORIENTED_EDGE ( 'NONE', *, *, #3937, .F. ) ;
#5250=EDGE_CURVE ( 'NONE', #16630, #13540, #12839, .T. ) ;
#5252=FACE_OUTER_BOUND ( 'NONE', #12753, .T. ) ;
#5253=CARTESIAN_POINT ( 'NONE',  ( 0.000000000000000000, -57.47876254627184522, 62.70072803846370135 ) ) ;
#5254=FACE_OUTER_BOUND ( 'NONE', #15752, .T. ) ;
#5255=DIRECTION ( 'NONE',  ( 0.000000000000000000, 0.000000000000000000, 1.000000000000000000 ) ) ;
#5259=CARTESIAN_POINT ( 'NONE',  ( 10.00000000000000000, 80.18694381077148137, -28.37681241246572483 ) ) ;
#5260=AXIS2_PLACEMENT_3D ( 'NONE', #10803, #12779, #2300 ) ;
#5262=AXIS2_PLACEMENT_3D ( 'NONE', #6397, #3173, #21725 ) ;
#5263=EDGE_LOOP ( 'NONE', ( #1447, #12934, #14925, #13349 ) ) ;
#5265=AXIS2_PLACEMENT_3D ( 'NONE', #870, #9252, #5638 ) ;
#5266=CARTESIAN_POINT ( 'NONE',  ( 10.00000000000000000, 0.000000000000000000, 0.000000000000000000 ) ) ;
#5267=ORIENTED_EDGE ( 'NONE', *, *, #15673, .F. ) ;
#5270=EDGE_CURVE ( 'NONE', #8367, #3730, #17628, .T. ) ;
#5272=ORIENTED_EDGE ( 'NONE', *, *, #19818, .T. ) ;
#5273=CARTESIAN_POINT ( 'NONE',  ( 10.00000000000000000, -48.19312842678424857, -70.09002648625245513 ) ) ;
#5274=VERTEX_POINT ( 'NONE', #16044 ) ;
#5277=CARTESIAN_POINT ( 'NONE',  ( 0.000000000000000000, -57.06999622551850138, 66.98518889142063415 ) ) ;
#5278=ORIENTED_EDGE ( 'NONE', *, *, #9812, .F. ) ;
#5280=CARTESIAN_POINT ( 'NONE',  ( 10.00000000000000000, 83.89484365856912973, 26.56417150042976161 ) ) ;
#5282=AXIS2_PLACEMENT_3D ( 'NONE', #17961, #12643, #9213 ) ;
#5285=AXIS2_PLACEMENT_3D ( 'NONE', #10250, #18872, #20430 ) ;
#5287=CARTESIAN_POINT ( 'NONE',  ( 5.000000000000000000, 79.38136668499741688, 37.98155635597341728 ) ) ;
#5288=EDGE_CURVE ( 'NONE', #20437, #17903, #7391, .T. ) ;
#5289=LINE ( 'NONE', #1851, #17568 ) ;
#5291=ORIENTED_EDGE ( 'NONE', *, *, #3566, .F. ) ;
#5292=ADVANCED_FACE ( 'NONE', ( #4238 ), #2900, .F. ) ;
#5293=DIRECTION ( 'NONE',  ( 0.000000000000000000, 0.000000000000000000, 1.000000000000000000 ) ) ;
#5294=CARTESIAN_POINT ( 'NONE',  ( 0.000000000000000000, 0.000000000000000000, 0.000000000000000000 ) ) ;
#5295=CARTESIAN_POINT ( 'NONE',  ( 10.00000000000000000, 0.000000000000000000, 0.000000000000000000 ) ) ;
#5296=ORIENTED_EDGE ( 'NONE', *, *, #2160, .F. ) ;
#5297=ADVANCED_FACE ( 'NONE', ( #18049 ), #6019, .F. ) ;
#5300=EDGE_LOOP ( 'NONE', ( #8478, #1385, #1863, #19510 ) ) ;
#5302=CYLINDRICAL_SURFACE ( 'NONE', #5591, 44.99999999999998579 ) ;
#5303=VECTOR ( 'NONE', #15192, 1000.000000000000000 ) ;
#5304=EDGE_LOOP ( 'NONE', ( #902, #15309, #18992, #558 ) ) ;
#5305=EDGE_CURVE ( 'NONE', #2378, #8708, #9497, .T. ) ;
#5308=CARTESIAN_POINT ( 'NONE',  ( 0.000000000000000000, 21.65267340503250537, 89.93106657554442052 ) ) ;
#5309=ORIENTED_EDGE ( 'NONE', *, *, #298, .F. ) ;
#5310=DIRECTION ( 'NONE',  ( 1.000000000000000000, 0.000000000000000000, 0.000000000000000000 ) ) ;
#5312=DIRECTION ( 'NONE',  ( -1.000000000000000000, 0.000000000000000000, 0.000000000000000000 ) ) ;
#5314=DIRECTION ( 'NONE',  ( 0.000000000000000000, 0.000000000000000000, 1.000000000000000000 ) ) ;
#5316=EDGE_CURVE ( 'NONE', #3086, #17425, #1754, .T. ) ;
#5320=ORIENTED_EDGE ( 'NONE', *, *, #7854, .F. ) ;
#5322=LINE ( 'NONE', #20773, #1635 ) ;
#5325=CARTESIAN_POINT ( 'NONE',  ( 10.00000000000000000, -71.33759994381919967, -58.88447872959059026 ) ) ;
#5328=CIRCLE ( 'NONE', #1441, 45.00000000000000000 ) ;
#5330=CARTESIAN_POINT ( 'NONE',  ( 0.000000000000000000, 0.000000000000000000, 0.000000000000000000 ) ) ;
#5331=ORIENTED_EDGE ( 'NONE', *, *, #8509, .F. ) ;
#5333=DIRECTION ( 'NONE',  ( -1.000000000000000000, 0.000000000000000000, -0.000000000000000000 ) ) ;
#5334=DIRECTION ( 'NONE',  ( -1.000000000000000000, 0.000000000000000000, -0.000000000000000000 ) ) ;
#5335=AXIS2_PLACEMENT_3D ( 'NONE', #8139, #21603, #3158 ) ;
#5336=DIRECTION ( 'NONE',  ( 0.000000000000000000, -0.4067366430758070917, 0.9135454576425978690 ) ) ;
#5339=DIRECTION ( 'NONE',  ( -1.000000000000000000, -0.000000000000000000, -0.000000000000000000 ) ) ;
#5341=VERTEX_POINT ( 'NONE', #1033 ) ;
#5343=DIRECTION ( 'NONE',  ( 1.000000000000000000, 0.000000000000000000, 0.000000000000000000 ) ) ;
#5344=FACE_OUTER_BOUND ( 'NONE', #14190, .T. ) ;
#5345=ORIENTED_EDGE ( 'NONE', *, *, #15969, .T. ) ;
#5346=DIRECTION ( 'NONE',  ( 0.000000000000000000, 0.000000000000000000, 1.000000000000000000 ) ) ;
#5347=ORIENTED_EDGE ( 'NONE', *, *, #8361, .F. ) ;
#5349=ORIENTED_EDGE ( 'NONE', *, *, #3102, .F. ) ;
#5350=CARTESIAN_POINT ( 'NONE',  ( 10.00000000000000000, 21.65267340503369198, -89.93106657554412209 ) ) ;
#5351=ORIENTED_EDGE ( 'NONE', *, *, #21212, .T. ) ;
#5352=VERTEX_POINT ( 'NONE', #12950 ) ;
#5357=DIRECTION ( 'NONE',  ( -1.000000000000000000, 0.000000000000000000, 0.000000000000000000 ) ) ;
#5358=DIRECTION ( 'NONE',  ( 1.000000000000000000, 0.000000000000000000, 0.000000000000000000 ) ) ;
#5359=CARTESIAN_POINT ( 'NONE',  ( 0.000000000000000000, 0.000000000000000000, 0.000000000000000000 ) ) ;
#5360=CARTESIAN_POINT ( 'NONE',  ( 5.000000000000002665, -5.479102470009884485, -87.82926298292120748 ) ) ;
#5361=CARTESIAN_POINT ( 'NONE',  ( 10.00000000000000000, 39.87723064937233630, -83.46401306393528330 ) ) ;
#5362=VERTEX_POINT ( 'NONE', #8104 ) ;
#5363=DIRECTION ( 'NONE',  ( 0.000000000000000000, 0.000000000000000000, 1.000000000000000000 ) ) ;
#5364=CARTESIAN_POINT ( 'NONE',  ( 0.000000000000000000, 36.39558101400137957, 80.12091913260394449 ) ) ;
#5365=VERTEX_POINT ( 'NONE', #8429 ) ;
#5366=DIRECTION ( 'NONE',  ( 0.000000000000000000, 0.000000000000000000, 1.000000000000000000 ) ) ;
#5367=ORIENTED_EDGE ( 'NONE', *, *, #5067, .T. ) ;
#5370=VERTEX_POINT ( 'NONE', #20363 ) ;
#5372=VERTEX_POINT ( 'NONE', #5222 ) ;
#5373=AXIS2_PLACEMENT_3D ( 'NONE', #19782, #5986, #12705 ) ;
#5375=VERTEX_POINT ( 'NONE', #18480 ) ;
#5377=VERTEX_POINT ( 'NONE', #6677 ) ;
#5378=CARTESIAN_POINT ( 'NONE',  ( 0.000000000000000000, -70.37753541435978377, 60.02863908169610596 ) ) ;
#5379=CYLINDRICAL_SURFACE ( 'NONE', #8648, 44.99999999999999289 ) ;
#5380=DIRECTION ( 'NONE',  ( 0.000000000000000000, 0.000000000000000000, 1.000000000000000000 ) ) ;
#5382=CARTESIAN_POINT ( 'NONE',  ( 0.000000000000000000, -57.06999622551760609, -66.98518889142141575 ) ) ;
#5383=CARTESIAN_POINT ( 'NONE',  ( 10.00000000000000000, 46.89573839703275127, 79.73220629831503459 ) ) ;
#5385=EDGE_CURVE ( 'NONE', #4539, #13627, #15152, .T. ) ;
#5386=DIRECTION ( 'NONE',  ( 0.000000000000000000, 0.000000000000000000, 1.000000000000000000 ) ) ;
#5387=CARTESIAN_POINT ( 'NONE',  ( -10.00000000000000000, 0.000000000000000000, 0.000000000000000000 ) ) ;
#5388=ORIENTED_EDGE ( 'NONE', *, *, #18097, .T. ) ;
#5389=CARTESIAN_POINT ( 'NONE',  ( 10.00000000000000000, -37.96946988134224910, 76.11510229470846411 ) ) ;
#5390=CIRCLE ( 'NONE', #8211, 92.50100000000000477 ) ;
#5393=AXIS2_PLACEMENT_3D ( 'NONE', #8902, #13786, #10673 ) ;
#5395=VERTEX_POINT ( 'NONE', #13489 ) ;
#5396=FACE_OUTER_BOUND ( 'NONE', #17597, .T. ) ;
#5397=ORIENTED_EDGE ( 'NONE', *, *, #16048, .T. ) ;
#5398=DIRECTION ( 'NONE',  ( -1.000000000000000000, -0.000000000000000000, 0.000000000000000000 ) ) ;
#5399=VERTEX_POINT ( 'NONE', #1795 ) ;
#5400=EDGE_CURVE ( 'NONE', #11838, #3976, #16932, .T. ) ;
#5404=CARTESIAN_POINT ( 'NONE',  ( 10.00000000000000000, 21.31452625070926743, 82.34610137166127686 ) ) ;
#5405=VECTOR ( 'NONE', #3098, 1000.000000000000000 ) ;
#5406=AXIS2_PLACEMENT_3D ( 'NONE', #2745, #4400, #17774 ) ;
#5408=DIRECTION ( 'NONE',  ( 1.000000000000000000, 0.000000000000000000, 0.000000000000000000 ) ) ;
#5413=CARTESIAN_POINT ( 'NONE',  ( 10.00000000000000000, 74.39348546125125949, -54.97312363261338675 ) ) ;
#5414=ADVANCED_FACE ( 'NONE', ( #3121 ), #15257, .F. ) ;
#5416=LINE ( 'NONE', #12253, #7228 ) ;
#5417=ADVANCED_FACE ( 'NONE', ( #3336 ), #11960, .F. ) ;
#5418=CYLINDRICAL_SURFACE ( 'NONE', #3427, 44.99999999999999289 ) ;
#5419=CARTESIAN_POINT ( 'NONE',  ( 0.000000000000000000, 60.65279801375343993, 63.75921967137637836 ) ) ;
#5421=STYLED_ITEM ( 'NONE', ( #9798 ), #6279 ) ;
#5422=ORIENTED_EDGE ( 'NONE', *, *, #7905, .T. ) ;
#5423=CARTESIAN_POINT ( 'NONE',  ( 0.000000000000000000, -92.22057093985034726, 7.197311757040199431 ) ) ;
#5424=AXIS2_PLACEMENT_3D ( 'NONE', #1928, #8671, #15401 ) ;
#5425=ORIENTED_EDGE ( 'NONE', *, *, #11470, .T. ) ;
#5426=CIRCLE ( 'NONE', #15285, 45.00000000000000711 ) ;
#5427=ORIENTED_EDGE ( 'NONE', *, *, #20008, .F. ) ;
#5429=LINE ( 'NONE', #18796, #7795 ) ;
#5432=EDGE_CURVE ( 'NONE', #15380, #2483, #11367, .T. ) ;
#5433=DIRECTION ( 'NONE',  ( 0.000000000000000000, 0.000000000000000000, 1.000000000000000000 ) ) ;
#5435=VERTEX_POINT ( 'NONE', #3560 ) ;
#5436=DIRECTION ( 'NONE',  ( -1.000000000000000000, -0.000000000000000000, -0.000000000000000000 ) ) ;
#5438=CARTESIAN_POINT ( 'NONE',  ( 10.00000000000000000, -8.925965667928249303, -92.06933331948791022 ) ) ;
#5444=DIRECTION ( 'NONE',  ( 0.000000000000000000, 0.000000000000000000, 1.000000000000000000 ) ) ;
#5447=CIRCLE ( 'NONE', #6519, 88.00000000000000000 ) ;
#5448=CARTESIAN_POINT ( 'NONE',  ( 0.000000000000000000, 0.000000000000000000, 0.000000000000000000 ) ) ;
#5449=EDGE_CURVE ( 'NONE', #18065, #16808, #11844, .T. ) ;
#5450=CIRCLE ( 'NONE', #17797, 44.99999999999998579 ) ;
#5452=ORIENTED_EDGE ( 'NONE', *, *, #9706, .T. ) ;
#5453=DIRECTION ( 'NONE',  ( 1.000000000000000000, 0.000000000000000000, 0.000000000000000000 ) ) ;
#5454=EDGE_CURVE ( 'NONE', #15310, #10766, #16601, .T. ) ;
#5458=DIRECTION ( 'NONE',  ( -1.000000000000000000, -0.000000000000000000, -0.000000000000000000 ) ) ;
#5460=ORIENTED_EDGE ( 'NONE', *, *, #13942, .T. ) ;
#5464=EDGE_CURVE ( 'NONE', #5588, #17357, #18381, .T. ) ;
#5465=CIRCLE ( 'NONE', #2279, 44.99999999999999289 ) ;
#5469=DIRECTION ( 'NONE',  ( 1.000000000000000000, -0.000000000000000000, -0.000000000000000000 ) ) ;
#5470=CARTESIAN_POINT ( 'NONE',  ( 10.00000000000000000, -41.87002153499058466, -74.04114219178087808 ) ) ;
#5471=AXIS2_PLACEMENT_3D ( 'NONE', #11577, #18329, #11245 ) ;
#5473=DIRECTION ( 'NONE',  ( -1.000000000000000000, 0.000000000000000000, -0.000000000000000000 ) ) ;
#5474=VECTOR ( 'NONE', #57, 1000.000000000000000 ) ;
#5475=EDGE_LOOP ( 'NONE', ( #9933, #9813, #20290, #13084 ) ) ;
#5480=ORIENTED_EDGE ( 'NONE', *, *, #17937, .T. ) ;
#5481=FACE_OUTER_BOUND ( 'NONE', #8617, .T. ) ;
#5482=CARTESIAN_POINT ( 'NONE',  ( 0.000000000000000000, 6.797690662956386021, -87.73705831432209834 ) ) ;
#5483=ORIENTED_EDGE ( 'NONE', *, *, #1666, .T. ) ;
#5484=VECTOR ( 'NONE', #19622, 1000.000000000000000 ) ;
#5487=ORIENTED_EDGE ( 'NONE', *, *, #5982, .F. ) ;
#5488=ORIENTED_EDGE ( 'NONE', *, *, #5550, .T. ) ;
#5489=DIRECTION ( 'NONE',  ( 1.000000000000000000, 0.000000000000000000, -0.000000000000000000 ) ) ;
#5490=ORIENTED_EDGE ( 'NONE', *, *, #11255, .F. ) ;
#5491=DIRECTION ( 'NONE',  ( -1.000000000000000000, 0.000000000000000000, -0.000000000000000000 ) ) ;
#5492=CARTESIAN_POINT ( 'NONE',  ( 10.00000000000000000, -8.134922360105496963, -84.67002113262489615 ) ) ;
#5493=DIRECTION ( 'NONE',  ( -1.000000000000000000, 0.000000000000000000, -0.000000000000000000 ) ) ;
#5494=LINE ( 'NONE', #12227, #8951 ) ;
#5495=DIRECTION ( 'NONE',  ( 0.000000000000000000, -0.2079116908177468526, -0.9781476007338083534 ) ) ;
#5496=AXIS2_PLACEMENT_3D ( 'NONE', #9507, #19358, #17923 ) ;
#5497=CARTESIAN_POINT ( 'NONE',  ( 10.00000000000000000, -88.70892494636754577, 26.21376805916555242 ) ) ;
#5500=VECTOR ( 'NONE', #13853, 1000.000000000000000 ) ;
#5502=AXIS2_PLACEMENT_3D ( 'NONE', #2224, #7525, #577 ) ;
#5503=CARTESIAN_POINT ( 'NONE',  ( 10.00000000000000000, -41.87002153499058466, -74.04114219178087808 ) ) ;
#5504=CARTESIAN_POINT ( 'NONE',  ( 0.000000000000000000, 0.000000000000000000, 0.000000000000000000 ) ) ;
#5508=CARTESIAN_POINT ( 'NONE',  ( -10.00000000000000000, 1.224646799147353217E-14, -100.0000000000000000 ) ) ;
#5509=ORIENTED_EDGE ( 'NONE', *, *, #5639, .F. ) ;
#5510=VERTEX_POINT ( 'NONE', #6778 ) ;
#5511=ADVANCED_FACE ( 'NONE', ( #18595 ), #7202, .F. ) ;
#5513=ORIENTED_EDGE ( 'NONE', *, *, #14040, .T. ) ;
#5516=FACE_OUTER_BOUND ( 'NONE', #13482, .T. ) ;
#5519=EDGE_CURVE ( 'NONE', #10355, #4606, #15607, .T. ) ;
#5520=DIRECTION ( 'NONE',  ( 0.000000000000000000, 0.000000000000000000, 1.000000000000000000 ) ) ;
#5521=DIRECTION ( 'NONE',  ( 0.000000000000000000, 0.000000000000000000, 1.000000000000000000 ) ) ;
#5522=CARTESIAN_POINT ( 'NONE',  ( 10.00000000000000000, 24.89070495400735794, 84.40647372620510680 ) ) ;
#5526=ORIENTED_EDGE ( 'NONE', *, *, #16538, .F. ) ;
#5528=EDGE_LOOP ( 'NONE', ( #13803, #11564, #700, #4557 ) ) ;
#5530=VERTEX_POINT ( 'NONE', #10617 ) ;
#5532=ORIENTED_EDGE ( 'NONE', *, *, #6218, .F. ) ;
#5533=EDGE_CURVE ( 'NONE', #17607, #4746, #7148, .T. ) ;
#5534=EDGE_CURVE ( 'NONE', #18366, #2155, #2123, .T. ) ;
#5535=EDGE_CURVE ( 'NONE', #13186, #10390, #1850, .T. ) ;
#5537=CARTESIAN_POINT ( 'NONE',  ( 10.00000000000000000, -84.19736439813830486, 38.30455363800902546 ) ) ;
#5538=VECTOR ( 'NONE', #1338, 1000.000000000000000 ) ;
#5540=ORIENTED_EDGE ( 'NONE', *, *, #6527, .F. ) ;
#5541=VECTOR ( 'NONE', #14775, 1000.000000000000000 ) ;
#5544=CARTESIAN_POINT ( 'NONE',  ( 10.00000000000000000, -71.72924546249979016, 45.71766382684644725 ) ) ;
#5547=FACE_OUTER_BOUND ( 'NONE', #15881, .T. ) ;
#5549=CARTESIAN_POINT ( 'NONE',  ( 10.00000000000000000, 0.000000000000000000, 0.000000000000000000 ) ) ;
#5550=EDGE_CURVE ( 'NONE', #13354, #10036, #5733, .T. ) ;
#5552=ORIENTED_EDGE ( 'NONE', *, *, #12465, .F. ) ;
#5557=VECTOR ( 'NONE', #838, 1000.000000000000000 ) ;
#5560=EDGE_CURVE ( 'NONE', #12130, #2487, #19838, .T. ) ;
#5563=DIRECTION ( 'NONE',  ( -1.000000000000000000, 0.000000000000000000, 0.000000000000000000 ) ) ;
#5564=EDGE_CURVE ( 'NONE', #6428, #21294, #20895, .T. ) ;
#5566=ORIENTED_EDGE ( 'NONE', *, *, #14870, .T. ) ;
#5569=VECTOR ( 'NONE', #7469, 1000.000000000000000 ) ;
#5571=DIRECTION ( 'NONE',  ( -1.000000000000000000, -0.000000000000000000, -0.000000000000000000 ) ) ;
#5572=AXIS2_PLACEMENT_3D ( 'NONE', #13947, #15498, #8759 ) ;
#5573=DIRECTION ( 'NONE',  ( -1.000000000000000000, -0.000000000000000000, -0.000000000000000000 ) ) ;
#5575=DIRECTION ( 'NONE',  ( 0.000000000000000000, 0.000000000000000000, 1.000000000000000000 ) ) ;
#5576=AXIS2_PLACEMENT_3D ( 'NONE', #7784, #15853, #713 ) ;
#5578=CYLINDRICAL_SURFACE ( 'NONE', #10987, 92.50100000000000477 ) ;
#5579=ADVANCED_FACE ( 'NONE', ( #9065 ), #17149, .F. ) ;
#5580=ORIENTED_EDGE ( 'NONE', *, *, #3282, .F. ) ;
#5581=ADVANCED_FACE ( 'NONE', ( #20473 ), #4102, .F. ) ;
#5585=EDGE_CURVE ( 'NONE', #2910, #13186, #11732, .T. ) ;
#5587=DIRECTION ( 'NONE',  ( 1.000000000000000000, 0.000000000000000000, 0.000000000000000000 ) ) ;
#5588=VERTEX_POINT ( 'NONE', #17479 ) ;
#5589=AXIS2_PLACEMENT_3D ( 'NONE', #17686, #17908, #11273 ) ;
#5590=CARTESIAN_POINT ( 'NONE',  ( 10.00000000000000000, 0.000000000000000000, 0.000000000000000000 ) ) ;
#5591=AXIS2_PLACEMENT_3D ( 'NONE', #18880, #20857, #1975 ) ;
#5592=VECTOR ( 'NONE', #9083, 1000.000000000000000 ) ;
#5593=CARTESIAN_POINT ( 'NONE',  ( 10.00000000000000000, -41.87002153499162915, 74.04114219178029543 ) ) ;
#5594=CIRCLE ( 'NONE', #20058, 44.99999999999999289 ) ;
#5596=ORIENTED_EDGE ( 'NONE', *, *, #3911, .F. ) ;
#5600=CARTESIAN_POINT ( 'NONE',  ( 10.00000000000000000, 0.000000000000000000, 0.000000000000000000 ) ) ;
#5602=LINE ( 'NONE', #4371, #12147 ) ;
#5605=DIRECTION ( 'NONE',  ( 0.000000000000000000, 0.000000000000000000, 1.000000000000000000 ) ) ;
#5607=AXIS2_PLACEMENT_3D ( 'NONE', #5846, #9357, #15990 ) ;
#5608=VECTOR ( 'NONE', #2789, 1000.000000000000000 ) ;
#5610=CIRCLE ( 'NONE', #16904, 92.50100000000000477 ) ;
#5611=ORIENTED_EDGE ( 'NONE', *, *, #14484, .T. ) ;
#5612=AXIS2_PLACEMENT_3D ( 'NONE', #11827, #18691, #8514 ) ;
#5613=CARTESIAN_POINT ( 'NONE',  ( 0.000000000000000000, 78.80192417387927151, 39.16958956249325752 ) ) ;
#5614=FACE_OUTER_BOUND ( 'NONE', #816, .T. ) ;
#5615=ADVANCED_FACE ( 'NONE', ( #3987 ), #10723, .F. ) ;
#5617=VERTEX_POINT ( 'NONE', #18127 ) ;
#5618=DIRECTION ( 'NONE',  ( -1.000000000000000000, 0.000000000000000000, 0.000000000000000000 ) ) ;
#5619=VERTEX_POINT ( 'NONE', #7519 ) ;
#5621=ORIENTED_EDGE ( 'NONE', *, *, #11259, .F. ) ;
#5622=VECTOR ( 'NONE', #8159, 1000.000000000000000 ) ;
#5623=VERTEX_POINT ( 'NONE', #21322 ) ;
#5629=EDGE_LOOP ( 'NONE', ( #430, #9582, #662, #2316 ) ) ;
#5631=DIRECTION ( 'NONE',  ( -1.000000000000000000, 0.000000000000000000, -0.000000000000000000 ) ) ;
#5633=CYLINDRICAL_SURFACE ( 'NONE', #11031, 44.99999999999998579 ) ;
#5634=CARTESIAN_POINT ( 'NONE',  ( 0.000000000000000000, -91.49386717542229519, 13.61276130276963592 ) ) ;
#5635=CYLINDRICAL_SURFACE ( 'NONE', #15428, 92.50100000000000477 ) ;
#5636=DIRECTION ( 'NONE',  ( 0.000000000000000000, 0.1391731009600589986, 0.9902680687415711391 ) ) ;
#5638=DIRECTION ( 'NONE',  ( 0.000000000000000000, 0.9510565162951521989, 0.3090169943749514481 ) ) ;
#5639=EDGE_CURVE ( 'NONE', #19613, #454, #886, .T. ) ;
#5640=CIRCLE ( 'NONE', #3526, 88.00000000000000000 ) ;
#5641=ORIENTED_EDGE ( 'NONE', *, *, #18514, .T. ) ;
#5642=CIRCLE ( 'NONE', #19405, 92.50100000000000477 ) ;
#5643=CARTESIAN_POINT ( 'NONE',  ( 0.000000000000000000, -72.53479564998751528, -44.42851404693431761 ) ) ;
#5645=ORIENTED_EDGE ( 'NONE', *, *, #670, .T. ) ;
#5646=PRODUCT_DEFINITION ( 'UNKNOWN', '', #5728, #12249 ) ;
#5647=ORIENTED_EDGE ( 'NONE', *, *, #19154, .T. ) ;
#5648=DIRECTION ( 'NONE',  ( 0.000000000000000000, 0.000000000000000000, 1.000000000000000000 ) ) ;
#5650=ORIENTED_EDGE ( 'NONE', *, *, #13213, .T. ) ;
#5651=DIRECTION ( 'NONE',  ( -1.000000000000000000, 0.000000000000000000, 0.000000000000000000 ) ) ;
#5652=ORIENTED_EDGE ( 'NONE', *, *, #12825, .T. ) ;
#5653=AXIS2_PLACEMENT_3D ( 'NONE', #15382, #259, #3790 ) ;
#5654=DIRECTION ( 'NONE',  ( -1.000000000000000000, 0.000000000000000000, 0.000000000000000000 ) ) ;
#5657=CARTESIAN_POINT ( 'NONE',  ( 10.00000000000000000, 0.000000000000000000, 0.000000000000000000 ) ) ;
#5659=DIRECTION ( 'NONE',  ( 0.000000000000000000, 0.000000000000000000, 1.000000000000000000 ) ) ;
#5660=CARTESIAN_POINT ( 'NONE',  ( 10.00000000000000000, -87.17509410653646285, 30.93441398372555540 ) ) ;
#5661=DIRECTION ( 'NONE',  ( -1.000000000000000000, -0.000000000000000000, -0.000000000000000000 ) ) ;
#5663=ORIENTED_EDGE ( 'NONE', *, *, #20802, .F. ) ;
#5664=CIRCLE ( 'NONE', #8149, 44.99999999999999289 ) ;
#5667=ORIENTED_EDGE ( 'NONE', *, *, #8275, .F. ) ;
#5668=CARTESIAN_POINT ( 'NONE',  ( 0.000000000000000000, 0.000000000000000000, 0.000000000000000000 ) ) ;
#5669=ORIENTED_EDGE ( 'NONE', *, *, #13896, .F. ) ;
#5671=EDGE_CURVE ( 'NONE', #16156, #12184, #1499, .T. ) ;
#5672=CARTESIAN_POINT ( 'NONE',  ( 10.00000000000000000, -78.01214607583776228, 33.90124636420084414 ) ) ;
#5673=ORIENTED_EDGE ( 'NONE', *, *, #15577, .T. ) ;
#5674=ORIENTED_EDGE ( 'NONE', *, *, #14559, .F. ) ;
#5676=CARTESIAN_POINT ( 'NONE',  ( -10.00000000000000000, 0.000000000000000000, 0.000000000000000000 ) ) ;
#5677=DIRECTION ( 'NONE',  ( 1.000000000000000000, -0.000000000000000000, 0.000000000000000000 ) ) ;
#5678=DIRECTION ( 'NONE',  ( 0.000000000000000000, 0.000000000000000000, 1.000000000000000000 ) ) ;
#5680=CARTESIAN_POINT ( 'NONE',  ( 10.00000000000000000, 19.83954325428658194, 82.71385593638699163 ) ) ;
#5682=CARTESIAN_POINT ( 'NONE',  ( 0.000000000000000000, 84.12297548659721258, -12.59025161327029529 ) ) ;
#5684=EDGE_CURVE ( 'NONE', #20304, #20166, #8203, .T. ) ;
#5687=DIRECTION ( 'NONE',  ( -1.000000000000000000, 0.000000000000000000, 0.000000000000000000 ) ) ;
#5689=ORIENTED_EDGE ( 'NONE', *, *, #12828, .T. ) ;
#5691=VERTEX_POINT ( 'NONE', #17796 ) ;
#5696=ORIENTED_EDGE ( 'NONE', *, *, #15173, .T. ) ;
#5697=SHAPE_REPRESENTATION_RELATIONSHIP ( 'NONE' , 'NONE' ,  #6721, #11474 ) ;
#5701=EDGE_LOOP ( 'NONE', ( #17091, #1510, #14691, #9545 ) ) ;
#5702=CARTESIAN_POINT ( 'NONE',  ( 0.000000000000000000, 90.32141448704707898, -19.96189084378133316 ) ) ;
#5705=ADVANCED_FACE ( 'NONE', ( #2653 ), #17914, .F. ) ;
#5708=CARTESIAN_POINT ( 'NONE',  ( 10.00000000000000000, 88.70892494636740366, 26.21376805916615282 ) ) ;
#5711=FACE_OUTER_BOUND ( 'NONE', #20940, .T. ) ;
#5712=CIRCLE ( 'NONE', #1830, 88.00000000000000000 ) ;
#5714=ORIENTED_EDGE ( 'NONE', *, *, #12827, .T. ) ;
#5715=LINE ( 'NONE', #629, #15156 ) ;
#5716=EDGE_CURVE ( 'NONE', #5365, #282, #14920, .T. ) ;
#5719=CARTESIAN_POINT ( 'NONE',  ( 10.00000000000000000, 0.000000000000000000, 0.000000000000000000 ) ) ;
#5720=ORIENTED_EDGE ( 'NONE', *, *, #21229, .T. ) ;
#5722=ORIENTED_EDGE ( 'NONE', *, *, #8001, .T. ) ;
#5723=LINE ( 'NONE', #5508, #1362 ) ;
#5724=VERTEX_POINT ( 'NONE', #9593 ) ;
#5726=ORIENTED_EDGE ( 'NONE', *, *, #18676, .F. ) ;
#5727=EDGE_LOOP ( 'NONE', ( #16650, #17474, #3625, #7744 ) ) ;
#5728=PRODUCT_DEFINITION_FORMATION_WITH_SPECIFIED_SOURCE ( 'ANY', '', #1745, .NOT_KNOWN. ) ;
#5729=CARTESIAN_POINT ( 'NONE',  ( 10.00000000000000000, 84.79630770241084292, -6.691460262315676033 ) ) ;
#5731=EDGE_LOOP ( 'NONE', ( #10692, #17824, #13787, #20774 ) ) ;
#5732=DIRECTION ( 'NONE',  ( 0.000000000000000000, -0.6946583704590033603, 0.7193398003386453077 ) ) ;
#5733=CIRCLE ( 'NONE', #19491, 88.00000000000000000 ) ;
#5735=CARTESIAN_POINT ( 'NONE',  ( 5.000000000000002665, -11.59241532900569993, -87.23311244498751194 ) ) ;
#5736=EDGE_CURVE ( 'NONE', #9520, #10561, #4682, .T. ) ;
#5738=EDGE_CURVE ( 'NONE', #8283, #2619, #11383, .T. ) ;
#5740=CYLINDRICAL_SURFACE ( 'NONE', #20913, 92.50100000000000477 ) ;
#5741=LINE ( 'NONE', #9248, #13294 ) ;
#5742=DIRECTION ( 'NONE',  ( -1.000000000000000000, 0.000000000000000000, 0.000000000000000000 ) ) ;
#5743=CIRCLE ( 'NONE', #8562, 92.50100000000000477 ) ;
#5744=CARTESIAN_POINT ( 'NONE',  ( 10.00000000000000000, 57.53593069156472239, -72.42963261300903355 ) ) ;
#5745=CARTESIAN_POINT ( 'NONE',  ( 5.000000000000000000, 51.18896083639367589, -71.57995730992126937 ) ) ;
#5747=FACE_OUTER_BOUND ( 'NONE', #10394, .T. ) ;
#5748=ORIENTED_EDGE ( 'NONE', *, *, #11376, .F. ) ;
#5749=CIRCLE ( 'NONE', #14556, 88.00000000000000000 ) ;
#5751=ORIENTED_EDGE ( 'NONE', *, *, #20575, .F. ) ;
#5753=VECTOR ( 'NONE', #12247, 1000.000000000000000 ) ;
#5754=VERTEX_POINT ( 'NONE', #16246 ) ;
#5755=ORIENTED_EDGE ( 'NONE', *, *, #969, .F. ) ;
#5756=AXIS2_PLACEMENT_3D ( 'NONE', #2136, #12299, #20812 ) ;
#5757=ORIENTED_EDGE ( 'NONE', *, *, #5533, .T. ) ;
#5758=DIRECTION ( 'NONE',  ( -1.000000000000000000, 0.000000000000000000, 0.000000000000000000 ) ) ;
#5759=AXIS2_PLACEMENT_3D ( 'NONE', #15818, #17799, #7425 ) ;
#5760=ORIENTED_EDGE ( 'NONE', *, *, #18758, .F. ) ;
#5762=DIRECTION ( 'NONE',  ( 1.000000000000000000, 0.000000000000000000, 0.000000000000000000 ) ) ;
#5763=CIRCLE ( 'NONE', #4352, 45.00000000000000000 ) ;
#5765=CARTESIAN_POINT ( 'NONE',  ( -10.00000000000000000, 0.000000000000000000, 0.000000000000000000 ) ) ;
#5767=FACE_OUTER_BOUND ( 'NONE', #9508, .T. ) ;
#5769=VECTOR ( 'NONE', #18840, 1000.000000000000000 ) ;
#5770=VECTOR ( 'NONE', #16439, 1000.000000000000000 ) ;
#5772=CIRCLE ( 'NONE', #16342, 45.00000000000000000 ) ;
#5774=CARTESIAN_POINT ( 'NONE',  ( 5.000000000000000000, -41.89587599971492438, -77.38692120905515992 ) ) ;
#5776=CIRCLE ( 'NONE', #3655, 44.99999999999999289 ) ;
#5777=VERTEX_POINT ( 'NONE', #16348 ) ;
#5778=DIRECTION ( 'NONE',  ( 1.000000000000000000, 0.000000000000000000, 0.000000000000000000 ) ) ;
#5779=ORIENTED_EDGE ( 'NONE', *, *, #16193, .T. ) ;
#5780=VECTOR ( 'NONE', #8208, 1000.000000000000000 ) ;
#5782=VERTEX_POINT ( 'NONE', #1219 ) ;
#5783=EDGE_CURVE ( 'NONE', #16840, #4926, #8075, .T. ) ;
#5784=ORIENTED_EDGE ( 'NONE', *, *, #2437, .F. ) ;
#5786=AXIS2_PLACEMENT_3D ( 'NONE', #16520, #4481, #17856 ) ;
#5788=DIRECTION ( 'NONE',  ( -1.000000000000000000, -0.000000000000000000, 0.000000000000000000 ) ) ;
#5790=CARTESIAN_POINT ( 'NONE',  ( 10.00000000000000000, 41.87002153499110335, 74.04114219178059386 ) ) ;
#5791=CARTESIAN_POINT ( 'NONE',  ( 5.000000000000002665, 24.89070495400845573, -84.40647372620476574 ) ) ;
#5794=CARTESIAN_POINT ( 'NONE',  ( 10.00000000000000000, 86.66425444033963288, -32.33793443156312009 ) ) ;
#5795=DIRECTION ( 'NONE',  ( 0.000000000000000000, 0.000000000000000000, 1.000000000000000000 ) ) ;
#5796=CIRCLE ( 'NONE', #9321, 92.50100000000000477 ) ;
#5798=FACE_OUTER_BOUND ( 'NONE', #1327, .T. ) ;
#5799=AXIS2_PLACEMENT_3D ( 'NONE', #16294, #6377, #16632 ) ;
#5801=VECTOR ( 'NONE', #20030, 1000.000000000000000 ) ;
#5803=ORIENTED_EDGE ( 'NONE', *, *, #13234, .T. ) ;
#5804=LINE ( 'NONE', #3819, #12318 ) ;
#5805=FACE_OUTER_BOUND ( 'NONE', #10011, .T. ) ;
#5809=VERTEX_POINT ( 'NONE', #11495 ) ;
#5811=EDGE_CURVE ( 'NONE', #12482, #21814, #16796, .T. ) ;
#5813=EDGE_CURVE ( 'NONE', #13984, #16102, #13140, .T. ) ;
#5814=ORIENTED_EDGE ( 'NONE', *, *, #20119, .F. ) ;
#5816=PLANE ( 'NONE',  #11777 ) ;
#5818=ORIENTED_EDGE ( 'NONE', *, *, #8163, .F. ) ;
#5819=AXIS2_PLACEMENT_3D ( 'NONE', #270, #15184, #3255 ) ;
#5820=EDGE_CURVE ( 'NONE', #5724, #17876, #19886, .T. ) ;
#5821=DIRECTION ( 'NONE',  ( 0.000000000000000000, -0.6946583704589885944, -0.7193398003386594075 ) ) ;
#5822=LINE ( 'NONE', #4041, #7002 ) ;
#5824=CARTESIAN_POINT ( 'NONE',  ( 10.00000000000000000, -83.03980459022467642, -18.42770452393328995 ) ) ;
#5826=CARTESIAN_POINT ( 'NONE',  ( 0.000000000000000000, 79.38136668499790005, -37.98155635597233726 ) ) ;
#5827=ORIENTED_EDGE ( 'NONE', *, *, #18676, .T. ) ;
#5828=DIRECTION ( 'NONE',  ( 0.000000000000000000, 0.000000000000000000, 1.000000000000000000 ) ) ;
#5829=EDGE_CURVE ( 'NONE', #18262, #21840, #15024, .T. ) ;
#5831=CARTESIAN_POINT ( 'NONE',  ( 10.00000000000000000, -3.974475837764312569, -92.41557521768193340 ) ) ;
#5836=ORIENTED_EDGE ( 'NONE', *, *, #6411, .F. ) ;
#5843=AXIS2_PLACEMENT_3D ( 'NONE', #7903, #16521, #3251 ) ;
#5844=DIRECTION ( 'NONE',  ( -1.000000000000000000, -0.000000000000000000, 0.000000000000000000 ) ) ;
#5846=CARTESIAN_POINT ( 'NONE',  ( 10.00000000000000000, 72.53479564998782791, 44.42851404693380601 ) ) ;
#5849=CARTESIAN_POINT ( 'NONE',  ( 0.000000000000000000, -67.05625154133410604, -63.71729851637880415 ) ) ;
#5852=DIRECTION ( 'NONE',  ( 0.000000000000000000, -0.2756373558170063798, 0.9612616959383167847 ) ) ;
#5853=AXIS2_PLACEMENT_3D ( 'NONE', #15289, #167, #3910 ) ;
#5855=DIRECTION ( 'NONE',  ( 0.000000000000000000, 0.000000000000000000, 1.000000000000000000 ) ) ;
#5857=LINE ( 'NONE', #15902, #12608 ) ;
#5858=DIRECTION ( 'NONE',  ( -1.000000000000000000, -0.000000000000000000, -0.000000000000000000 ) ) ;
#5860=ADVANCED_FACE ( 'NONE', ( #2980 ), #8405, .F. ) ;
#5864=VERTEX_POINT ( 'NONE', #6430 ) ;
#5865=EDGE_CURVE ( 'NONE', #966, #6505, #5749, .T. ) ;
#5866=AXIS2_PLACEMENT_3D ( 'NONE', #3918, #10872, #10647 ) ;
#5867=CIRCLE ( 'NONE', #3053, 92.50100000000003320 ) ;
#5869=ORIENTED_EDGE ( 'NONE', *, *, #11821, .F. ) ;
#5873=CARTESIAN_POINT ( 'NONE',  ( 10.00000000000000000, 32.56745702629739014, 78.57830605990665163 ) ) ;
#5874=VERTEX_POINT ( 'NONE', #18358 ) ;
#5875=CARTESIAN_POINT ( 'NONE',  ( 0.000000000000000000, 35.18804927320642406, -80.65854690202642985 ) ) ;
#5876=DIRECTION ( 'NONE',  ( 0.000000000000000000, 0.000000000000000000, 1.000000000000000000 ) ) ;
#5878=DIRECTION ( 'NONE',  ( -1.000000000000000000, -0.000000000000000000, -0.000000000000000000 ) ) ;
#5881=CIRCLE ( 'NONE', #16820, 44.99999999999999289 ) ;
#5882=DIRECTION ( 'NONE',  ( 1.000000000000000000, 0.000000000000000000, 0.000000000000000000 ) ) ;
#5883=LINE ( 'NONE', #10949, #19802 ) ;
#5886=CARTESIAN_POINT ( 'NONE',  ( 0.000000000000000000, 81.34229909304724515, -33.57723005635285318 ) ) ;
#5887=CYLINDRICAL_SURFACE ( 'NONE', #9449, 92.50100000000000477 ) ;
#5888=AXIS2_PLACEMENT_3D ( 'NONE', #18031, #2879, #9599 ) ;
#5889=DIRECTION ( 'NONE',  ( 0.000000000000000000, 0.9702957262759954737, 0.2419218955996715048 ) ) ;
#5890=ORIENTED_EDGE ( 'NONE', *, *, #3966, .F. ) ;
#5891=AXIS2_PLACEMENT_3D ( 'NONE', #9481, #17572, #19433 ) ;
#5892=CARTESIAN_POINT ( 'NONE',  ( 0.000000000000000000, 0.000000000000000000, 0.000000000000000000 ) ) ;
#5893=VERTEX_POINT ( 'NONE', #3202 ) ;
#5894=AXIS2_PLACEMENT_3D ( 'NONE', #11167, #14588, #13257 ) ;
#5895=DIRECTION ( 'NONE',  ( 1.000000000000000000, 0.000000000000000000, 0.000000000000000000 ) ) ;
#5897=VERTEX_POINT ( 'NONE', #1768 ) ;
#5899=CARTESIAN_POINT ( 'NONE',  ( 10.00000000000000000, 8.134922360106093819, 84.67002113262482510 ) ) ;
#5900=CARTESIAN_POINT ( 'NONE',  ( 10.00000000000000000, 87.17509410653623547, 30.93441398372612738 ) ) ;
#5901=DIRECTION ( 'NONE',  ( -1.000000000000000000, -0.000000000000000000, -0.000000000000000000 ) ) ;
#5902=CARTESIAN_POINT ( 'NONE',  ( 0.000000000000000000, 87.17509410653623547, 30.93441398372613094 ) ) ;
#5903=CYLINDRICAL_SURFACE ( 'NONE', #19193, 44.99999999999998579 ) ;
#5904=CARTESIAN_POINT ( 'NONE',  ( 5.000000000000000000, -72.58367602204218372, 49.75550195834843237 ) ) ;
#5905=FACE_OUTER_BOUND ( 'NONE', #19801, .T. ) ;
#5906=CARTESIAN_POINT ( 'NONE',  ( 0.000000000000000000, -78.04699792498111321, -49.64978465107371619 ) ) ;
#5908=AXIS2_PLACEMENT_3D ( 'NONE', #18224, #13120, #6072 ) ;
#5910=EDGE_CURVE ( 'NONE', #3795, #20360, #2220, .T. ) ;
#5912=CARTESIAN_POINT ( 'NONE',  ( 10.00000000000000000, 29.29369617358468858, 87.74003855418408193 ) ) ;
#5915=ORIENTED_EDGE ( 'NONE', *, *, #13788, .F. ) ;
#5919=ORIENTED_EDGE ( 'NONE', *, *, #6598, .T. ) ;
#5920=ORIENTED_EDGE ( 'NONE', *, *, #9361, .T. ) ;
#5921=CIRCLE ( 'NONE', #15444, 44.99999999999999289 ) ;
#5922=ORIENTED_EDGE ( 'NONE', *, *, #785, .T. ) ;
#5923=FACE_OUTER_BOUND ( 'NONE', #13802, .T. ) ;
#5924=CARTESIAN_POINT ( 'NONE',  ( 0.000000000000000000, -36.39558101400082535, -80.12091913260421450 ) ) ;
#5925=CIRCLE ( 'NONE', #1683, 92.50100000000000477 ) ;
#5927=DIRECTION ( 'NONE',  ( 0.000000000000000000, 0.000000000000000000, 1.000000000000000000 ) ) ;
#5928=CARTESIAN_POINT ( 'NONE',  ( 0.000000000000000000, 78.83848282823974785, -48.38314403117421847 ) ) ;
#5930=CARTESIAN_POINT ( 'NONE',  ( 0.000000000000000000, -90.63195040374199607, 18.50093422002390398 ) ) ;
#5932=LINE ( 'NONE', #14537, #20156 ) ;
#5933=ORIENTED_EDGE ( 'NONE', *, *, #10816, .T. ) ;
#5934=DIRECTION ( 'NONE',  ( 1.000000000000000000, 0.000000000000000000, 0.000000000000000000 ) ) ;
#5935=CIRCLE ( 'NONE', #18293, 88.00000000000000000 ) ;
#5938=EDGE_CURVE ( 'NONE', #20049, #20543, #795, .T. ) ;
#5939=VECTOR ( 'NONE', #20260, 1000.000000000000000 ) ;
#5940=EDGE_CURVE ( 'NONE', #20731, #10690, #16684, .T. ) ;
#5941=VECTOR ( 'NONE', #947, 1000.000000000000000 ) ;
#5942=AXIS2_PLACEMENT_3D ( 'NONE', #18057, #18166, #19922 ) ;
#5943=DIRECTION ( 'NONE',  ( 1.000000000000000000, 0.000000000000000000, 0.000000000000000000 ) ) ;
#5944=EDGE_LOOP ( 'NONE', ( #2383, #16208, #18677, #4531 ) ) ;
#5945=DIRECTION ( 'NONE',  ( 0.000000000000000000, 0.000000000000000000, 1.000000000000000000 ) ) ;
#5949=ORIENTED_EDGE ( 'NONE', *, *, #15940, .F. ) ;
#5950=VERTEX_POINT ( 'NONE', #12362 ) ;
#5951=CARTESIAN_POINT ( 'NONE',  ( 10.00000000000000000, 3.974475837764916530, 92.41557521768191918 ) ) ;
#5952=ORIENTED_EDGE ( 'NONE', *, *, #3381, .T. ) ;
#5954=DIRECTION ( 'NONE',  ( 1.000000000000000000, 0.000000000000000000, 0.000000000000000000 ) ) ;
#5956=CARTESIAN_POINT ( 'NONE',  ( 0.000000000000000000, 0.000000000000000000, 0.000000000000000000 ) ) ;
#5957=CARTESIAN_POINT ( 'NONE',  ( 10.00000000000000000, 0.000000000000000000, 88.00000000000000000 ) ) ;
#5960=AXIS2_PLACEMENT_3D ( 'NONE', #17696, #5661, #19243 ) ;
#5963=DIRECTION ( 'NONE',  ( 1.000000000000000000, 0.000000000000000000, 0.000000000000000000 ) ) ;
#5964=DIRECTION ( 'NONE',  ( 1.000000000000000000, 0.000000000000000000, 0.000000000000000000 ) ) ;
#5967=EDGE_CURVE ( 'NONE', #19371, #17637, #17383, .T. ) ;
#5968=ADVANCED_FACE ( 'NONE', ( #8833 ), #18780, .F. ) ;
#5971=CARTESIAN_POINT ( 'NONE',  ( 10.00000000000000000, 0.000000000000000000, 0.000000000000000000 ) ) ;
#5973=ORIENTED_EDGE ( 'NONE', *, *, #687, .T. ) ;
#5975=AXIS2_PLACEMENT_3D ( 'NONE', #6059, #6168, #6286 ) ;
#5976=ORIENTED_EDGE ( 'NONE', *, *, #4878, .F. ) ;
#5978=AXIS2_PLACEMENT_3D ( 'NONE', #18789, #13814, #3318 ) ;
#5979=ORIENTED_EDGE ( 'NONE', *, *, #8390, .F. ) ;
#5980=EDGE_LOOP ( 'NONE', ( #20337, #14267, #5645, #19824 ) ) ;
#5981=ORIENTED_EDGE ( 'NONE', *, *, #18430, .T. ) ;
#5982=EDGE_CURVE ( 'NONE', #1182, #20772, #9255, .T. ) ;
#5984=LINE ( 'NONE', #16242, #5241 ) ;
#5985=ORIENTED_EDGE ( 'NONE', *, *, #9312, .T. ) ;
#5986=DIRECTION ( 'NONE',  ( -1.000000000000000000, -0.000000000000000000, -0.000000000000000000 ) ) ;
#5987=EDGE_CURVE ( 'NONE', #8524, #21192, #8726, .T. ) ;
#5993=VECTOR ( 'NONE', #8218, 1000.000000000000000 ) ;
#5996=VECTOR ( 'NONE', #12018, 1000.000000000000000 ) ;
#5998=CARTESIAN_POINT ( 'NONE',  ( 10.00000000000000000, 0.000000000000000000, 0.000000000000000000 ) ) ;
#5999=CARTESIAN_POINT ( 'NONE',  ( 10.00000000000000000, 65.83713140174729972, 58.39068529131218099 ) ) ;
#6001=ORIENTED_EDGE ( 'NONE', *, *, #17695, .T. ) ;
#6002=DIRECTION ( 'NONE',  ( 1.000000000000000000, 0.000000000000000000, 0.000000000000000000 ) ) ;
#6009=CARTESIAN_POINT ( 'NONE',  ( 0.000000000000000000, 61.33825423015685629, 69.23910433415966281 ) ) ;
#6010=VERTEX_POINT ( 'NONE', #6970 ) ;
#6011=CIRCLE ( 'NONE', #18363, 45.00000000000000711 ) ;
#6014=LINE ( 'NONE', #2797, #12120 ) ;
#6015=ORIENTED_EDGE ( 'NONE', *, *, #10086, .F. ) ;
#6016=VERTEX_POINT ( 'NONE', #3750 ) ;
#6017=LINE ( 'NONE', #17715, #1225 ) ;
#6018=ADVANCED_FACE ( 'NONE', ( #2099 ), #5633, .F. ) ;
#6019=CYLINDRICAL_SURFACE ( 'NONE', #17994, 44.99999999999999289 ) ;
#6020=DIRECTION ( 'NONE',  ( -1.000000000000000000, 0.000000000000000000, -0.000000000000000000 ) ) ;
#6021=LINE ( 'NONE', #19477, #291 ) ;
#6023=DIRECTION ( 'NONE',  ( 0.000000000000000000, 0.5877852522924740253, -0.8090169943749466741 ) ) ;
#6025=DIRECTION ( 'NONE',  ( 0.000000000000000000, 0.9510565162951523099, 0.3090169943749513926 ) ) ;
#6026=CYLINDRICAL_SURFACE ( 'NONE', #5133, 92.50100000000000477 ) ;
#6027=FACE_OUTER_BOUND ( 'NONE', #6369, .T. ) ;
#6031=ORIENTED_EDGE ( 'NONE', *, *, #17033, .F. ) ;
#6032=DIRECTION ( 'NONE',  ( 0.000000000000000000, 0.000000000000000000, 1.000000000000000000 ) ) ;
#6034=FACE_OUTER_BOUND ( 'NONE', #4119, .T. ) ;
#6036=ORIENTED_EDGE ( 'NONE', *, *, #13525, .T. ) ;
#6037=ORIENTED_EDGE ( 'NONE', *, *, #12107, .T. ) ;
#6038=ORIENTED_EDGE ( 'NONE', *, *, #2972, .F. ) ;
#6039=AXIS2_PLACEMENT_3D ( 'NONE', #18209, #19521, #16547 ) ;
#6040=CARTESIAN_POINT ( 'NONE',  ( 0.000000000000000000, 0.000000000000000000, 0.000000000000000000 ) ) ;
#6045=DIRECTION ( 'NONE',  ( 0.000000000000000000, 0.4067366430757948792, 0.9135454576426031981 ) ) ;
#6046=FACE_OUTER_BOUND ( 'NONE', #15862, .T. ) ;
#6048=DIRECTION ( 'NONE',  ( 0.000000000000000000, -0.9271838545667908660, 0.3746065934159032440 ) ) ;
#6052=DIRECTION ( 'NONE',  ( -1.000000000000000000, -0.000000000000000000, 0.000000000000000000 ) ) ;
#6053=AXIS2_PLACEMENT_3D ( 'NONE', #187, #1837, #8577 ) ;
#6055=DIRECTION ( 'NONE',  ( 1.000000000000000000, 0.000000000000000000, 0.000000000000000000 ) ) ;
#6056=VERTEX_POINT ( 'NONE', #1194 ) ;
#6059=CARTESIAN_POINT ( 'NONE',  ( 0.000000000000000000, -48.19312842678519360, 70.09002648625178722 ) ) ;
#6061=LINE ( 'NONE', #6499, #17674 ) ;
#6064=DIRECTION ( 'NONE',  ( 0.000000000000000000, 0.000000000000000000, 1.000000000000000000 ) ) ;
#6065=ORIENTED_EDGE ( 'NONE', *, *, #4169, .F. ) ;
#6066=CYLINDRICAL_SURFACE ( 'NONE', #5260, 88.00000000000000000 ) ;
#6068=DIRECTION ( 'NONE',  ( 0.000000000000000000, 0.000000000000000000, 1.000000000000000000 ) ) ;
#6069=EDGE_CURVE ( 'NONE', #173, #7162, #7520, .T. ) ;
#6071=CYLINDRICAL_SURFACE ( 'NONE', #11769, 44.99999999999998579 ) ;
#6072=DIRECTION ( 'NONE',  ( 0.000000000000000000, 0.000000000000000000, 1.000000000000000000 ) ) ;
#6073=DIRECTION ( 'NONE',  ( -1.000000000000000000, -0.000000000000000000, -0.000000000000000000 ) ) ;
#6074=ADVANCED_FACE ( 'NONE', ( #10920 ), #4075, .F. ) ;
#6075=DIRECTION ( 'NONE',  ( 0.000000000000000000, 0.000000000000000000, -1.000000000000000000 ) ) ;
#6076=CARTESIAN_POINT ( 'NONE',  ( 10.00000000000000000, -51.76708072107842185, -67.49339815138544907 ) ) ;
#6077=DIRECTION ( 'NONE',  ( 1.000000000000000000, 0.000000000000000000, 0.000000000000000000 ) ) ;
#6079=ORIENTED_EDGE ( 'NONE', *, *, #2488, .F. ) ;
#6081=EDGE_LOOP ( 'NONE', ( #21046, #9106, #8844, #18266 ) ) ;
#6082=ORIENTED_EDGE ( 'NONE', *, *, #9281, .F. ) ;
#6084=VERTEX_POINT ( 'NONE', #19318 ) ;
#6085=DIRECTION ( 'NONE',  ( 0.000000000000000000, 2.312964634635743213E-14, -1.000000000000000000 ) ) ;
#6086=EDGE_CURVE ( 'NONE', #1178, #6420, #12450, .T. ) ;
#6087=VERTEX_POINT ( 'NONE', #976 ) ;
#6088=CARTESIAN_POINT ( 'NONE',  ( 10.00000000000000000, 81.32027326007866463, 44.08455690949082850 ) ) ;
#6089=EDGE_CURVE ( 'NONE', #13540, #9424, #14934, .T. ) ;
#6090=EDGE_CURVE ( 'NONE', #7603, #5274, #17401, .T. ) ;
#6094=DIRECTION ( 'NONE',  ( -1.000000000000000000, -0.000000000000000000, -0.000000000000000000 ) ) ;
#6095=CYLINDRICAL_SURFACE ( 'NONE', #14216, 88.00000000000000000 ) ;
#6098=CARTESIAN_POINT ( 'NONE',  ( 0.000000000000000000, -69.74988376403980794, -53.65588238863407611 ) ) ;
#6099=DIRECTION ( 'NONE',  ( 0.000000000000000000, 0.000000000000000000, 1.000000000000000000 ) ) ;
#6101=DIRECTION ( 'NONE',  ( 1.000000000000000000, 0.000000000000000000, 0.000000000000000000 ) ) ;
#6102=EDGE_CURVE ( 'NONE', #17425, #8447, #6832, .T. ) ;
#6103=CIRCLE ( 'NONE', #13500, 44.99999999999998579 ) ;
#6104=ORIENTED_EDGE ( 'NONE', *, *, #2818, .T. ) ;
#6105=CARTESIAN_POINT ( 'NONE',  ( 10.00000000000000000, 84.80486432185190893, 36.94008646920423899 ) ) ;
#6106=EDGE_CURVE ( 'NONE', #13328, #13109, #14458, .T. ) ;
#6107=CYLINDRICAL_SURFACE ( 'NONE', #14117, 88.00000000000000000 ) ;
#6109=EDGE_LOOP ( 'NONE', ( #15300, #9485, #16626, #17306 ) ) ;
#6111=ORIENTED_EDGE ( 'NONE', *, *, #8779, .T. ) ;
#6112=ORIENTED_EDGE ( 'NONE', *, *, #2440, .T. ) ;
#6113=CARTESIAN_POINT ( 'NONE',  ( 10.00000000000000000, 14.02138820415029663, -83.89630571862271324 ) ) ;
#6118=CARTESIAN_POINT ( 'NONE',  ( 10.00000000000000000, 0.000000000000000000, 0.000000000000000000 ) ) ;
#6119=CIRCLE ( 'NONE', #18826, 45.00000000000000711 ) ;
#6121=ADVANCED_FACE ( 'NONE', ( #19651 ), #6071, .F. ) ;
#6122=CARTESIAN_POINT ( 'NONE',  ( 10.00000000000000000, 0.000000000000000000, 0.000000000000000000 ) ) ;
#6124=CARTESIAN_POINT ( 'NONE',  ( 10.00000000000000000, 62.44821182181090791, 68.23969402963524544 ) ) ;
#6125=CARTESIAN_POINT ( 'NONE',  ( 0.000000000000000000, 8.925965667930080727, -92.06933331948771126 ) ) ;
#6128=CARTESIAN_POINT ( 'NONE',  ( 10.00000000000000000, 0.000000000000000000, 0.000000000000000000 ) ) ;
#6129=DIRECTION ( 'NONE',  ( -1.000000000000000000, -0.000000000000000000, 0.000000000000000000 ) ) ;
#6131=CARTESIAN_POINT ( 'NONE',  ( 10.00000000000000000, 84.19736439813806328, 38.30455363800960811 ) ) ;
#6132=EDGE_CURVE ( 'NONE', #13321, #11004, #19531, .T. ) ;
#6134=ORIENTED_EDGE ( 'NONE', *, *, #8507, .F. ) ;
#6135=EDGE_CURVE ( 'NONE', #21594, #7164, #19874, .T. ) ;
#6136=FACE_OUTER_BOUND ( 'NONE', #8565, .T. ) ;
#6140=DIRECTION ( 'NONE',  ( 0.000000000000000000, 0.000000000000000000, 1.000000000000000000 ) ) ;
#6142=AXIS2_PLACEMENT_3D ( 'NONE', #20192, #13332, #4952 ) ;
#6143=EDGE_CURVE ( 'NONE', #20543, #393, #10341, .T. ) ;
#6145=ORIENTED_EDGE ( 'NONE', *, *, #21107, .T. ) ;
#6146=ORIENTED_EDGE ( 'NONE', *, *, #14877, .F. ) ;
#6149=DIRECTION ( 'NONE',  ( 1.000000000000000000, 0.000000000000000000, 0.000000000000000000 ) ) ;
#6150=ORIENTED_EDGE ( 'NONE', *, *, #7981, .T. ) ;
#6152=CARTESIAN_POINT ( 'NONE',  ( 0.000000000000000000, 25.56104204395415991, -81.12843256239638379 ) ) ;
#6155=DIRECTION ( 'NONE',  ( 0.000000000000000000, 0.4067366430758011520, -0.9135454576426004225 ) ) ;
#6161=DIRECTION ( 'NONE',  ( -1.000000000000000000, 0.000000000000000000, 0.000000000000000000 ) ) ;
#6162=DIRECTION ( 'NONE',  ( 0.000000000000000000, 0.000000000000000000, 1.000000000000000000 ) ) ;
#6163=ORIENTED_EDGE ( 'NONE', *, *, #14864, .F. ) ;
#6166=CIRCLE ( 'NONE', #10734, 44.99999999999999289 ) ;
#6168=DIRECTION ( 'NONE',  ( -1.000000000000000000, -0.000000000000000000, -0.000000000000000000 ) ) ;
#6169=ORIENTED_EDGE ( 'NONE', *, *, #21249, .F. ) ;
#6171=AXIS2_PLACEMENT_3D ( 'NONE', #10131, #17093, #13446 ) ;
#6172=ORIENTED_EDGE ( 'NONE', *, *, #8548, .F. ) ;
#6173=ORIENTED_EDGE ( 'NONE', *, *, #15699, .T. ) ;
#6175=AXIS2_PLACEMENT_3D ( 'NONE', #10968, #13062, #19586 ) ;
#6176=ORIENTED_EDGE ( 'NONE', *, *, #8082, .T. ) ;
#6182=DIRECTION ( 'NONE',  ( -1.000000000000000000, 0.000000000000000000, -0.000000000000000000 ) ) ;
#6185=CARTESIAN_POINT ( 'NONE',  ( 10.00000000000000000, -87.17509410653646285, 30.93441398372555540 ) ) ;
#6187=AXIS2_PLACEMENT_3D ( 'NONE', #17890, #14456, #15781 ) ;
#6189=ORIENTED_EDGE ( 'NONE', *, *, #517, .F. ) ;
#6190=EDGE_CURVE ( 'NONE', #5588, #5691, #3301, .T. ) ;
#6192=VERTEX_POINT ( 'NONE', #12575 ) ;
#6193=ORIENTED_EDGE ( 'NONE', *, *, #17195, .F. ) ;
#6195=VECTOR ( 'NONE', #9019, 1000.000000000000000 ) ;
#6196=CIRCLE ( 'NONE', #6571, 44.99999999999998579 ) ;
#6197=EDGE_CURVE ( 'NONE', #1, #11814, #863, .T. ) ;
#6198=CIRCLE ( 'NONE', #6552, 44.99999999999999289 ) ;
#6199=ORIENTED_EDGE ( 'NONE', *, *, #16200, .F. ) ;
#6200=VECTOR ( 'NONE', #8204, 1000.000000000000000 ) ;
#6201=DIRECTION ( 'NONE',  ( 0.000000000000000000, 0.000000000000000000, 1.000000000000000000 ) ) ;
#6202=VERTEX_POINT ( 'NONE', #3403 ) ;
#6205=DIRECTION ( 'NONE',  ( -1.000000000000000000, -0.000000000000000000, -0.000000000000000000 ) ) ;
#6206=DIRECTION ( 'NONE',  ( 0.000000000000000000, 0.000000000000000000, 1.000000000000000000 ) ) ;
#6207=DIRECTION ( 'NONE',  ( -1.000000000000000000, -0.000000000000000000, -0.000000000000000000 ) ) ;
#6209=LINE ( 'NONE', #7851, #3037 ) ;
#6210=CARTESIAN_POINT ( 'NONE',  ( 0.000000000000000000, 69.74988376404090218, -53.65588238863266213 ) ) ;
#6211=DIRECTION ( 'NONE',  ( -1.000000000000000000, 0.000000000000000000, -0.000000000000000000 ) ) ;
#6213=ORIENTED_EDGE ( 'NONE', *, *, #8783, .T. ) ;
#6215=CIRCLE ( 'NONE', #3021, 92.50100000000003320 ) ;
#6216=DIRECTION ( 'NONE',  ( -1.000000000000000000, -0.000000000000000000, -0.000000000000000000 ) ) ;
#6217=EDGE_CURVE ( 'NONE', #19144, #1974, #114, .T. ) ;
#6218=EDGE_CURVE ( 'NONE', #13174, #6690, #2933, .T. ) ;
#6219=EDGE_CURVE ( 'NONE', #6420, #15764, #8376, .T. ) ;
#6220=ORIENTED_EDGE ( 'NONE', *, *, #133, .T. ) ;
#6224=ORIENTED_EDGE ( 'NONE', *, *, #19598, .T. ) ;
#6227=ORIENTED_EDGE ( 'NONE', *, *, #11790, .T. ) ;
#6229=DIRECTION ( 'NONE',  ( 1.000000000000000000, 0.000000000000000000, 0.000000000000000000 ) ) ;
#6230=ORIENTED_EDGE ( 'NONE', *, *, #4300, .F. ) ;
#6232=ORIENTED_EDGE ( 'NONE', *, *, #1396, .T. ) ;
#6233=CYLINDRICAL_SURFACE ( 'NONE', #7931, 44.99999999999998579 ) ;
#6234=VECTOR ( 'NONE', #6455, 1000.000000000000000 ) ;
#6237=VECTOR ( 'NONE', #6504, 1000.000000000000000 ) ;
#6240=FACE_OUTER_BOUND ( 'NONE', #9565, .T. ) ;
#6241=DIRECTION ( 'NONE',  ( -1.000000000000000000, 0.000000000000000000, 0.000000000000000000 ) ) ;
#6243=ADVANCED_FACE ( 'NONE', ( #19979 ), #13449, .F. ) ;
#6244=CARTESIAN_POINT ( 'NONE',  ( 5.000000000000002665, 30.71797041605925216, -82.46457599186518905 ) ) ;
#6245=DIRECTION ( 'NONE',  ( 0.000000000000000000, 0.9945218953682728458, 0.1045284632676570791 ) ) ;
#6246=VERTEX_POINT ( 'NONE', #6297 ) ;
#6247=DIRECTION ( 'NONE',  ( 0.000000000000000000, 0.000000000000000000, 1.000000000000000000 ) ) ;
#6249=CIRCLE ( 'NONE', #19293, 92.50099999999999056 ) ;
#6252=LINE ( 'NONE', #4680, #978 ) ;
#6255=CARTESIAN_POINT ( 'NONE',  ( 0.000000000000000000, -27.87320266523496315, -88.20158487341788600 ) ) ;
#6258=VERTEX_POINT ( 'NONE', #18338 ) ;
#6259=ORIENTED_EDGE ( 'NONE', *, *, #15928, .F. ) ;
#6260=DIRECTION ( 'NONE',  ( 0.000000000000000000, 0.000000000000000000, 1.000000000000000000 ) ) ;
#6261=LINE ( 'NONE', #13189, #21372 ) ;
#6263=ADVANCED_FACE ( 'NONE', ( #16881 ), #15104, .F. ) ;
#6264=AXIS2_PLACEMENT_3D ( 'NONE', #9388, #12713, #11051 ) ;
#6266=DIRECTION ( 'NONE',  ( 1.000000000000000000, 0.000000000000000000, 0.000000000000000000 ) ) ;
#6267=CIRCLE ( 'NONE', #18951, 44.99999999999999289 ) ;
#6269=EDGE_CURVE ( 'NONE', #17102, #4746, #5763, .T. ) ;
#6270=CARTESIAN_POINT ( 'NONE',  ( 10.00000000000000000, 57.53593069156472239, -72.42963261300903355 ) ) ;
#6271=CIRCLE ( 'NONE', #17901, 92.50100000000000477 ) ;
#6277=DIRECTION ( 'NONE',  ( 0.000000000000000000, 0.7431448254773910245, 0.6691306063588617903 ) ) ;
#6279=MANIFOLD_SOLID_BREP ( 'TeethCuts', #1959 ) ;
#6280=CARTESIAN_POINT ( 'NONE',  ( 10.00000000000000000, 32.56745702629844175, -78.57830605990621109 ) ) ;
#6281=VERTEX_POINT ( 'NONE', #13878 ) ;
#6282=AXIS2_PLACEMENT_3D ( 'NONE', #2754, #18107, #1090 ) ;
#6285=CIRCLE ( 'NONE', #3095, 44.99999999999999289 ) ;
#6286=DIRECTION ( 'NONE',  ( 0.000000000000000000, -1.773272886554069860E-14, -1.000000000000000000 ) ) ;
#6287=AXIS2_PLACEMENT_3D ( 'NONE', #15213, #1963, #5180 ) ;
#6290=ORIENTED_EDGE ( 'NONE', *, *, #10492, .F. ) ;
#6291=ORIENTED_EDGE ( 'NONE', *, *, #2082, .T. ) ;
#6293=EDGE_LOOP ( 'NONE', ( #3950, #8067, #6702, #14539 ) ) ;
#6294=CYLINDRICAL_SURFACE ( 'NONE', #15499, 88.00000000000000000 ) ;
#6297=CARTESIAN_POINT ( 'NONE',  ( 10.00000000000000000, 41.89587599971653731, -77.38692120905427885 ) ) ;
#6300=CIRCLE ( 'NONE', #15460, 45.00000000000000711 ) ;
#6301=CARTESIAN_POINT ( 'NONE',  ( 0.000000000000000000, -84.90234713953988432, 5.175025661883520200 ) ) ;
#6302=CARTESIAN_POINT ( 'NONE',  ( 10.00000000000000000, 65.64563793391906188, -54.09103124042745492 ) ) ;
#6304=AXIS2_PLACEMENT_3D ( 'NONE', #16827, #13403, #12957 ) ;
#6306=DIRECTION ( 'NONE',  ( 0.000000000000000000, 0.8660254037844363761, 0.5000000000000041078 ) ) ;
#6307=DIRECTION ( 'NONE',  ( 1.000000000000000000, 0.000000000000000000, 0.000000000000000000 ) ) ;
#6309=VECTOR ( 'NONE', #5334, 1000.000000000000000 ) ;
#6311=ORIENTED_EDGE ( 'NONE', *, *, #5736, .T. ) ;
#6313=ORIENTED_EDGE ( 'NONE', *, *, #5564, .F. ) ;
#6315=ORIENTED_EDGE ( 'NONE', *, *, #9039, .F. ) ;
#6317=AXIS2_PLACEMENT_3D ( 'NONE', #18588, #18704, #8523 ) ;
#6318=CIRCLE ( 'NONE', #19003, 44.99999999999999289 ) ;
#6319=ORIENTED_EDGE ( 'NONE', *, *, #862, .F. ) ;
#6320=CARTESIAN_POINT ( 'NONE',  ( 10.00000000000000000, 29.29369617358583255, -87.74003855418371245 ) ) ;
#6322=FACE_OUTER_BOUND ( 'NONE', #7041, .T. ) ;
#6323=DIRECTION ( 'NONE',  ( 1.000000000000000000, 0.000000000000000000, 0.000000000000000000 ) ) ;
#6324=DIRECTION ( 'NONE',  ( 0.000000000000000000, 0.000000000000000000, 1.000000000000000000 ) ) ;
#6327=CARTESIAN_POINT ( 'NONE',  ( 0.000000000000000000, 68.36541360927188293, 50.60987712331726840 ) ) ;
#6328=CARTESIAN_POINT ( 'NONE',  ( 10.00000000000000000, -72.58367602204151581, -49.75550195834941292 ) ) ;
#6329=CARTESIAN_POINT ( 'NONE',  ( -10.00000000000000000, 0.000000000000000000, 0.000000000000000000 ) ) ;
#6330=CIRCLE ( 'NONE', #18678, 88.00000000000000000 ) ;
#6331=AXIS2_PLACEMENT_3D ( 'NONE', #8039, #2841, #11451 ) ;
#6332=VERTEX_POINT ( 'NONE', #12013 ) ;
#6333=AXIS2_PLACEMENT_3D ( 'NONE', #6076, #20771, #4084 ) ;
#6337=DIRECTION ( 'NONE',  ( 0.000000000000000000, 0.000000000000000000, 1.000000000000000000 ) ) ;
#6340=DIRECTION ( 'NONE',  ( -1.000000000000000000, -0.000000000000000000, -0.000000000000000000 ) ) ;
#6344=AXIS2_PLACEMENT_3D ( 'NONE', #19262, #8483, #12109 ) ;
#6345=DIRECTION ( 'NONE',  ( 0.000000000000000000, 0.000000000000000000, -1.000000000000000000 ) ) ;
#6346=VERTEX_POINT ( 'NONE', #5382 ) ;
#6347=VECTOR ( 'NONE', #12418, 1000.000000000000000 ) ;
#6352=DIRECTION ( 'NONE',  ( 0.000000000000000000, 0.000000000000000000, 1.000000000000000000 ) ) ;
#6353=DIRECTION ( 'NONE',  ( 1.000000000000000000, 0.000000000000000000, 0.000000000000000000 ) ) ;
#6354=EDGE_CURVE ( 'NONE', #6719, #19647, #2171, .T. ) ;
#6355=CARTESIAN_POINT ( 'NONE',  ( 10.00000000000000000, 77.39385041987100067, 35.28996114464738554 ) ) ;
#6356=DIRECTION ( 'NONE',  ( 1.000000000000000000, 0.000000000000000000, 0.000000000000000000 ) ) ;
#6358=FACE_OUTER_BOUND ( 'NONE', #20245, .T. ) ;
#6359=CARTESIAN_POINT ( 'NONE',  ( 10.00000000000000000, -60.65655256511276860, 59.63197188857500919 ) ) ;
#6361=EDGE_CURVE ( 'NONE', #508, #791, #17097, .T. ) ;
#6363=CIRCLE ( 'NONE', #18709, 92.50100000000000477 ) ;
#6364=AXIS2_PLACEMENT_3D ( 'NONE', #9778, #19631, #16533 ) ;
#6367=CARTESIAN_POINT ( 'NONE',  ( 10.00000000000000000, 83.35585896458619004, 16.94078559807978124 ) ) ;
#6369=EDGE_LOOP ( 'NONE', ( #20960, #10822, #17312, #6749 ) ) ;
#6371=ORIENTED_EDGE ( 'NONE', *, *, #14359, .F. ) ;
#6375=ORIENTED_EDGE ( 'NONE', *, *, #15106, .T. ) ;
#6377=DIRECTION ( 'NONE',  ( -1.000000000000000000, -0.000000000000000000, -0.000000000000000000 ) ) ;
#6378=CARTESIAN_POINT ( 'NONE',  ( 5.000000000000002665, -73.32282170386882569, 48.65967342042752364 ) ) ;
#6379=EDGE_CURVE ( 'NONE', #1789, #13415, #20946, .T. ) ;
#6380=DIRECTION ( 'NONE',  ( 0.000000000000000000, 0.000000000000000000, 1.000000000000000000 ) ) ;
#6381=EDGE_CURVE ( 'NONE', #15480, #15273, #832, .T. ) ;
#6382=CIRCLE ( 'NONE', #14825, 92.50100000000000477 ) ;
#6385=LINE ( 'NONE', #16529, #10965 ) ;
#6389=CARTESIAN_POINT ( 'NONE',  ( 10.00000000000000000, -60.65655256511196569, -59.63197188857583342 ) ) ;
#6392=CARTESIAN_POINT ( 'NONE',  ( 5.000000000000000000, -65.83713140174766920, 58.39068529131174756 ) ) ;
#6393=EDGE_CURVE ( 'NONE', #5049, #5074, #3314, .T. ) ;
#6395=CARTESIAN_POINT ( 'NONE',  ( 0.000000000000000000, 0.000000000000000000, 0.000000000000000000 ) ) ;
#6397=CARTESIAN_POINT ( 'NONE',  ( 0.000000000000000000, 0.000000000000000000, 0.000000000000000000 ) ) ;
#6399=DIRECTION ( 'NONE',  ( -1.000000000000000000, -0.000000000000000000, -0.000000000000000000 ) ) ;
#6400=ADVANCED_FACE ( 'NONE', ( #3938 ), #2072, .F. ) ;
#6401=VERTEX_POINT ( 'NONE', #7146 ) ;
#6404=EDGE_CURVE ( 'NONE', #393, #3324, #5494, .T. ) ;
#6406=LINE ( 'NONE', #4839, #5622 ) ;
#6407=CIRCLE ( 'NONE', #21557, 44.99999999999999289 ) ;
#6408=DIRECTION ( 'NONE',  ( -1.000000000000000000, 0.000000000000000000, -0.000000000000000000 ) ) ;
#6411=EDGE_CURVE ( 'NONE', #20191, #1625, #5776, .T. ) ;
#6416=DIRECTION ( 'NONE',  ( 0.000000000000000000, 0.000000000000000000, 1.000000000000000000 ) ) ;
#6418=DIRECTION ( 'NONE',  ( 0.000000000000000000, 0.000000000000000000, 1.000000000000000000 ) ) ;
#6420=VERTEX_POINT ( 'NONE', #16990 ) ;
#6423=VERTEX_POINT ( 'NONE', #515 ) ;
#6427=DIRECTION ( 'NONE',  ( 0.000000000000000000, 0.000000000000000000, 1.000000000000000000 ) ) ;
#6428=VERTEX_POINT ( 'NONE', #7376 ) ;
#6429=CARTESIAN_POINT ( 'NONE',  ( -10.00000000000000000, 0.000000000000000000, 0.000000000000000000 ) ) ;
#6430=CARTESIAN_POINT ( 'NONE',  ( 0.000000000000000000, -92.22057093985026199, -7.197311757041478408 ) ) ;
#6431=CARTESIAN_POINT ( 'NONE',  ( 0.000000000000000000, 0.000000000000000000, 0.000000000000000000 ) ) ;
#6433=DIRECTION ( 'NONE',  ( 0.000000000000000000, 0.000000000000000000, 1.000000000000000000 ) ) ;
#6435=LINE ( 'NONE', #21770, #17948 ) ;
#6438=CARTESIAN_POINT ( 'NONE',  ( -10.00000000000000000, 0.000000000000000000, 0.000000000000000000 ) ) ;
#6439=ORIENTED_EDGE ( 'NONE', *, *, #7740, .F. ) ;
#6440=ORIENTED_EDGE ( 'NONE', *, *, #5250, .T. ) ;
#6442=AXIS2_PLACEMENT_3D ( 'NONE', #2650, #9379, #16133 ) ;
#6444=CYLINDRICAL_SURFACE ( 'NONE', #14054, 44.99999999999999289 ) ;
#6448=DIRECTION ( 'NONE',  ( 1.000000000000000000, 0.000000000000000000, 0.000000000000000000 ) ) ;
#6449=ORIENTED_EDGE ( 'NONE', *, *, #7029, .F. ) ;
#6450=LINE ( 'NONE', #13164, #4044 ) ;
#6452=AXIS2_PLACEMENT_3D ( 'NONE', #17365, #2010, #2219 ) ;
#6455=DIRECTION ( 'NONE',  ( -1.000000000000000000, 0.000000000000000000, 0.000000000000000000 ) ) ;
#6456=DIRECTION ( 'NONE',  ( 0.000000000000000000, 0.000000000000000000, 1.000000000000000000 ) ) ;
#6458=DIRECTION ( 'NONE',  ( 0.000000000000000000, 0.8660254037844362651, 0.5000000000000039968 ) ) ;
#6460=ORIENTED_EDGE ( 'NONE', *, *, #4203, .T. ) ;
#6461=CARTESIAN_POINT ( 'NONE',  ( 10.00000000000000000, 68.93609746931237225, -54.69748134696388320 ) ) ;
#6462=CARTESIAN_POINT ( 'NONE',  ( 10.00000000000000000, -29.47587714451095309, 82.91666097089111531 ) ) ;
#6465=EDGE_CURVE ( 'NONE', #2214, #7364, #12126, .T. ) ;
#6466=DIRECTION ( 'NONE',  ( 0.000000000000000000, 3.546545773108139957E-15, -1.000000000000000000 ) ) ;
#6467=ORIENTED_EDGE ( 'NONE', *, *, #1769, .F. ) ;
#6468=ORIENTED_EDGE ( 'NONE', *, *, #20015, .T. ) ;
#6470=FACE_OUTER_BOUND ( 'NONE', #1650, .T. ) ;
#6471=ORIENTED_EDGE ( 'NONE', *, *, #21794, .F. ) ;
#6477=VERTEX_POINT ( 'NONE', #7476 ) ;
#6479=DIRECTION ( 'NONE',  ( -1.000000000000000000, 0.000000000000000000, 0.000000000000000000 ) ) ;
#6481=CARTESIAN_POINT ( 'NONE',  ( 0.000000000000000000, 84.79630770241077187, 6.691460262316813790 ) ) ;
#6482=DIRECTION ( 'NONE',  ( -1.000000000000000000, -0.000000000000000000, -0.000000000000000000 ) ) ;
#6485=AXIS2_PLACEMENT_3D ( 'NONE', #10267, #19425, #757 ) ;
#6486=ORIENTED_EDGE ( 'NONE', *, *, #15173, .F. ) ;
#6488=CIRCLE ( 'NONE', #11053, 44.99999999999998579 ) ;
#6490=ORIENTED_EDGE ( 'NONE', *, *, #3163, .F. ) ;
#6491=CARTESIAN_POINT ( 'NONE',  ( -10.00000000000000000, 0.000000000000000000, 0.000000000000000000 ) ) ;
#6492=ORIENTED_EDGE ( 'NONE', *, *, #7461, .T. ) ;
#6493=CIRCLE ( 'NONE', #2590, 92.50100000000000477 ) ;
#6494=EDGE_CURVE ( 'NONE', #17311, #11431, #21308, .T. ) ;
#6495=EDGE_CURVE ( 'NONE', #14735, #19098, #19888, .T. ) ;
#6496=EDGE_CURVE ( 'NONE', #13465, #18176, #11785, .T. ) ;
#6497=CYLINDRICAL_SURFACE ( 'NONE', #11963, 44.99999999999999289 ) ;
#6498=ORIENTED_EDGE ( 'NONE', *, *, #5060, .T. ) ;
#6499=CARTESIAN_POINT ( 'NONE',  ( 5.000000000000002665, 46.07110168784820559, 74.97635353408399794 ) ) ;
#6503=VERTEX_POINT ( 'NONE', #9334 ) ;
#6504=DIRECTION ( 'NONE',  ( -1.000000000000000000, 0.000000000000000000, -0.000000000000000000 ) ) ;
#6505=VERTEX_POINT ( 'NONE', #737 ) ;
#6508=DIRECTION ( 'NONE',  ( 0.000000000000000000, 0.000000000000000000, 1.000000000000000000 ) ) ;
#6510=LINE ( 'NONE', #10133, #17812 ) ;
#6513=CIRCLE ( 'NONE', #4379, 44.99999999999998579 ) ;
#6515=CARTESIAN_POINT ( 'NONE',  ( -10.00000000000000000, 0.000000000000000000, 0.000000000000000000 ) ) ;
#6516=DIRECTION ( 'NONE',  ( 0.000000000000000000, 0.000000000000000000, 1.000000000000000000 ) ) ;
#6519=AXIS2_PLACEMENT_3D ( 'NONE', #5359, #60, #3695 ) ;
#6520=CARTESIAN_POINT ( 'NONE',  ( 10.00000000000000000, 5.479102470010468018, 87.82926298292115064 ) ) ;
#6521=CARTESIAN_POINT ( 'NONE',  ( -10.00000000000000000, 0.000000000000000000, 0.000000000000000000 ) ) ;
#6522=CIRCLE ( 'NONE', #6171, 44.99999999999999289 ) ;
#6524=ORIENTED_EDGE ( 'NONE', *, *, #3112, .T. ) ;
#6526=VERTEX_POINT ( 'NONE', #4490 ) ;
#6527=EDGE_CURVE ( 'NONE', #5809, #7682, #13534, .T. ) ;
#6531=AXIS2_PLACEMENT_3D ( 'NONE', #14837, #21578, #6456 ) ;
#6533=CARTESIAN_POINT ( 'NONE',  ( 0.000000000000000000, 0.000000000000000000, 0.000000000000000000 ) ) ;
#6534=AXIS2_PLACEMENT_3D ( 'NONE', #14679, #13453, #6741 ) ;
#6537=EDGE_CURVE ( 'NONE', #16339, #10824, #18129, .T. ) ;
#6538=CIRCLE ( 'NONE', #8629, 44.99999999999999289 ) ;
#6539=CARTESIAN_POINT ( 'NONE',  ( -10.00000000000000000, 0.000000000000000000, 0.000000000000000000 ) ) ;
#6543=CIRCLE ( 'NONE', #13588, 88.00000000000000000 ) ;
#6544=DIRECTION ( 'NONE',  ( 0.000000000000000000, 0.000000000000000000, 1.000000000000000000 ) ) ;
#6545=CARTESIAN_POINT ( 'NONE',  ( 0.000000000000000000, 81.55207211302078463, -24.17537951050094236 ) ) ;
#6546=EDGE_CURVE ( 'NONE', #16218, #8158, #19538, .T. ) ;
#6547=VERTEX_POINT ( 'NONE', #17978 ) ;
#6548=EDGE_CURVE ( 'NONE', #7517, #16720, #4001, .T. ) ;
#6549=CARTESIAN_POINT ( 'NONE',  ( 10.00000000000000000, 2.481790431839256517, 92.46770094066594936 ) ) ;
#6552=AXIS2_PLACEMENT_3D ( 'NONE', #8699, #307, #10572 ) ;
#6560=ORIENTED_EDGE ( 'NONE', *, *, #5005, .F. ) ;
#6561=AXIS2_PLACEMENT_3D ( 'NONE', #14788, #14890, #4724 ) ;
#6564=ORIENTED_EDGE ( 'NONE', *, *, #12403, .T. ) ;
#6565=AXIS2_PLACEMENT_3D ( 'NONE', #13751, #2141, #18730 ) ;
#6568=DIRECTION ( 'NONE',  ( 1.000000000000000000, 0.000000000000000000, 0.000000000000000000 ) ) ;
#6569=CARTESIAN_POINT ( 'NONE',  ( 10.00000000000000000, 36.60317927562579854, 76.78148674856777234 ) ) ;
#6570=CIRCLE ( 'NONE', #12192, 92.50099999999999056 ) ;
#6571=AXIS2_PLACEMENT_3D ( 'NONE', #15274, #46, #10414 ) ;
#6572=CIRCLE ( 'NONE', #11145, 44.99999999999999289 ) ;
#6575=CARTESIAN_POINT ( 'NONE',  ( 0.000000000000000000, -16.79755869217588682, -90.96305306542271296 ) ) ;
#6576=VERTEX_POINT ( 'NONE', #15879 ) ;
#6577=DIRECTION ( 'NONE',  ( 0.000000000000000000, 0.000000000000000000, 1.000000000000000000 ) ) ;
#6579=ORIENTED_EDGE ( 'NONE', *, *, #16759, .T. ) ;
#6581=LINE ( 'NONE', #8333, #21013 ) ;
#6582=ORIENTED_EDGE ( 'NONE', *, *, #18382, .T. ) ;
#6583=CIRCLE ( 'NONE', #16090, 92.50100000000000477 ) ;
#6584=AXIS2_PLACEMENT_3D ( 'NONE', #9380, #5059, #1424 ) ;
#6585=EDGE_LOOP ( 'NONE', ( #16984, #14881, #19356, #6230 ) ) ;
#6588=VERTEX_POINT ( 'NONE', #5930 ) ;
#6589=CARTESIAN_POINT ( 'NONE',  ( 10.00000000000000000, 18.94217447942559573, 85.93715160505956874 ) ) ;
#6590=DIRECTION ( 'NONE',  ( 0.000000000000000000, -0.2756373558169869509, -0.9612616959383223358 ) ) ;
#6593=DIRECTION ( 'NONE',  ( 0.000000000000000000, -0.4694715627858975782, 0.8829475928589234357 ) ) ;
#6598=EDGE_CURVE ( 'NONE', #3581, #2939, #4159, .T. ) ;
#6599=AXIS2_PLACEMENT_3D ( 'NONE', #15654, #14000, #526 ) ;
#6603=CYLINDRICAL_SURFACE ( 'NONE', #4435, 92.50100000000000477 ) ;
#6606=CARTESIAN_POINT ( 'NONE',  ( 10.00000000000000000, 52.96496548042942010, -66.55750800669305534 ) ) ;
#6607=VERTEX_POINT ( 'NONE', #19183 ) ;
#6609=DIRECTION ( 'NONE',  ( 0.000000000000000000, 0.000000000000000000, 1.000000000000000000 ) ) ;
#6610=ORIENTED_EDGE ( 'NONE', *, *, #17422, .F. ) ;
#6611=DIRECTION ( 'NONE',  ( 0.000000000000000000, 0.000000000000000000, 1.000000000000000000 ) ) ;
#6612=VECTOR ( 'NONE', #11714, 1000.000000000000000 ) ;
#6615=VERTEX_POINT ( 'NONE', #4043 ) ;
#6617=CIRCLE ( 'NONE', #9774, 45.00000000000000000 ) ;
#6618=VERTEX_POINT ( 'NONE', #17649 ) ;
#6619=DIRECTION ( 'NONE',  ( -1.000000000000000000, -0.000000000000000000, -0.000000000000000000 ) ) ;
#6620=DIRECTION ( 'NONE',  ( -1.000000000000000000, -0.000000000000000000, -0.000000000000000000 ) ) ;
#6621=CARTESIAN_POINT ( 'NONE',  ( 0.000000000000000000, 29.47587714451039531, 82.91666097089130005 ) ) ;
#6624=EDGE_CURVE ( 'NONE', #18366, #6894, #4717, .T. ) ;
#6625=DIRECTION ( 'NONE',  ( -1.000000000000000000, -0.000000000000000000, -0.000000000000000000 ) ) ;
#6627=DIRECTION ( 'NONE',  ( -1.000000000000000000, 0.000000000000000000, 0.000000000000000000 ) ) ;
#6628=VECTOR ( 'NONE', #14530, 1000.000000000000000 ) ;
#6631=VECTOR ( 'NONE', #6182, 1000.000000000000000 ) ;
#6633=ORIENTED_EDGE ( 'NONE', *, *, #12154, .T. ) ;
#6634=CARTESIAN_POINT ( 'NONE',  ( 0.000000000000000000, 0.000000000000000000, 0.000000000000000000 ) ) ;
#6635=ORIENTED_EDGE ( 'NONE', *, *, #9479, .T. ) ;
#6636=ORIENTED_EDGE ( 'NONE', *, *, #3608, .F. ) ;
#6638=VERTEX_POINT ( 'NONE', #9655 ) ;
#6640=EDGE_CURVE ( 'NONE', #4926, #4858, #12470, .T. ) ;
#6641=CARTESIAN_POINT ( 'NONE',  ( 0.000000000000000000, -74.74361964203200159, -40.60271866773624083 ) ) ;
#6644=CARTESIAN_POINT ( 'NONE',  ( 10.00000000000000000, -90.63195040374199607, 18.50093422002390398 ) ) ;
#6646=VECTOR ( 'NONE', #1693, 1000.000000000000000 ) ;
#6649=LINE ( 'NONE', #15345, #7169 ) ;
#6650=EDGE_CURVE ( 'NONE', #13109, #14874, #7534, .T. ) ;
#6651=CYLINDRICAL_SURFACE ( 'NONE', #4491, 92.50100000000000477 ) ;
#6652=ADVANCED_FACE ( 'NONE', ( #21823 ), #11326, .F. ) ;
#6653=DIRECTION ( 'NONE',  ( -1.000000000000000000, 0.000000000000000000, -0.000000000000000000 ) ) ;
#6658=CARTESIAN_POINT ( 'NONE',  ( 10.00000000000000000, 57.47876254627143311, 62.70072803846409215 ) ) ;
#6659=AXIS2_PLACEMENT_3D ( 'NONE', #2436, #9377, #7743 ) ;
#6662=CIRCLE ( 'NONE', #8771, 44.99999999999999289 ) ;
#6663=CIRCLE ( 'NONE', #2767, 88.00000000000000000 ) ;
#6664=ORIENTED_EDGE ( 'NONE', *, *, #12685, .T. ) ;
#6668=DIRECTION ( 'NONE',  ( -1.000000000000000000, -0.000000000000000000, 0.000000000000000000 ) ) ;
#6674=CYLINDRICAL_SURFACE ( 'NONE', #15799, 88.00000000000000000 ) ;
#6675=VERTEX_POINT ( 'NONE', #6270 ) ;
#6676=CARTESIAN_POINT ( 'NONE',  ( -10.00000000000000000, 0.000000000000000000, 0.000000000000000000 ) ) ;
#6677=CARTESIAN_POINT ( 'NONE',  ( 10.00000000000000000, -79.38136668499713267, -37.98155635597392887 ) ) ;
#6678=EDGE_CURVE ( 'NONE', #10690, #16223, #11432, .T. ) ;
#6679=AXIS2_PLACEMENT_3D ( 'NONE', #13464, #5081, #222 ) ;
#6681=FACE_OUTER_BOUND ( 'NONE', #9646, .T. ) ;
#6683=DIRECTION ( 'NONE',  ( 0.000000000000000000, 0.000000000000000000, 1.000000000000000000 ) ) ;
#6684=AXIS2_PLACEMENT_3D ( 'NONE', #5682, #12408, #1826 ) ;
#6685=CIRCLE ( 'NONE', #4550, 44.99999999999999289 ) ;
#6686=DIRECTION ( 'NONE',  ( 0.000000000000000000, 0.000000000000000000, 1.000000000000000000 ) ) ;
#6688=CARTESIAN_POINT ( 'NONE',  ( 10.00000000000000000, -15.32665449651985590, 91.22241316115413667 ) ) ;
#6689=EDGE_CURVE ( 'NONE', #3682, #12864, #12141, .T. ) ;
#6690=VERTEX_POINT ( 'NONE', #12987 ) ;
#6691=EDGE_CURVE ( 'NONE', #11054, #6401, #18508, .T. ) ;
#6693=AXIS2_PLACEMENT_3D ( 'NONE', #7994, #1248, #10969 ) ;
#6696=AXIS2_PLACEMENT_3D ( 'NONE', #9670, #8042, #20081 ) ;
#6697=VECTOR ( 'NONE', #7922, 1000.000000000000000 ) ;
#6698=DIRECTION ( 'NONE',  ( 1.000000000000000000, 0.000000000000000000, 0.000000000000000000 ) ) ;
#6701=EDGE_LOOP ( 'NONE', ( #3107, #12661, #9824, #3435 ) ) ;
#6702=ORIENTED_EDGE ( 'NONE', *, *, #20822, .F. ) ;
#6704=ORIENTED_EDGE ( 'NONE', *, *, #15582, .F. ) ;
#6705=VERTEX_POINT ( 'NONE', #18191 ) ;
#6707=ORIENTED_EDGE ( 'NONE', *, *, #2998, .T. ) ;
#6709=CARTESIAN_POINT ( 'NONE',  ( 0.000000000000000000, -10.41137886060169038, 91.91321010181843576 ) ) ;
#6712=DIRECTION ( 'NONE',  ( 0.000000000000000000, 0.000000000000000000, 1.000000000000000000 ) ) ;
#6713=CARTESIAN_POINT ( 'NONE',  ( -10.00000000000000000, 0.000000000000000000, 0.000000000000000000 ) ) ;
#6716=VERTEX_POINT ( 'NONE', #14867 ) ;
#6717=DIRECTION ( 'NONE',  ( 0.000000000000000000, 0.000000000000000000, 1.000000000000000000 ) ) ;
#6718=CARTESIAN_POINT ( 'NONE',  ( 10.00000000000000000, 60.65279801375343993, 63.75921967137637836 ) ) ;
#6719=VERTEX_POINT ( 'NONE', #4815 ) ;
#6720=FACE_OUTER_BOUND ( 'NONE', #12205, .T. ) ;
#6721=SHAPE_REPRESENTATION ( 'internal spur gear_iso_ISO - Internal spur gear 2M 90T 20PA 10FW ---S90S200OD 1.0AF', ( #15567 ), #19793 ) ;
#6722=ORIENTED_EDGE ( 'NONE', *, *, #7235, .F. ) ;
#6725=ORIENTED_EDGE ( 'NONE', *, *, #18657, .T. ) ;
#6727=ORIENTED_EDGE ( 'NONE', *, *, #2848, .T. ) ;
#6728=ORIENTED_EDGE ( 'NONE', *, *, #1781, .T. ) ;
#6729=VERTEX_POINT ( 'NONE', #8235 ) ;
#6730=AXIS2_PLACEMENT_3D ( 'NONE', #16717, #5011, #15170 ) ;
#6731=CARTESIAN_POINT ( 'NONE',  ( 0.000000000000000000, -84.79630770241089976, 6.691460262315113816 ) ) ;
#6735=DIRECTION ( 'NONE',  ( 0.000000000000000000, 0.000000000000000000, 1.000000000000000000 ) ) ;
#6736=DIRECTION ( 'NONE',  ( 0.000000000000000000, 0.000000000000000000, 1.000000000000000000 ) ) ;
#6739=CARTESIAN_POINT ( 'NONE',  ( 10.00000000000000000, -64.95266917914277371, -59.37298010463037912 ) ) ;
#6740=CARTESIAN_POINT ( 'NONE',  ( 10.00000000000000000, -78.04699792498179534, 49.64978465107262906 ) ) ;
#6741=DIRECTION ( 'NONE',  ( 0.000000000000000000, -1.063963731932441790E-14, -1.000000000000000000 ) ) ;
#6742=CIRCLE ( 'NONE', #16245, 45.00000000000000000 ) ;
#6745=DIRECTION ( 'NONE',  ( 1.000000000000000000, 0.000000000000000000, 0.000000000000000000 ) ) ;
#6746=ORIENTED_EDGE ( 'NONE', *, *, #2532, .F. ) ;
#6748=ORIENTED_EDGE ( 'NONE', *, *, #20288, .F. ) ;
#6749=ORIENTED_EDGE ( 'NONE', *, *, #7306, .F. ) ;
#6751=ORIENTED_EDGE ( 'NONE', *, *, #7928, .F. ) ;
#6753=ORIENTED_EDGE ( 'NONE', *, *, #17310, .T. ) ;
#6754=CARTESIAN_POINT ( 'NONE',  ( 0.000000000000000000, -52.34334029047928993, 76.26670130689468863 ) ) ;
#6755=DIRECTION ( 'NONE',  ( -1.000000000000000000, -0.000000000000000000, -0.000000000000000000 ) ) ;
#6756=EDGE_CURVE ( 'NONE', #12590, #8355, #11667, .T. ) ;
#6757=DIRECTION ( 'NONE',  ( 0.000000000000000000, 0.000000000000000000, 1.000000000000000000 ) ) ;
#6759=CARTESIAN_POINT ( 'NONE',  ( 0.000000000000000000, 90.32141448704683739, 19.96189084378252332 ) ) ;
#6760=EDGE_CURVE ( 'NONE', #20731, #14184, #17792, .T. ) ;
#6761=FACE_OUTER_BOUND ( 'NONE', #4469, .T. ) ;
#6762=ORIENTED_EDGE ( 'NONE', *, *, #11821, .T. ) ;
#6763=CARTESIAN_POINT ( 'NONE',  ( 0.000000000000000000, 2.481790431840498634, -92.46770094066590673 ) ) ;
#6764=VERTEX_POINT ( 'NONE', #12310 ) ;
#6765=VERTEX_POINT ( 'NONE', #6807 ) ;
#6766=CARTESIAN_POINT ( 'NONE',  ( 10.00000000000000000, -52.96496548042899377, 66.55750800669339640 ) ) ;
#6769=ADVANCED_FACE ( 'NONE', ( #20392 ), #10430, .F. ) ;
#6770=ADVANCED_FACE ( 'NONE', ( #5254 ), #13530, .F. ) ;
#6773=ORIENTED_EDGE ( 'NONE', *, *, #7327, .T. ) ;
#6776=EDGE_CURVE ( 'NONE', #15522, #18255, #3806, .T. ) ;
#6778=CARTESIAN_POINT ( 'NONE',  ( 0.000000000000000000, -92.32475887865419395, -5.707354816231489991 ) ) ;
#6780=CARTESIAN_POINT ( 'NONE',  ( 10.00000000000000000, 91.49386717542239467, -13.61276130276895557 ) ) ;
#6783=DIRECTION ( 'NONE',  ( -1.000000000000000000, -0.000000000000000000, -0.000000000000000000 ) ) ;
#6785=CARTESIAN_POINT ( 'NONE',  ( 10.00000000000000000, 0.000000000000000000, 0.000000000000000000 ) ) ;
#6786=ORIENTED_EDGE ( 'NONE', *, *, #15389, .F. ) ;
#6791=ORIENTED_EDGE ( 'NONE', *, *, #7529, .T. ) ;
#6792=FACE_OUTER_BOUND ( 'NONE', #17114, .T. ) ;
#6793=ORIENTED_EDGE ( 'NONE', *, *, #21763, .T. ) ;
#6794=ORIENTED_EDGE ( 'NONE', *, *, #12154, .F. ) ;
#6797=VECTOR ( 'NONE', #13281, 1000.000000000000000 ) ;
#6798=ORIENTED_EDGE ( 'NONE', *, *, #17407, .F. ) ;
#6800=LINE ( 'NONE', #20492, #17445 ) ;
#6801=DIRECTION ( 'NONE',  ( 0.000000000000000000, 0.000000000000000000, 1.000000000000000000 ) ) ;
#6802=ORIENTED_EDGE ( 'NONE', *, *, #1624, .F. ) ;
#6803=AXIS2_PLACEMENT_3D ( 'NONE', #14368, #13038, #16462 ) ;
#6805=DIRECTION ( 'NONE',  ( 0.000000000000000000, 0.000000000000000000, -1.000000000000000000 ) ) ;
#6806=CARTESIAN_POINT ( 'NONE',  ( 10.00000000000000000, 0.000000000000000000, 0.000000000000000000 ) ) ;
#6807=CARTESIAN_POINT ( 'NONE',  ( 0.000000000000000000, -8.925965667929483871, 92.06933331948778232 ) ) ;
#6808=CIRCLE ( 'NONE', #786, 88.00000000000000000 ) ;
#6809=DIRECTION ( 'NONE',  ( -1.000000000000000000, 0.000000000000000000, 0.000000000000000000 ) ) ;
#6812=ORIENTED_EDGE ( 'NONE', *, *, #14737, .F. ) ;
#6813=EDGE_CURVE ( 'NONE', #21676, #14602, #19904, .T. ) ;
#6814=DIRECTION ( 'NONE',  ( 0.000000000000000000, 0.9945218953682737340, -0.1045284632676505010 ) ) ;
#6817=ORIENTED_EDGE ( 'NONE', *, *, #7319, .F. ) ;
#6819=EDGE_CURVE ( 'NONE', #5724, #8570, #5447, .T. ) ;
#6820=DIRECTION ( 'NONE',  ( 1.000000000000000000, 0.000000000000000000, 0.000000000000000000 ) ) ;
#6821=ORIENTED_EDGE ( 'NONE', *, *, #16994, .F. ) ;
#6822=AXIS2_PLACEMENT_3D ( 'NONE', #9151, #5312, #15898 ) ;
#6824=VERTEX_POINT ( 'NONE', #8561 ) ;
#6828=ORIENTED_EDGE ( 'NONE', *, *, #2959, .F. ) ;
#6829=CARTESIAN_POINT ( 'NONE',  ( 10.00000000000000000, -46.07110168784872428, 74.97635353408365688 ) ) ;
#6830=ORIENTED_EDGE ( 'NONE', *, *, #19713, .F. ) ;
#6832=CIRCLE ( 'NONE', #21291, 44.99999999999998579 ) ;
#6833=CARTESIAN_POINT ( 'NONE',  ( 10.00000000000000000, -14.02138820414970688, 83.89630571862279851 ) ) ;
#6834=DIRECTION ( 'NONE',  ( 1.000000000000000000, 0.000000000000000000, 0.000000000000000000 ) ) ;
#6835=DIRECTION ( 'NONE',  ( 1.000000000000000000, 0.000000000000000000, 0.000000000000000000 ) ) ;
#6837=AXIS2_PLACEMENT_3D ( 'NONE', #19480, #8984, #10644 ) ;
#6841=CIRCLE ( 'NONE', #6142, 92.50100000000000477 ) ;
#6843=CARTESIAN_POINT ( 'NONE',  ( 0.000000000000000000, 0.000000000000000000, 0.000000000000000000 ) ) ;
#6844=CARTESIAN_POINT ( 'NONE',  ( 0.000000000000000000, -60.65279801375299229, -63.75921967137679047 ) ) ;
#6845=VERTEX_POINT ( 'NONE', #17182 ) ;
#6846=AXIS2_PLACEMENT_3D ( 'NONE', #19295, #17536, #950 ) ;
#6847=CARTESIAN_POINT ( 'NONE',  ( 0.000000000000000000, -57.53593069156421791, 72.42963261300944566 ) ) ;
#6850=ORIENTED_EDGE ( 'NONE', *, *, #7196, .F. ) ;
#6851=VECTOR ( 'NONE', #8322, 1000.000000000000000 ) ;
#6852=ORIENTED_EDGE ( 'NONE', *, *, #4193, .F. ) ;
#6855=ORIENTED_EDGE ( 'NONE', *, *, #2840, .T. ) ;
#6856=CARTESIAN_POINT ( 'NONE',  ( 0.000000000000000000, 0.000000000000000000, 0.000000000000000000 ) ) ;
#6858=DIRECTION ( 'NONE',  ( -1.000000000000000000, -0.000000000000000000, 0.000000000000000000 ) ) ;
#6859=CARTESIAN_POINT ( 'NONE',  ( 10.00000000000000000, 0.000000000000000000, 0.000000000000000000 ) ) ;
#6860=DIRECTION ( 'NONE',  ( -1.000000000000000000, 0.000000000000000000, 0.000000000000000000 ) ) ;
#6863=EDGE_CURVE ( 'NONE', #14822, #8942, #15290, .T. ) ;
#6864=VERTEX_POINT ( 'NONE', #2041 ) ;
#6866=CIRCLE ( 'NONE', #18500, 44.99999999999999289 ) ;
#6867=FACE_OUTER_BOUND ( 'NONE', #12716, .T. ) ;
#6868=ORIENTED_EDGE ( 'NONE', *, *, #17682, .T. ) ;
#6869=ADVANCED_FACE ( 'NONE', ( #8780 ), #386, .F. ) ;
#6870=EDGE_LOOP ( 'NONE', ( #925, #5663, #4204, #5952 ) ) ;
#6871=LINE ( 'NONE', #8739, #13436 ) ;
#6874=CIRCLE ( 'NONE', #19212, 44.99999999999999289 ) ;
#6875=CYLINDRICAL_SURFACE ( 'NONE', #650, 44.99999999999999289 ) ;
#6876=ORIENTED_EDGE ( 'NONE', *, *, #12022, .F. ) ;
#6881=ORIENTED_EDGE ( 'NONE', *, *, #17706, .T. ) ;
#6882=VECTOR ( 'NONE', #8201, 1000.000000000000000 ) ;
#6883=CARTESIAN_POINT ( 'NONE',  ( 10.00000000000000000, 0.000000000000000000, 0.000000000000000000 ) ) ;
#6885=CYLINDRICAL_SURFACE ( 'NONE', #10167, 88.00000000000000000 ) ;
#6886=CARTESIAN_POINT ( 'NONE',  ( 10.00000000000000000, -18.94217447942616417, 85.93715160505946926 ) ) ;
#6889=DIRECTION ( 'NONE',  ( 0.000000000000000000, -0.9848077530122096857, 0.1736481776669207000 ) ) ;
#6890=AXIS2_PLACEMENT_3D ( 'NONE', #868, #4291, #7503 ) ;
#6891=EDGE_CURVE ( 'NONE', #12476, #12259, #8272, .T. ) ;
#6892=CIRCLE ( 'NONE', #6534, 44.99999999999999289 ) ;
#6893=ADVANCED_FACE ( 'NONE', ( #15850 ), #15944, .F. ) ;
#6894=VERTEX_POINT ( 'NONE', #21153 ) ;
#6895=AXIS2_PLACEMENT_3D ( 'NONE', #19312, #8921, #4178 ) ;
#6897=CIRCLE ( 'NONE', #12876, 88.00000000000000000 ) ;
#6900=ORIENTED_EDGE ( 'NONE', *, *, #10393, .T. ) ;
#6902=ORIENTED_EDGE ( 'NONE', *, *, #2017, .T. ) ;
#6903=EDGE_CURVE ( 'NONE', #15915, #10612, #6166, .T. ) ;
#6904=VERTEX_POINT ( 'NONE', #7551 ) ;
#6905=DIRECTION ( 'NONE',  ( 1.000000000000000000, 0.000000000000000000, 0.000000000000000000 ) ) ;
#6908=VERTEX_POINT ( 'NONE', #2688 ) ;
#6910=CARTESIAN_POINT ( 'NONE',  ( 0.000000000000000000, -29.29369617358527833, 87.74003855418389719 ) ) ;
#6912=AXIS2_PLACEMENT_3D ( 'NONE', #18864, #17419, #9008 ) ;
#6913=EDGE_CURVE ( 'NONE', #14686, #3581, #1214, .T. ) ;
#6916=DIRECTION ( 'NONE',  ( 0.000000000000000000, 0.9993908270190958731, -0.03489949670249761771 ) ) ;
#6918=CARTESIAN_POINT ( 'NONE',  ( 5.000000000000000000, -51.18896083639217665, -71.57995730992236361 ) ) ;
#6920=ADVANCED_FACE ( 'NONE', ( #17721 ), #7348, .F. ) ;
#6921=EDGE_CURVE ( 'NONE', #1002, #18170, #846, .T. ) ;
#6923=ORIENTED_EDGE ( 'NONE', *, *, #18059, .T. ) ;
#6924=VECTOR ( 'NONE', #15055, 1000.000000000000000 ) ;
#6925=CARTESIAN_POINT ( 'NONE',  ( 0.000000000000000000, -35.34277389771592226, 85.48288328206373876 ) ) ;
#6926=ADVANCED_FACE ( 'NONE', ( #17831 ), #5903, .F. ) ;
#6928=ORIENTED_EDGE ( 'NONE', *, *, #21625, .T. ) ;
#6930=CIRCLE ( 'NONE', #19978, 88.00000000000000000 ) ;
#6931=CIRCLE ( 'NONE', #4438, 44.99999999999998579 ) ;
#6932=CARTESIAN_POINT ( 'NONE',  ( -10.00000000000000000, 0.000000000000000000, 0.000000000000000000 ) ) ;
#6933=ORIENTED_EDGE ( 'NONE', *, *, #4737, .F. ) ;
#6934=DIRECTION ( 'NONE',  ( -1.000000000000000000, -0.000000000000000000, 0.000000000000000000 ) ) ;
#6935=CARTESIAN_POINT ( 'NONE',  ( -10.00000000000000000, 0.000000000000000000, 0.000000000000000000 ) ) ;
#6937=EDGE_CURVE ( 'NONE', #12778, #2153, #20613, .T. ) ;
#6938=ORIENTED_EDGE ( 'NONE', *, *, #13797, .T. ) ;
#6939=ORIENTED_EDGE ( 'NONE', *, *, #10591, .F. ) ;
#6940=EDGE_LOOP ( 'NONE', ( #6440, #11152, #15220, #3878 ) ) ;
#6941=CARTESIAN_POINT ( 'NONE',  ( 10.00000000000000000, 2.481790431839256517, 92.46770094066594936 ) ) ;
#6942=EDGE_CURVE ( 'NONE', #15480, #11066, #9199, .T. ) ;
#6943=ORIENTED_EDGE ( 'NONE', *, *, #11129, .F. ) ;
#6944=DIRECTION ( 'NONE',  ( 0.000000000000000000, 0.9702957262759954737, 0.2419218955996715048 ) ) ;
#6945=DIRECTION ( 'NONE',  ( -1.000000000000000000, 0.000000000000000000, 0.000000000000000000 ) ) ;
#6950=EDGE_CURVE ( 'NONE', #7932, #15044, #505, .T. ) ;
#6952=CARTESIAN_POINT ( 'NONE',  ( 10.00000000000000000, -84.80486432185169576, -36.94008646920480743 ) ) ;
#6953=CARTESIAN_POINT ( 'NONE',  ( 0.000000000000000000, 0.000000000000000000, 0.000000000000000000 ) ) ;
#6955=DIRECTION ( 'NONE',  ( -1.000000000000000000, 0.000000000000000000, 0.000000000000000000 ) ) ;
#6956=EDGE_CURVE ( 'NONE', #16874, #10308, #12848, .T. ) ;
#6958=DIRECTION ( 'NONE',  ( 0.000000000000000000, 0.000000000000000000, -1.000000000000000000 ) ) ;
#6960=CIRCLE ( 'NONE', #20009, 44.99999999999999289 ) ;
#6962=DIRECTION ( 'NONE',  ( -1.000000000000000000, -0.000000000000000000, -0.000000000000000000 ) ) ;
#6964=ORIENTED_EDGE ( 'NONE', *, *, #1620, .T. ) ;
#6965=ORIENTED_EDGE ( 'NONE', *, *, #9467, .T. ) ;
#6966=ORIENTED_EDGE ( 'NONE', *, *, #8548, .T. ) ;
#6968=EDGE_LOOP ( 'NONE', ( #2823, #18183, #2557, #12321 ) ) ;
#6970=CARTESIAN_POINT ( 'NONE',  ( 0.000000000000000000, 76.53853822674039975, -43.42639941457040464 ) ) ;
#6971=EDGE_CURVE ( 'NONE', #9520, #15915, #21319, .T. ) ;
#6972=CIRCLE ( 'NONE', #3080, 44.99999999999999289 ) ;
#6973=CARTESIAN_POINT ( 'NONE',  ( 10.00000000000000000, 84.90234713953992696, -5.175025661882965089 ) ) ;
#6975=CARTESIAN_POINT ( 'NONE',  ( 0.000000000000000000, -41.89587599971492438, -77.38692120905515992 ) ) ;
#6976=DIRECTION ( 'NONE',  ( 0.000000000000000000, 0.2079116908177599254, -0.9781476007338055778 ) ) ;
#6977=AXIS2_PLACEMENT_3D ( 'NONE', #11146, #4845, #14794 ) ;
#6978=DIRECTION ( 'NONE',  ( 0.000000000000000000, 0.000000000000000000, 1.000000000000000000 ) ) ;
#6980=ORIENTED_EDGE ( 'NONE', *, *, #13637, .T. ) ;
#6981=FACE_OUTER_BOUND ( 'NONE', #20229, .T. ) ;
#6984=CIRCLE ( 'NONE', #12622, 45.00000000000000000 ) ;
#6985=CARTESIAN_POINT ( 'NONE',  ( 10.00000000000000000, 32.56745702629844175, -78.57830605990621109 ) ) ;
#6987=VERTEX_POINT ( 'NONE', #7451 ) ;
#6988=CIRCLE ( 'NONE', #11915, 44.99999999999998579 ) ;
#6989=CARTESIAN_POINT ( 'NONE',  ( 0.000000000000000000, -83.35585896458606214, -16.94078559808036033 ) ) ;
#6990=EDGE_LOOP ( 'NONE', ( #11368, #1646, #11315, #8851 ) ) ;
#6991=DIRECTION ( 'NONE',  ( 0.000000000000000000, 0.000000000000000000, 1.000000000000000000 ) ) ;
#6992=CYLINDRICAL_SURFACE ( 'NONE', #19601, 92.50100000000000477 ) ;
#6994=CARTESIAN_POINT ( 'NONE',  ( 0.000000000000000000, -84.19736439813780748, -38.30455363801015523 ) ) ;
#6995=EDGE_CURVE ( 'NONE', #20174, #6864, #5796, .T. ) ;
#6998=LINE ( 'NONE', #12174, #13327 ) ;
#7000=VECTOR ( 'NONE', #2472, 1000.000000000000000 ) ;
#7001=AXIS2_PLACEMENT_3D ( 'NONE', #21803, #9638, #1267 ) ;
#7002=VECTOR ( 'NONE', #10777, 1000.000000000000000 ) ;
#7004=AXIS2_PLACEMENT_3D ( 'NONE', #20688, #13498, #6889 ) ;
#7006=FACE_OUTER_BOUND ( 'NONE', #1885, .T. ) ;
#7008=CARTESIAN_POINT ( 'NONE',  ( 10.00000000000000000, 60.65655256511237781, 59.63197188857542841 ) ) ;
#7010=AXIS2_PLACEMENT_3D ( 'NONE', #9703, #21760, #18571 ) ;
#7012=CARTESIAN_POINT ( 'NONE',  ( 0.000000000000000000, 0.000000000000000000, 0.000000000000000000 ) ) ;
#7016=ORIENTED_EDGE ( 'NONE', *, *, #19736, .F. ) ;
#7019=AXIS2_PLACEMENT_3D ( 'NONE', #1992, #8733, #17018 ) ;
#7020=DIRECTION ( 'NONE',  ( -1.000000000000000000, -0.000000000000000000, -0.000000000000000000 ) ) ;
#7022=DIRECTION ( 'NONE',  ( 0.000000000000000000, 0.4067366430758009854, -0.9135454576426005335 ) ) ;
#7024=ADVANCED_FACE ( 'NONE', ( #12515 ), #19267, .F. ) ;
#7025=CARTESIAN_POINT ( 'NONE',  ( 10.00000000000000000, 52.96496548042853192, 66.55750800669373746 ) ) ;
#7026=FACE_OUTER_BOUND ( 'NONE', #13111, .T. ) ;
#7029=EDGE_CURVE ( 'NONE', #13846, #16223, #9301, .T. ) ;
#7030=CIRCLE ( 'NONE', #10526, 44.99999999999999289 ) ;
#7035=FACE_OUTER_BOUND ( 'NONE', #5300, .T. ) ;
#7036=VERTEX_POINT ( 'NONE', #6125 ) ;
#7039=ORIENTED_EDGE ( 'NONE', *, *, #8929, .T. ) ;
#7041=EDGE_LOOP ( 'NONE', ( #12543, #13663, #10360, #11595 ) ) ;
#7042=EDGE_CURVE ( 'NONE', #21518, #18065, #21334, .T. ) ;
#7043=EDGE_CURVE ( 'NONE', #21588, #13276, #19209, .T. ) ;
#7045=EDGE_CURVE ( 'NONE', #2607, #12265, #3688, .T. ) ;
#7046=DIRECTION ( 'NONE',  ( -1.000000000000000000, 0.000000000000000000, 0.000000000000000000 ) ) ;
#7048=CARTESIAN_POINT ( 'NONE',  ( 5.000000000000002665, 86.54587337002898551, -15.93147207946920396 ) ) ;
#7049=AXIS2_PLACEMENT_3D ( 'NONE', #19375, #16494, #14832 ) ;
#7050=EDGE_CURVE ( 'NONE', #5365, #9724, #14617, .T. ) ;
#7051=DIRECTION ( 'NONE',  ( 0.000000000000000000, 0.000000000000000000, 1.000000000000000000 ) ) ;
#7055=CIRCLE ( 'NONE', #9487, 92.50100000000000477 ) ;
#7058=CARTESIAN_POINT ( 'NONE',  ( -10.00000000000000000, 0.000000000000000000, 0.000000000000000000 ) ) ;
#7059=DIRECTION ( 'NONE',  ( 0.000000000000000000, -0.9945218953682742891, 0.1045284632676436315 ) ) ;
#7060=ORIENTED_EDGE ( 'NONE', *, *, #3381, .F. ) ;
#7061=LINE ( 'NONE', #15440, #19389 ) ;
#7062=EDGE_CURVE ( 'NONE', #9931, #20877, #4030, .T. ) ;
#7063=DIRECTION ( 'NONE',  ( 0.000000000000000000, 0.000000000000000000, 1.000000000000000000 ) ) ;
#7064=EDGE_CURVE ( 'NONE', #7682, #9443, #4049, .T. ) ;
#7065=DIRECTION ( 'NONE',  ( -1.000000000000000000, -0.000000000000000000, 0.000000000000000000 ) ) ;
#7068=ORIENTED_EDGE ( 'NONE', *, *, #331, .F. ) ;
#7071=AXIS2_PLACEMENT_3D ( 'NONE', #14872, #21605, #4494 ) ;
#7072=ADVANCED_FACE ( 'NONE', ( #9744 ), #111, .F. ) ;
#7075=ORIENTED_EDGE ( 'NONE', *, *, #18685, .F. ) ;
#7076=DIRECTION ( 'NONE',  ( 1.000000000000000000, 0.000000000000000000, 0.000000000000000000 ) ) ;
#7077=ADVANCED_FACE ( 'NONE', ( #9629 ), #13587, .F. ) ;
#7078=ORIENTED_EDGE ( 'NONE', *, *, #4782, .T. ) ;
#7082=CARTESIAN_POINT ( 'NONE',  ( 10.00000000000000000, 0.000000000000000000, 0.000000000000000000 ) ) ;
#7085=VECTOR ( 'NONE', #16262, 1000.000000000000000 ) ;
#7087=CARTESIAN_POINT ( 'NONE',  ( 10.00000000000000000, 69.74988376404090218, -53.65588238863266213 ) ) ;
#7088=EDGE_CURVE ( 'NONE', #5100, #2139, #5465, .T. ) ;
#7089=EDGE_LOOP ( 'NONE', ( #21493, #4362, #11442, #5278 ) ) ;
#7092=EDGE_LOOP ( 'NONE', ( #6486, #11924, #18399, #19334 ) ) ;
#7094=EDGE_CURVE ( 'NONE', #13650, #20538, #16275, .T. ) ;
#7096=CARTESIAN_POINT ( 'NONE',  ( 10.00000000000000000, -84.79630770241078608, -6.691460262316255125 ) ) ;
#7099=VERTEX_POINT ( 'NONE', #12843 ) ;
#7101=VERTEX_POINT ( 'NONE', #7884 ) ;
#7104=FACE_OUTER_BOUND ( 'NONE', #15204, .T. ) ;
#7105=CARTESIAN_POINT ( 'NONE',  ( 10.00000000000000000, -62.44821182181044605, -68.23969402963567177 ) ) ;
#7108=DIRECTION ( 'NONE',  ( 1.000000000000000000, 0.000000000000000000, 0.000000000000000000 ) ) ;
#7110=ORIENTED_EDGE ( 'NONE', *, *, #17293, .T. ) ;
#7111=DIRECTION ( 'NONE',  ( -1.000000000000000000, 0.000000000000000000, -0.000000000000000000 ) ) ;
#7112=CARTESIAN_POINT ( 'NONE',  ( 0.000000000000000000, -83.48638250753248258, 27.82128566055087049 ) ) ;
#7113=ORIENTED_EDGE ( 'NONE', *, *, #13345, .T. ) ;
#7116=DIRECTION ( 'NONE',  ( 0.000000000000000000, 0.000000000000000000, 1.000000000000000000 ) ) ;
#7119=LINE ( 'NONE', #12400, #21678 ) ;
#7120=DIRECTION ( 'NONE',  ( 0.000000000000000000, -0.9848077530122062440, -0.1736481776669404620 ) ) ;
#7121=DIRECTION ( 'NONE',  ( 0.000000000000000000, 0.000000000000000000, -1.000000000000000000 ) ) ;
#7122=LINE ( 'NONE', #13852, #20051 ) ;
#7124=DIRECTION ( 'NONE',  ( 1.000000000000000000, -0.000000000000000000, -0.000000000000000000 ) ) ;
#7125=CARTESIAN_POINT ( 'NONE',  ( 10.00000000000000000, -75.45728100697627383, 39.26051685139039193 ) ) ;
#7129=ADVANCED_FACE ( 'NONE', ( #19595 ), #1141, .F. ) ;
#7130=VERTEX_POINT ( 'NONE', #16384 ) ;
#7139=ORIENTED_EDGE ( 'NONE', *, *, #14360, .F. ) ;
#7141=ORIENTED_EDGE ( 'NONE', *, *, #1792, .T. ) ;
#7143=CYLINDRICAL_SURFACE ( 'NONE', #11793, 92.50100000000000477 ) ;
#7145=DIRECTION ( 'NONE',  ( -1.000000000000000000, 0.000000000000000000, -0.000000000000000000 ) ) ;
#7146=CARTESIAN_POINT ( 'NONE',  ( 10.00000000000000000, 51.10509369859540385, -77.10190917907144126 ) ) ;
#7148=CIRCLE ( 'NONE', #20199, 88.00000000000000000 ) ;
#7150=VERTEX_POINT ( 'NONE', #19811 ) ;
#7152=VECTOR ( 'NONE', #7291, 1000.000000000000000 ) ;
#7156=ADVANCED_FACE ( 'NONE', ( #8108 ), #10164, .F. ) ;
#7157=CIRCLE ( 'NONE', #3619, 88.00000000000000000 ) ;
#7158=CARTESIAN_POINT ( 'NONE',  ( 10.00000000000000000, 29.29369617358583255, -87.74003855418371245 ) ) ;
#7159=ORIENTED_EDGE ( 'NONE', *, *, #14086, .F. ) ;
#7160=EDGE_CURVE ( 'NONE', #12492, #19254, #5117, .T. ) ;
#7161=CYLINDRICAL_SURFACE ( 'NONE', #20095, 45.00000000000000000 ) ;
#7162=VERTEX_POINT ( 'NONE', #20769 ) ;
#7164=VERTEX_POINT ( 'NONE', #439 ) ;
#7165=ORIENTED_EDGE ( 'NONE', *, *, #5967, .T. ) ;
#7167=EDGE_CURVE ( 'NONE', #17904, #19570, #7567, .T. ) ;
#7168=DIRECTION ( 'NONE',  ( 0.000000000000000000, 0.000000000000000000, 1.000000000000000000 ) ) ;
#7169=VECTOR ( 'NONE', #6858, 1000.000000000000000 ) ;
#7171=CARTESIAN_POINT ( 'NONE',  ( 5.000000000000002665, -12.90135963484022241, -87.04915231966658951 ) ) ;
#7172=CARTESIAN_POINT ( 'NONE',  ( 10.00000000000000000, 64.66851233300727131, 55.25552418572984692 ) ) ;
#7173=DIRECTION ( 'NONE',  ( -1.000000000000000000, 0.000000000000000000, 0.000000000000000000 ) ) ;
#7174=VECTOR ( 'NONE', #5563, 1000.000000000000000 ) ;
#7176=ADVANCED_FACE ( 'NONE', ( #1990 ), #18896, .F. ) ;
#7179=DIRECTION ( 'NONE',  ( 0.000000000000000000, 0.000000000000000000, 1.000000000000000000 ) ) ;
#7180=DIRECTION ( 'NONE',  ( 1.000000000000000000, 0.000000000000000000, 0.000000000000000000 ) ) ;
#7182=( GEOMETRIC_REPRESENTATION_CONTEXT ( 3 ) GLOBAL_UNCERTAINTY_ASSIGNED_CONTEXT ( ( #18078 ) ) GLOBAL_UNIT_ASSIGNED_CONTEXT ( ( #18440, #10019, #8164 ) ) REPRESENTATION_CONTEXT ( 'NONE', 'WORKASPACE' ) );
#7183=ADVANCED_FACE ( 'NONE', ( #13811 ), #17242, .F. ) ;
#7184=EDGE_LOOP ( 'NONE', ( #19721, #15620, #6633, #18465 ) ) ;
#7186=AXIS2_PLACEMENT_3D ( 'NONE', #4188, #18076, #4699 ) ;
#7192=DIRECTION ( 'NONE',  ( -1.000000000000000000, 0.000000000000000000, 0.000000000000000000 ) ) ;
#7194=VERTEX_POINT ( 'NONE', #5522 ) ;
#7196=EDGE_CURVE ( 'NONE', #8891, #3730, #3344, .T. ) ;
#7199=ORIENTED_EDGE ( 'NONE', *, *, #18702, .T. ) ;
#7200=ADVANCED_FACE ( 'NONE', ( #12043 ), #4081, .F. ) ;
#7202=CYLINDRICAL_SURFACE ( 'NONE', #8551, 44.99999999999998579 ) ;
#7204=DIRECTION ( 'NONE',  ( -1.000000000000000000, -0.000000000000000000, 0.000000000000000000 ) ) ;
#7206=LINE ( 'NONE', #3777, #10800 ) ;
#7207=EDGE_CURVE ( 'NONE', #1843, #13321, #1231, .T. ) ;
#7212=DIRECTION ( 'NONE',  ( -1.000000000000000000, 0.000000000000000000, -0.000000000000000000 ) ) ;
#7214=AXIS2_PLACEMENT_3D ( 'NONE', #10104, #16850, #1719 ) ;
#7215=EDGE_CURVE ( 'NONE', #16161, #4858, #8731, .T. ) ;
#7217=AXIS2_PLACEMENT_3D ( 'NONE', #20519, #6945, #18541 ) ;
#7218=CARTESIAN_POINT ( 'NONE',  ( 10.00000000000000000, -83.03980459022491800, 18.42770452393216374 ) ) ;
#7219=EDGE_LOOP ( 'NONE', ( #13290, #14269, #20218, #3954 ) ) ;
#7220=DIRECTION ( 'NONE',  ( 0.000000000000000000, 0.000000000000000000, 1.000000000000000000 ) ) ;
#7221=ORIENTED_EDGE ( 'NONE', *, *, #14476, .F. ) ;
#7222=VECTOR ( 'NONE', #4237, 1000.000000000000000 ) ;
#7223=CARTESIAN_POINT ( 'NONE',  ( 0.000000000000000000, 0.000000000000000000, 0.000000000000000000 ) ) ;
#7224=VERTEX_POINT ( 'NONE', #7403 ) ;
#7225=ORIENTED_EDGE ( 'NONE', *, *, #21793, .T. ) ;
#7226=DIRECTION ( 'NONE',  ( -1.000000000000000000, -0.000000000000000000, -0.000000000000000000 ) ) ;
#7227=DIRECTION ( 'NONE',  ( 0.000000000000000000, 0.000000000000000000, 1.000000000000000000 ) ) ;
#7228=VECTOR ( 'NONE', #17565, 1000.000000000000000 ) ;
#7229=CARTESIAN_POINT ( 'NONE',  ( -10.00000000000000000, 0.000000000000000000, 0.000000000000000000 ) ) ;
#7230=DIRECTION ( 'NONE',  ( -1.000000000000000000, -0.000000000000000000, -0.000000000000000000 ) ) ;
#7232=CYLINDRICAL_SURFACE ( 'NONE', #9016, 88.00000000000000000 ) ;
#7235=EDGE_CURVE ( 'NONE', #9876, #13595, #5416, .T. ) ;
#7236=CARTESIAN_POINT ( 'NONE',  ( 10.00000000000000000, 2.208823992044147033, 85.03123271466937183 ) ) ;
#7237=LINE ( 'NONE', #5361, #8176 ) ;
#7239=CIRCLE ( 'NONE', #19574, 44.99999999999998579 ) ;
#7240=ORIENTED_EDGE ( 'NONE', *, *, #5534, .F. ) ;
#7241=VECTOR ( 'NONE', #19422, 1000.000000000000000 ) ;
#7242=DIRECTION ( 'NONE',  ( 1.000000000000000000, -0.000000000000000000, 0.000000000000000000 ) ) ;
#7243=ORIENTED_EDGE ( 'NONE', *, *, #4508, .F. ) ;
#7244=CARTESIAN_POINT ( 'NONE',  ( 0.000000000000000000, 84.90234713953985590, 5.175025661884123274 ) ) ;
#7245=ORIENTED_EDGE ( 'NONE', *, *, #8371, .T. ) ;
#7247=CIRCLE ( 'NONE', #19591, 44.99999999999999289 ) ;
#7250=AXIS2_PLACEMENT_3D ( 'NONE', #3467, #20809, #2556 ) ;
#7251=ORIENTED_EDGE ( 'NONE', *, *, #19746, .F. ) ;
#7252=CIRCLE ( 'NONE', #19596, 92.50100000000000477 ) ;
#7256=ORIENTED_EDGE ( 'NONE', *, *, #19273, .T. ) ;
#7257=ORIENTED_EDGE ( 'NONE', *, *, #8200, .F. ) ;
#7258=LINE ( 'NONE', #8893, #21303 ) ;
#7259=EDGE_LOOP ( 'NONE', ( #10898, #6227, #3781, #14499 ) ) ;
#7261=DIRECTION ( 'NONE',  ( 0.000000000000000000, 0.000000000000000000, 1.000000000000000000 ) ) ;
#7263=CARTESIAN_POINT ( 'NONE',  ( 0.000000000000000000, -92.49798535263882115, -0.7467976319030308341 ) ) ;
#7264=CARTESIAN_POINT ( 'NONE',  ( 0.000000000000000000, -32.56745702629687855, -78.57830605990686479 ) ) ;
#7265=DIRECTION ( 'NONE',  ( -1.000000000000000000, -0.000000000000000000, -0.000000000000000000 ) ) ;
#7271=CIRCLE ( 'NONE', #5853, 88.00000000000000000 ) ;
#7272=CARTESIAN_POINT ( 'NONE',  ( 10.00000000000000000, -61.60362715319078575, 62.84101464466223774 ) ) ;
#7273=AXIS2_PLACEMENT_3D ( 'NONE', #5729, #2514, #3856 ) ;
#7275=CARTESIAN_POINT ( 'NONE',  ( 10.00000000000000000, 89.12061559554365431, -24.77803214283454736 ) ) ;
#7276=ORIENTED_EDGE ( 'NONE', *, *, #9486, .F. ) ;
#7277=CARTESIAN_POINT ( 'NONE',  ( 0.000000000000000000, -64.95266917914358373, 59.37298010462950515 ) ) ;
#7279=DIRECTION ( 'NONE',  ( 0.000000000000000000, 0.000000000000000000, 1.000000000000000000 ) ) ;
#7282=ORIENTED_EDGE ( 'NONE', *, *, #19302, .T. ) ;
#7284=ORIENTED_EDGE ( 'NONE', *, *, #21055, .F. ) ;
#7285=CARTESIAN_POINT ( 'NONE',  ( 10.00000000000000000, 0.000000000000000000, 0.000000000000000000 ) ) ;
#7287=ORIENTED_EDGE ( 'NONE', *, *, #473, .F. ) ;
#7288=AXIS2_PLACEMENT_3D ( 'NONE', #83, #16657, #15211 ) ;
#7291=DIRECTION ( 'NONE',  ( -1.000000000000000000, 0.000000000000000000, 0.000000000000000000 ) ) ;
#7293=FACE_OUTER_BOUND ( 'NONE', #11482, .T. ) ;
#7294=CARTESIAN_POINT ( 'NONE',  ( 10.00000000000000000, 37.96946988134172329, 76.11510229470873412 ) ) ;
#7297=CARTESIAN_POINT ( 'NONE',  ( 5.000000000000000000, 86.77540292929701593, 14.62974526292747868 ) ) ;
#7299=ORIENTED_EDGE ( 'NONE', *, *, #10707, .F. ) ;
#7301=LINE ( 'NONE', #3644, #17518 ) ;
#7303=ORIENTED_EDGE ( 'NONE', *, *, #5716, .F. ) ;
#7304=ORIENTED_EDGE ( 'NONE', *, *, #16785, .F. ) ;
#7306=EDGE_CURVE ( 'NONE', #4889, #8180, #10041, .T. ) ;
#7307=DIRECTION ( 'NONE',  ( -1.000000000000000000, -0.000000000000000000, -0.000000000000000000 ) ) ;
#7309=ORIENTED_EDGE ( 'NONE', *, *, #2100, .F. ) ;
#7311=CIRCLE ( 'NONE', #19657, 44.99999999999999289 ) ;
#7314=EDGE_CURVE ( 'NONE', #11159, #2487, #10404, .T. ) ;
#7316=CARTESIAN_POINT ( 'NONE',  ( 10.00000000000000000, 0.000000000000000000, 0.000000000000000000 ) ) ;
#7317=CIRCLE ( 'NONE', #20012, 88.00000000000000000 ) ;
#7318=DIRECTION ( 'NONE',  ( -1.000000000000000000, -0.000000000000000000, -0.000000000000000000 ) ) ;
#7319=EDGE_CURVE ( 'NONE', #12668, #18181, #20993, .T. ) ;
#7321=DIRECTION ( 'NONE',  ( -1.000000000000000000, -0.000000000000000000, -0.000000000000000000 ) ) ;
#7322=DIRECTION ( 'NONE',  ( -1.000000000000000000, -0.000000000000000000, 0.000000000000000000 ) ) ;
#7323=LINE ( 'NONE', #21121, #21722 ) ;
#7326=ORIENTED_EDGE ( 'NONE', *, *, #5449, .T. ) ;
#7327=EDGE_CURVE ( 'NONE', #8870, #20207, #14278, .T. ) ;
#7328=CIRCLE ( 'NONE', #11913, 88.00000000000000000 ) ;
#7330=CYLINDRICAL_SURFACE ( 'NONE', #10517, 44.99999999999998579 ) ;
#7331=EDGE_CURVE ( 'NONE', #791, #17102, #4764, .T. ) ;
#7332=AXIS2_PLACEMENT_3D ( 'NONE', #9657, #1065, #7803 ) ;
#7333=DIRECTION ( 'NONE',  ( 1.000000000000000000, 0.000000000000000000, 0.000000000000000000 ) ) ;
#7334=EDGE_LOOP ( 'NONE', ( #13793, #15353, #357, #15176 ) ) ;
#7335=CARTESIAN_POINT ( 'NONE',  ( 5.000000000000000000, 57.06999622551805373, 66.98518889142101784 ) ) ;
#7336=ORIENTED_EDGE ( 'NONE', *, *, #5005, .T. ) ;
#7337=EDGE_CURVE ( 'NONE', #15117, #2159, #17119, .T. ) ;
#7340=ORIENTED_EDGE ( 'NONE', *, *, #11805, .T. ) ;
#7341=CARTESIAN_POINT ( 'NONE',  ( 10.00000000000000000, 46.89573839703275127, 79.73220629831503459 ) ) ;
#7342=EDGE_CURVE ( 'NONE', #5623, #11894, #20983, .T. ) ;
#7343=DIRECTION ( 'NONE',  ( -1.000000000000000000, -0.000000000000000000, -0.000000000000000000 ) ) ;
#7346=DIRECTION ( 'NONE',  ( 0.000000000000000000, 0.000000000000000000, 1.000000000000000000 ) ) ;
#7347=CIRCLE ( 'NONE', #5231, 88.00000000000000000 ) ;
#7348=CYLINDRICAL_SURFACE ( 'NONE', #8965, 88.00000000000000000 ) ;
#7349=AXIS2_PLACEMENT_3D ( 'NONE', #18717, #15265, #5444 ) ;
#7351=CARTESIAN_POINT ( 'NONE',  ( -10.00000000000000000, 0.000000000000000000, 0.000000000000000000 ) ) ;
#7352=VERTEX_POINT ( 'NONE', #16115 ) ;
#7353=DIRECTION ( 'NONE',  ( 0.000000000000000000, -0.8290375725550350738, -0.5591929034707566748 ) ) ;
#7355=EDGE_CURVE ( 'NONE', #9424, #6845, #7589, .T. ) ;
#7357=ORIENTED_EDGE ( 'NONE', *, *, #7952, .T. ) ;
#7358=CIRCLE ( 'NONE', #11944, 44.99999999999999289 ) ;
#7359=CARTESIAN_POINT ( 'NONE',  ( 0.000000000000000000, 75.87763420127893710, -44.57111876559645225 ) ) ;
#7361=AXIS2_PLACEMENT_3D ( 'NONE', #8421, #3445, #10064 ) ;
#7363=AXIS2_PLACEMENT_3D ( 'NONE', #3103, #14817, #4761 ) ;
#7364=VERTEX_POINT ( 'NONE', #11257 ) ;
#7365=EDGE_CURVE ( 'NONE', #8963, #13997, #10923, .T. ) ;
#7367=ORIENTED_EDGE ( 'NONE', *, *, #2882, .T. ) ;
#7368=ORIENTED_EDGE ( 'NONE', *, *, #8004, .F. ) ;
#7370=DIRECTION ( 'NONE',  ( 1.000000000000000000, 0.000000000000000000, 0.000000000000000000 ) ) ;
#7372=ORIENTED_EDGE ( 'NONE', *, *, #13338, .F. ) ;
#7376=CARTESIAN_POINT ( 'NONE',  ( 10.00000000000000000, -92.32475887865429343, 5.707354816230212791 ) ) ;
#7378=CIRCLE ( 'NONE', #15121, 44.99999999999999289 ) ;
#7379=CIRCLE ( 'NONE', #12659, 92.50099999999999056 ) ;
#7381=ORIENTED_EDGE ( 'NONE', *, *, #2755, .F. ) ;
#7383=CARTESIAN_POINT ( 'NONE',  ( 0.000000000000000000, -33.95793648385871677, 86.04239391577978324 ) ) ;
#7384=CYLINDRICAL_SURFACE ( 'NONE', #16769, 88.00000000000000000 ) ;
#7385=DIRECTION ( 'NONE',  ( 0.000000000000000000, 0.000000000000000000, 1.000000000000000000 ) ) ;
#7386=ORIENTED_EDGE ( 'NONE', *, *, #162, .T. ) ;
#7387=CARTESIAN_POINT ( 'NONE',  ( 5.000000000000000000, 24.89070495400736505, 84.40647372620510680 ) ) ;
#7389=LINE ( 'NONE', #15660, #8768 ) ;
#7390=ORIENTED_EDGE ( 'NONE', *, *, #19282, .F. ) ;
#7391=CIRCLE ( 'NONE', #7049, 44.99999999999999289 ) ;
#7393=ORIENTED_EDGE ( 'NONE', *, *, #17705, .T. ) ;
#7395=CARTESIAN_POINT ( 'NONE',  ( 10.00000000000000000, -48.19312842678519360, 70.09002648625178722 ) ) ;
#7397=CARTESIAN_POINT ( 'NONE',  ( 0.000000000000000000, 0.000000000000000000, 0.000000000000000000 ) ) ;
#7399=CARTESIAN_POINT ( 'NONE',  ( 10.00000000000000000, -10.41137886060169038, 91.91321010181843576 ) ) ;
#7403=CARTESIAN_POINT ( 'NONE',  ( 0.000000000000000000, -56.05743251323904985, 67.83483072893783117 ) ) ;
#7404=CARTESIAN_POINT ( 'NONE',  ( 0.000000000000000000, 35.34277389771533961, 85.48288328206398035 ) ) ;
#7407=CIRCLE ( 'NONE', #7768, 92.50099999999999056 ) ;
#7408=ORIENTED_EDGE ( 'NONE', *, *, #4563, .T. ) ;
#7412=ORIENTED_EDGE ( 'NONE', *, *, #14599, .T. ) ;
#7413=ORIENTED_EDGE ( 'NONE', *, *, #4894, .T. ) ;
#7415=ORIENTED_EDGE ( 'NONE', *, *, #4865, .F. ) ;
#7416=EDGE_CURVE ( 'NONE', #8339, #20733, #9684, .T. ) ;
#7420=CIRCLE ( 'NONE', #17314, 88.00000000000000000 ) ;
#7422=DIRECTION ( 'NONE',  ( 0.000000000000000000, 0.06975647374411846069, 0.9975640502598246417 ) ) ;
#7425=DIRECTION ( 'NONE',  ( 0.000000000000000000, -0.4694715627858975782, 0.8829475928589234357 ) ) ;
#7426=CARTESIAN_POINT ( 'NONE',  ( 0.000000000000000000, -0.6609040254617754018, 87.99751818016873983 ) ) ;
#7428=CARTESIAN_POINT ( 'NONE',  ( 0.000000000000000000, -83.89484365856893078, -26.56417150043033359 ) ) ;
#7429=CARTESIAN_POINT ( 'NONE',  ( 0.000000000000000000, 0.000000000000000000, 0.000000000000000000 ) ) ;
#7430=ORIENTED_EDGE ( 'NONE', *, *, #8165, .T. ) ;
#7431=DIRECTION ( 'NONE',  ( -1.000000000000000000, -0.000000000000000000, 0.000000000000000000 ) ) ;
#7432=EDGE_CURVE ( 'NONE', #783, #10259, #12332, .T. ) ;
#7436=EDGE_CURVE ( 'NONE', #14422, #4009, #18799, .T. ) ;
#7437=DIRECTION ( 'NONE',  ( 0.000000000000000000, 0.6427876096865405842, -0.7660444431189771253 ) ) ;
#7438=ORIENTED_EDGE ( 'NONE', *, *, #4588, .F. ) ;
#7440=ORIENTED_EDGE ( 'NONE', *, *, #17361, .F. ) ;
#7443=EDGE_LOOP ( 'NONE', ( #20837, #20609, #11786, #3346 ) ) ;
#7445=DIRECTION ( 'NONE',  ( -1.000000000000000000, -0.000000000000000000, -0.000000000000000000 ) ) ;
#7447=DIRECTION ( 'NONE',  ( 1.000000000000000000, -0.000000000000000000, -0.000000000000000000 ) ) ;
#7449=DIRECTION ( 'NONE',  ( 0.000000000000000000, 0.8290375725550390706, 0.5591929034707506796 ) ) ;
#7450=CIRCLE ( 'NONE', #18053, 44.99999999999998579 ) ;
#7451=CARTESIAN_POINT ( 'NONE',  ( 10.00000000000000000, 12.90135963484081216, 87.04915231966650424 ) ) ;
#7452=DIRECTION ( 'NONE',  ( 0.000000000000000000, -0.2079116908177467415, -0.9781476007338083534 ) ) ;
#7453=ADVANCED_FACE ( 'NONE', ( #7615 ), #7940, .F. ) ;
#7457=CARTESIAN_POINT ( 'NONE',  ( 10.00000000000000000, -57.47876254627184522, 62.70072803846370135 ) ) ;
#7458=ORIENTED_EDGE ( 'NONE', *, *, #6546, .F. ) ;
#7461=EDGE_CURVE ( 'NONE', #1066, #7352, #19136, .T. ) ;
#7464=EDGE_LOOP ( 'NONE', ( #999, #17377, #2030, #8451 ) ) ;
#7468=CARTESIAN_POINT ( 'NONE',  ( 10.00000000000000000, 84.12297548659721258, -12.59025161327029529 ) ) ;
#7469=DIRECTION ( 'NONE',  ( -1.000000000000000000, 0.000000000000000000, 0.000000000000000000 ) ) ;
#7470=ORIENTED_EDGE ( 'NONE', *, *, #17724, .F. ) ;
#7471=EDGE_CURVE ( 'NONE', #1435, #3525, #2962, .T. ) ;
#7472=FACE_OUTER_BOUND ( 'NONE', #3649, .T. ) ;
#7474=DIRECTION ( 'NONE',  ( 1.000000000000000000, 0.000000000000000000, 0.000000000000000000 ) ) ;
#7476=CARTESIAN_POINT ( 'NONE',  ( 10.00000000000000000, 51.18896083639367589, -71.57995730992126937 ) ) ;
#7478=VECTOR ( 'NONE', #2074, 1000.000000000000000 ) ;
#7480=ORIENTED_EDGE ( 'NONE', *, *, #3565, .T. ) ;
#7481=EDGE_CURVE ( 'NONE', #8355, #1096, #10319, .T. ) ;
#7482=CARTESIAN_POINT ( 'NONE',  ( 10.00000000000000000, 51.10509369859433804, 77.10190917907216601 ) ) ;
#7483=DIRECTION ( 'NONE',  ( 1.000000000000000000, 0.000000000000000000, 0.000000000000000000 ) ) ;
#7484=DIRECTION ( 'NONE',  ( -1.000000000000000000, -0.000000000000000000, 0.000000000000000000 ) ) ;
#7486=EDGE_LOOP ( 'NONE', ( #3623, #5748, #20445, #4635 ) ) ;
#7488=ORIENTED_EDGE ( 'NONE', *, *, #1771, .F. ) ;
#7492=ORIENTED_EDGE ( 'NONE', *, *, #7988, .F. ) ;
#7493=DIRECTION ( 'NONE',  ( -1.000000000000000000, -0.000000000000000000, 0.000000000000000000 ) ) ;
#7495=CARTESIAN_POINT ( 'NONE',  ( 10.00000000000000000, -78.01214607583727911, -33.90124636420193838 ) ) ;
#7500=CIRCLE ( 'NONE', #10314, 44.99999999999999289 ) ;
#7501=LINE ( 'NONE', #20868, #16325 ) ;
#7502=DIRECTION ( 'NONE',  ( -1.000000000000000000, 0.000000000000000000, 0.000000000000000000 ) ) ;
#7503=DIRECTION ( 'NONE',  ( 0.000000000000000000, 0.000000000000000000, -1.000000000000000000 ) ) ;
#7505=LINE ( 'NONE', #17781, #9783 ) ;
#7506=CARTESIAN_POINT ( 'NONE',  ( 0.000000000000000000, 19.83954325428658194, 82.71385593638699163 ) ) ;
#7507=FACE_OUTER_BOUND ( 'NONE', #10213, .T. ) ;
#7509=VECTOR ( 'NONE', #4868, 1000.000000000000000 ) ;
#7512=AXIS2_PLACEMENT_3D ( 'NONE', #6973, #13702, #20451 ) ;
#7513=VERTEX_POINT ( 'NONE', #8269 ) ;
#7514=AXIS2_PLACEMENT_3D ( 'NONE', #7223, #15391, #12504 ) ;
#7515=EDGE_LOOP ( 'NONE', ( #14154, #561, #3415, #12028 ) ) ;
#7517=VERTEX_POINT ( 'NONE', #1750 ) ;
#7518=DIRECTION ( 'NONE',  ( 0.000000000000000000, 0.000000000000000000, 1.000000000000000000 ) ) ;
#7519=CARTESIAN_POINT ( 'NONE',  ( 10.00000000000000000, -92.22057093985034726, 7.197311757040196767 ) ) ;
#7520=CIRCLE ( 'NONE', #6485, 92.50099999999999056 ) ;
#7521=DIRECTION ( 'NONE',  ( 1.000000000000000000, 0.000000000000000000, 0.000000000000000000 ) ) ;
#7523=ADVANCED_FACE ( 'NONE', ( #14795 ), #5065, .F. ) ;
#7524=DIRECTION ( 'NONE',  ( 0.000000000000000000, -0.2756373558170062132, 0.9612616959383166737 ) ) ;
#7525=DIRECTION ( 'NONE',  ( -1.000000000000000000, 0.000000000000000000, 0.000000000000000000 ) ) ;
#7526=DIRECTION ( 'NONE',  ( 0.000000000000000000, 0.000000000000000000, 1.000000000000000000 ) ) ;
#7527=DIRECTION ( 'NONE',  ( -1.000000000000000000, -0.000000000000000000, -0.000000000000000000 ) ) ;
#7529=EDGE_CURVE ( 'NONE', #11066, #21052, #7157, .T. ) ;
#7532=LINE ( 'NONE', #21134, #11599 ) ;
#7533=CARTESIAN_POINT ( 'NONE',  ( 10.00000000000000000, -57.47876254627099257, -62.70072803846446163 ) ) ;
#7534=CIRCLE ( 'NONE', #17783, 88.00000000000000000 ) ;
#7535=ORIENTED_EDGE ( 'NONE', *, *, #2190, .F. ) ;
#7536=DIRECTION ( 'NONE',  ( 0.000000000000000000, 0.8290375725550428454, -0.5591929034707450175 ) ) ;
#7539=AXIS2_PLACEMENT_3D ( 'NONE', #21363, #19812, #2906 ) ;
#7540=CARTESIAN_POINT ( 'NONE',  ( 0.000000000000000000, 69.74988376404020585, 53.65588238863360715 ) ) ;
#7542=VERTEX_POINT ( 'NONE', #16662 ) ;
#7544=CIRCLE ( 'NONE', #11425, 44.99999999999999289 ) ;
#7545=FACE_OUTER_BOUND ( 'NONE', #19541, .T. ) ;
#7546=CARTESIAN_POINT ( 'NONE',  ( 10.00000000000000000, -87.44637528609653998, -9.855528870799524555 ) ) ;
#7547=DIRECTION ( 'NONE',  ( 1.000000000000000000, -0.000000000000000000, -0.000000000000000000 ) ) ;
#7548=EDGE_CURVE ( 'NONE', #10938, #8963, #8213, .T. ) ;
#7550=FACE_OUTER_BOUND ( 'NONE', #17437, .T. ) ;
#7551=CARTESIAN_POINT ( 'NONE',  ( 10.00000000000000000, 74.39348546125125949, -54.97312363261338675 ) ) ;
#7553=DIRECTION ( 'NONE',  ( 0.000000000000000000, 0.000000000000000000, 1.000000000000000000 ) ) ;
#7554=CARTESIAN_POINT ( 'NONE',  ( 10.00000000000000000, -72.53479564998751528, -44.42851404693431761 ) ) ;
#7555=AXIS2_PLACEMENT_3D ( 'NONE', #4243, #804, #21035 ) ;
#7557=CARTESIAN_POINT ( 'NONE',  ( 10.00000000000000000, 0.000000000000000000, 0.000000000000000000 ) ) ;
#7559=VERTEX_POINT ( 'NONE', #13121 ) ;
#7562=ADVANCED_FACE ( 'NONE', ( #15002 ), #9803, .F. ) ;
#7563=VERTEX_POINT ( 'NONE', #6739 ) ;
#7564=CARTESIAN_POINT ( 'NONE',  ( 5.000000000000002665, -87.58454185039444440, 8.540961822681374827 ) ) ;
#7565=EDGE_LOOP ( 'NONE', ( #20513, #21567, #18849, #3474 ) ) ;
#7567=CIRCLE ( 'NONE', #20293, 88.00000000000000000 ) ;
#7568=VERTEX_POINT ( 'NONE', #1427 ) ;
#7570=CIRCLE ( 'NONE', #14981, 44.99999999999999289 ) ;
#7571=ORIENTED_EDGE ( 'NONE', *, *, #2167, .F. ) ;
#7573=AXIS2_PLACEMENT_3D ( 'NONE', #5549, #467, #18716 ) ;
#7574=LINE ( 'NONE', #19176, #15455 ) ;
#7578=DIRECTION ( 'NONE',  ( -1.000000000000000000, -0.000000000000000000, -0.000000000000000000 ) ) ;
#7581=CARTESIAN_POINT ( 'NONE',  ( 0.000000000000000000, -78.04699792498179534, 49.64978465107262906 ) ) ;
#7583=DIRECTION ( 'NONE',  ( 1.000000000000000000, 0.000000000000000000, 0.000000000000000000 ) ) ;
#7584=CIRCLE ( 'NONE', #14270, 44.99999999999999289 ) ;
#7587=ORIENTED_EDGE ( 'NONE', *, *, #19188, .F. ) ;
#7588=DIRECTION ( 'NONE',  ( 0.000000000000000000, 0.000000000000000000, 1.000000000000000000 ) ) ;
#7589=CIRCLE ( 'NONE', #19934, 92.50100000000000477 ) ;
#7590=CARTESIAN_POINT ( 'NONE',  ( 10.00000000000000000, 21.65267340503250537, 89.93106657554442052 ) ) ;
#7592=CIRCLE ( 'NONE', #2996, 44.99999999999998579 ) ;
#7594=EDGE_CURVE ( 'NONE', #21723, #14855, #6808, .T. ) ;
#7598=CARTESIAN_POINT ( 'NONE',  ( 0.000000000000000000, 0.000000000000000000, 0.000000000000000000 ) ) ;
#7599=EDGE_CURVE ( 'NONE', #15453, #20112, #13856, .T. ) ;
#7600=CIRCLE ( 'NONE', #885, 45.00000000000000000 ) ;
#7601=EDGE_LOOP ( 'NONE', ( #9426, #8599, #10144, #2373 ) ) ;
#7602=EDGE_LOOP ( 'NONE', ( #6748, #16834, #16013, #10563 ) ) ;
#7603=VERTEX_POINT ( 'NONE', #1641 ) ;
#7606=EDGE_LOOP ( 'NONE', ( #1804, #11449, #4530, #19163 ) ) ;
#7609=DIRECTION ( 'NONE',  ( -1.000000000000000000, -0.000000000000000000, -0.000000000000000000 ) ) ;
#7613=EDGE_CURVE ( 'NONE', #1120, #19953, #518, .T. ) ;
#7615=FACE_OUTER_BOUND ( 'NONE', #13261, .T. ) ;
#7616=CYLINDRICAL_SURFACE ( 'NONE', #15441, 44.99999999999998579 ) ;
#7617=DIRECTION ( 'NONE',  ( -1.000000000000000000, 0.000000000000000000, 0.000000000000000000 ) ) ;
#7618=FACE_OUTER_BOUND ( 'NONE', #17906, .T. ) ;
#7619=ORIENTED_EDGE ( 'NONE', *, *, #12209, .T. ) ;
#7620=CIRCLE ( 'NONE', #20331, 45.00000000000000000 ) ;
#7622=AXIS2_PLACEMENT_3D ( 'NONE', #20786, #15916, #7518 ) ;
#7623=ADVANCED_FACE ( 'NONE', ( #412 ), #20741, .F. ) ;
#7626=AXIS2_PLACEMENT_3D ( 'NONE', #8961, #466, #14257 ) ;
#7627=ORIENTED_EDGE ( 'NONE', *, *, #17178, .T. ) ;
#7632=CARTESIAN_POINT ( 'NONE',  ( 10.00000000000000000, -81.32027326007839463, -44.08455690949136851 ) ) ;
#7633=CARTESIAN_POINT ( 'NONE',  ( 10.00000000000000000, 35.18804927320529430, 80.65854690202691302 ) ) ;
#7634=DIRECTION ( 'NONE',  ( 1.000000000000000000, 0.000000000000000000, 0.000000000000000000 ) ) ;
#7635=DIRECTION ( 'NONE',  ( 1.000000000000000000, 0.000000000000000000, 0.000000000000000000 ) ) ;
#7637=CIRCLE ( 'NONE', #13975, 88.00000000000000000 ) ;
#7638=CARTESIAN_POINT ( 'NONE',  ( 0.000000000000000000, 30.71797041605808687, 82.46457599186561538 ) ) ;
#7639=AXIS2_PLACEMENT_3D ( 'NONE', #14255, #14149, #17482 ) ;
#7641=DIRECTION ( 'NONE',  ( 1.000000000000000000, 0.000000000000000000, 0.000000000000000000 ) ) ;
#7643=ORIENTED_EDGE ( 'NONE', *, *, #13682, .F. ) ;
#7645=EDGE_CURVE ( 'NONE', #659, #1075, #5743, .T. ) ;
#7646=CARTESIAN_POINT ( 'NONE',  ( 10.00000000000000000, 0.000000000000000000, 0.000000000000000000 ) ) ;
#7647=CIRCLE ( 'NONE', #20003, 45.00000000000000000 ) ;
#7648=CYLINDRICAL_SURFACE ( 'NONE', #19770, 88.00000000000000000 ) ;
#7649=VECTOR ( 'NONE', #11434, 1000.000000000000000 ) ;
#7651=CIRCLE ( 'NONE', #3756, 92.50100000000000477 ) ;
#7653=ORIENTED_EDGE ( 'NONE', *, *, #584, .T. ) ;
#7655=CIRCLE ( 'NONE', #3787, 92.50100000000000477 ) ;
#7659=ORIENTED_EDGE ( 'NONE', *, *, #14870, .F. ) ;
#7660=CARTESIAN_POINT ( 'NONE',  ( 10.00000000000000000, -48.19312842678519360, 70.09002648625178722 ) ) ;
#7661=DIRECTION ( 'NONE',  ( 0.000000000000000000, 0.000000000000000000, 1.000000000000000000 ) ) ;
#7664=FACE_OUTER_BOUND ( 'NONE', #10851, .T. ) ;
#7665=CARTESIAN_POINT ( 'NONE',  ( -10.00000000000000000, 0.000000000000000000, 0.000000000000000000 ) ) ;
#7668=CYLINDRICAL_SURFACE ( 'NONE', #4504, 44.99999999999999289 ) ;
#7673=ORIENTED_EDGE ( 'NONE', *, *, #12665, .F. ) ;
#7674=CYLINDRICAL_SURFACE ( 'NONE', #2038, 44.99999999999998579 ) ;
#7677=DIRECTION ( 'NONE',  ( -1.000000000000000000, -0.000000000000000000, -0.000000000000000000 ) ) ;
#7678=ORIENTED_EDGE ( 'NONE', *, *, #342, .T. ) ;
#7680=VERTEX_POINT ( 'NONE', #314 ) ;
#7682=VERTEX_POINT ( 'NONE', #5497 ) ;
#7683=VECTOR ( 'NONE', #18189, 1000.000000000000000 ) ;
#7684=CARTESIAN_POINT ( 'NONE',  ( 10.00000000000000000, -21.31452625070873452, -82.34610137166143318 ) ) ;
#7685=CARTESIAN_POINT ( 'NONE',  ( 10.00000000000000000, -51.76708072107842185, -67.49339815138544907 ) ) ;
#7686=AXIS2_PLACEMENT_3D ( 'NONE', #3891, #5116, #366 ) ;
#7688=EDGE_LOOP ( 'NONE', ( #8821, #13823, #11187, #15691 ) ) ;
#7690=DIRECTION ( 'NONE',  ( -1.000000000000000000, 0.000000000000000000, 0.000000000000000000 ) ) ;
#7692=CARTESIAN_POINT ( 'NONE',  ( 0.000000000000000000, 0.000000000000000000, 0.000000000000000000 ) ) ;
#7693=AXIS2_PLACEMENT_3D ( 'NONE', #12170, #15260, #13937 ) ;
#7694=LINE ( 'NONE', #952, #5557 ) ;
#7695=ADVANCED_FACE ( 'NONE', ( #17424 ), #3613, .F. ) ;
#7696=ORIENTED_EDGE ( 'NONE', *, *, #20676, .T. ) ;
#7698=AXIS2_PLACEMENT_3D ( 'NONE', #21217, #10826, #16345 ) ;
#7699=CIRCLE ( 'NONE', #9800, 88.00000000000000000 ) ;
#7701=AXIS2_PLACEMENT_3D ( 'NONE', #1908, #8649, #15381 ) ;
#7702=VECTOR ( 'NONE', #6211, 1000.000000000000000 ) ;
#7703=CARTESIAN_POINT ( 'NONE',  ( 10.00000000000000000, -91.70173545986510533, -12.13370160540135423 ) ) ;
#7705=EDGE_CURVE ( 'NONE', #2939, #419, #3969, .T. ) ;
#7706=DIRECTION ( 'NONE',  ( -1.000000000000000000, 0.000000000000000000, 0.000000000000000000 ) ) ;
#7708=ADVANCED_FACE ( 'NONE', ( #19085 ), #3941, .F. ) ;
#7715=ORIENTED_EDGE ( 'NONE', *, *, #19827, .T. ) ;
#7718=CARTESIAN_POINT ( 'NONE',  ( 10.00000000000000000, -79.66702613806795341, 29.80527447819410369 ) ) ;
#7719=CIRCLE ( 'NONE', #8787, 44.99999999999999289 ) ;
#7722=AXIS2_PLACEMENT_3D ( 'NONE', #17112, #6962, #8718 ) ;
#7723=AXIS2_PLACEMENT_3D ( 'NONE', #9712, #17917, #13256 ) ;
#7725=DIRECTION ( 'NONE',  ( 0.000000000000000000, 0.9848077530122073542, 0.1736481776669339949 ) ) ;
#7726=EDGE_CURVE ( 'NONE', #5530, #8987, #20901, .T. ) ;
#7727=CARTESIAN_POINT ( 'NONE',  ( 0.000000000000000000, -35.18804927320473297, -80.65854690202716881 ) ) ;
#7728=DIRECTION ( 'NONE',  ( 0.000000000000000000, -0.6946583704590034714, 0.7193398003386453077 ) ) ;
#7732=CARTESIAN_POINT ( 'NONE',  ( 0.000000000000000000, 85.54350296776112828, 20.64725405482881726 ) ) ;
#7736=VERTEX_POINT ( 'NONE', #11545 ) ;
#7740=EDGE_CURVE ( 'NONE', #20538, #9177, #10680, .T. ) ;
#7743=DIRECTION ( 'NONE',  ( 0.000000000000000000, 0.000000000000000000, 1.000000000000000000 ) ) ;
#7744=ORIENTED_EDGE ( 'NONE', *, *, #3834, .T. ) ;
#7745=DIRECTION ( 'NONE',  ( -1.000000000000000000, -0.000000000000000000, 0.000000000000000000 ) ) ;
#7749=ADVANCED_FACE ( 'NONE', ( #13185 ), #9878, .F. ) ;
#7752=VECTOR ( 'NONE', #14743, 1000.000000000000000 ) ;
#7753=DIRECTION ( 'NONE',  ( 1.000000000000000000, 0.000000000000000000, 0.000000000000000000 ) ) ;
#7760=ORIENTED_EDGE ( 'NONE', *, *, #2470, .T. ) ;
#7761=EDGE_CURVE ( 'NONE', #17932, #2613, #13869, .T. ) ;
#7763=DIRECTION ( 'NONE',  ( 0.000000000000000000, 0.000000000000000000, 1.000000000000000000 ) ) ;
#7764=ORIENTED_EDGE ( 'NONE', *, *, #19442, .T. ) ;
#7766=CARTESIAN_POINT ( 'NONE',  ( 10.00000000000000000, 65.64563793391829449, 54.09103124042837862 ) ) ;
#7768=AXIS2_PLACEMENT_3D ( 'NONE', #16511, #14847, #21585 ) ;
#7769=CYLINDRICAL_SURFACE ( 'NONE', #15714, 92.50100000000000477 ) ;
#7771=ORIENTED_EDGE ( 'NONE', *, *, #13279, .T. ) ;
#7773=DIRECTION ( 'NONE',  ( 0.000000000000000000, 0.000000000000000000, 1.000000000000000000 ) ) ;
#7774=ORIENTED_EDGE ( 'NONE', *, *, #4193, .T. ) ;
#7776=LINE ( 'NONE', #1134, #4396 ) ;
#7778=DIRECTION ( 'NONE',  ( -1.000000000000000000, 0.000000000000000000, -0.000000000000000000 ) ) ;
#7781=CARTESIAN_POINT ( 'NONE',  ( 10.00000000000000000, 65.64563793391829449, 54.09103124042837862 ) ) ;
#7783=DIRECTION ( 'NONE',  ( 1.000000000000000000, 0.000000000000000000, 0.000000000000000000 ) ) ;
#7784=CARTESIAN_POINT ( 'NONE',  ( 10.00000000000000000, 0.000000000000000000, 0.000000000000000000 ) ) ;
#7786=CARTESIAN_POINT ( 'NONE',  ( 10.00000000000000000, -81.32027326007897727, 44.08455690949027428 ) ) ;
#7790=CYLINDRICAL_SURFACE ( 'NONE', #4214, 44.99999999999999289 ) ;
#7791=ORIENTED_EDGE ( 'NONE', *, *, #10161, .T. ) ;
#7794=ORIENTED_EDGE ( 'NONE', *, *, #1917, .T. ) ;
#7795=VECTOR ( 'NONE', #10283, 1000.000000000000000 ) ;
#7796=CARTESIAN_POINT ( 'NONE',  ( 10.00000000000000000, 0.000000000000000000, 0.000000000000000000 ) ) ;
#7797=DIRECTION ( 'NONE',  ( 0.000000000000000000, -0.7880107536067145757, -0.6156614753256675066 ) ) ;
#7800=DIRECTION ( 'NONE',  ( 0.000000000000000000, 0.000000000000000000, 1.000000000000000000 ) ) ;
#7803=DIRECTION ( 'NONE',  ( 0.000000000000000000, 0.2079116908177598144, -0.9781476007338055778 ) ) ;
#7807=CARTESIAN_POINT ( 'NONE',  ( 10.00000000000000000, 1.224646799147353217E-14, -100.0000000000000000 ) ) ;
#7808=VERTEX_POINT ( 'NONE', #20381 ) ;
#7810=DIRECTION ( 'NONE',  ( -1.000000000000000000, -0.000000000000000000, -0.000000000000000000 ) ) ;
#7811=ORIENTED_EDGE ( 'NONE', *, *, #14057, .F. ) ;
#7813=CYLINDRICAL_SURFACE ( 'NONE', #17611, 45.00000000000000000 ) ;
#7816=EDGE_LOOP ( 'NONE', ( #20612, #5674, #6725, #355 ) ) ;
#7817=ORIENTED_EDGE ( 'NONE', *, *, #17695, .F. ) ;
#7819=ORIENTED_EDGE ( 'NONE', *, *, #5585, .F. ) ;
#7823=DIRECTION ( 'NONE',  ( 1.000000000000000000, 0.000000000000000000, 0.000000000000000000 ) ) ;
#7824=EDGE_CURVE ( 'NONE', #17747, #12605, #11039, .T. ) ;
#7825=DIRECTION ( 'NONE',  ( 0.000000000000000000, -0.3420201433256569445, -0.9396926207859126468 ) ) ;
#7827=CARTESIAN_POINT ( 'NONE',  ( 0.000000000000000000, -69.25892805976475586, -49.38005998797915908 ) ) ;
#7829=LINE ( 'NONE', #17897, #21776 ) ;
#7830=FACE_OUTER_BOUND ( 'NONE', #6585, .T. ) ;
#7831=ADVANCED_FACE ( 'NONE', ( #6470 ), #10211, .F. ) ;
#7835=EDGE_LOOP ( 'NONE', ( #593, #21210, #20781, #9135 ) ) ;
#7836=EDGE_CURVE ( 'NONE', #4275, #20304, #13502, .T. ) ;
#7838=ORIENTED_EDGE ( 'NONE', *, *, #13457, .T. ) ;
#7839=ORIENTED_EDGE ( 'NONE', *, *, #17, .T. ) ;
#7840=EDGE_CURVE ( 'NONE', #5185, #10039, #19866, .T. ) ;
#7841=CYLINDRICAL_SURFACE ( 'NONE', #18658, 92.50100000000000477 ) ;
#7842=VECTOR ( 'NONE', #21113, 1000.000000000000000 ) ;
#7843=ORIENTED_EDGE ( 'NONE', *, *, #15969, .F. ) ;
#7844=LINE ( 'NONE', #3905, #4303 ) ;
#7846=AXIS2_PLACEMENT_3D ( 'NONE', #18979, #20526, #18870 ) ;
#7847=DIRECTION ( 'NONE',  ( 1.000000000000000000, 0.000000000000000000, 0.000000000000000000 ) ) ;
#7848=CARTESIAN_POINT ( 'NONE',  ( 10.00000000000000000, 0.000000000000000000, 0.000000000000000000 ) ) ;
#7849=CYLINDRICAL_SURFACE ( 'NONE', #9753, 88.00000000000000000 ) ;
#7850=EDGE_CURVE ( 'NONE', #11042, #15057, #14926, .T. ) ;
#7851=CARTESIAN_POINT ( 'NONE',  ( 10.00000000000000000, -92.49798535263882115, -0.7467976319030308341 ) ) ;
#7853=CARTESIAN_POINT ( 'NONE',  ( 10.00000000000000000, -31.15801000616779248, -79.14775961996421927 ) ) ;
#7854=EDGE_CURVE ( 'NONE', #12163, #6716, #18614, .T. ) ;
#7857=CARTESIAN_POINT ( 'NONE',  ( 10.00000000000000000, -56.35896156214896280, -73.34918167666369015 ) ) ;
#7858=AXIS2_PLACEMENT_3D ( 'NONE', #8183, #13469, #1547 ) ;
#7862=DIRECTION ( 'NONE',  ( -1.000000000000000000, -0.000000000000000000, 0.000000000000000000 ) ) ;
#7863=EDGE_CURVE ( 'NONE', #19313, #9664, #156, .T. ) ;
#7864=CARTESIAN_POINT ( 'NONE',  ( 0.000000000000000000, 65.64563793391829449, 54.09103124042837862 ) ) ;
#7865=AXIS2_PLACEMENT_3D ( 'NONE', #10619, #17367, #2222 ) ;
#7866=ORIENTED_EDGE ( 'NONE', *, *, #6361, .F. ) ;
#7867=CARTESIAN_POINT ( 'NONE',  ( 10.00000000000000000, 36.39558101400137957, 80.12091913260394449 ) ) ;
#7868=ORIENTED_EDGE ( 'NONE', *, *, #6069, .F. ) ;
#7869=EDGE_CURVE ( 'NONE', #173, #18557, #8972, .T. ) ;
#7873=AXIS2_PLACEMENT_3D ( 'NONE', #14672, #12461, #2629 ) ;
#7874=VERTEX_POINT ( 'NONE', #4007 ) ;
#7875=ORIENTED_EDGE ( 'NONE', *, *, #3004, .T. ) ;
#7876=EDGE_CURVE ( 'NONE', #17373, #17077, #3981, .T. ) ;
#7879=EDGE_CURVE ( 'NONE', #20207, #8011, #10333, .T. ) ;
#7883=LINE ( 'NONE', #8206, #10441 ) ;
#7884=CARTESIAN_POINT ( 'NONE',  ( 0.000000000000000000, -62.44821182181136976, 68.23969402963483333 ) ) ;
#7885=CYLINDRICAL_SURFACE ( 'NONE', #497, 92.50100000000000477 ) ;
#7889=ORIENTED_EDGE ( 'NONE', *, *, #11162, .F. ) ;
#7893=LINE ( 'NONE', #8214, #16863 ) ;
#7897=AXIS2_PLACEMENT_3D ( 'NONE', #6731, #13664, #18433 ) ;
#7903=CARTESIAN_POINT ( 'NONE',  ( 0.000000000000000000, -37.96946988134122591, -76.11510229470897571 ) ) ;
#7905=EDGE_CURVE ( 'NONE', #20271, #1347, #18106, .T. ) ;
#7906=AXIS2_PLACEMENT_3D ( 'NONE', #12434, #12547, #14317 ) ;
#7908=DIRECTION ( 'NONE',  ( 0.000000000000000000, 0.000000000000000000, 1.000000000000000000 ) ) ;
#7909=DIRECTION ( 'NONE',  ( 1.000000000000000000, -0.000000000000000000, -0.000000000000000000 ) ) ;
#7910=CARTESIAN_POINT ( 'NONE',  ( 10.00000000000000000, 0.000000000000000000, 0.000000000000000000 ) ) ;
#7911=CARTESIAN_POINT ( 'NONE',  ( 10.00000000000000000, 92.49798535263882115, 0.7467976319023850174 ) ) ;
#7913=AXIS2_PLACEMENT_3D ( 'NONE', #2827, #11221, #21502 ) ;
#7914=ORIENTED_EDGE ( 'NONE', *, *, #11893, .T. ) ;
#7915=AXIS2_PLACEMENT_3D ( 'NONE', #3475, #8341, #15180 ) ;
#7916=CARTESIAN_POINT ( 'NONE',  ( 10.00000000000000000, -90.63195040374174027, -18.50093422002511900 ) ) ;
#7917=CARTESIAN_POINT ( 'NONE',  ( 10.00000000000000000, 21.31452625071037943, -82.34610137166097843 ) ) ;
#7918=ORIENTED_EDGE ( 'NONE', *, *, #4971, .T. ) ;
#7919=DIRECTION ( 'NONE',  ( 0.000000000000000000, 0.3420201433256694901, -0.9396926207859080948 ) ) ;
#7920=ORIENTED_EDGE ( 'NONE', *, *, #12107, .F. ) ;
#7921=AXIS2_PLACEMENT_3D ( 'NONE', #14646, #21393, #1286 ) ;
#7922=DIRECTION ( 'NONE',  ( -1.000000000000000000, 0.000000000000000000, 0.000000000000000000 ) ) ;
#7923=DIRECTION ( 'NONE',  ( 0.000000000000000000, -0.7880107536067275653, 0.6156614753256510753 ) ) ;
#7927=ORIENTED_EDGE ( 'NONE', *, *, #7836, .F. ) ;
#7928=EDGE_CURVE ( 'NONE', #20507, #454, #9607, .T. ) ;
#7929=ORIENTED_EDGE ( 'NONE', *, *, #15303, .T. ) ;
#7930=CARTESIAN_POINT ( 'NONE',  ( 10.00000000000000000, 78.01214607583800387, -33.90124636420030413 ) ) ;
#7931=AXIS2_PLACEMENT_3D ( 'NONE', #7660, #18155, #3011 ) ;
#7932=VERTEX_POINT ( 'NONE', #17173 ) ;
#7936=DIRECTION ( 'NONE',  ( 0.000000000000000000, 0.000000000000000000, 1.000000000000000000 ) ) ;
#7937=EDGE_CURVE ( 'NONE', #19662, #16982, #16690, .T. ) ;
#7940=CYLINDRICAL_SURFACE ( 'NONE', #9250, 92.50100000000000477 ) ;
#7942=LINE ( 'NONE', #18009, #11552 ) ;
#7944=AXIS2_PLACEMENT_3D ( 'NONE', #18806, #8318, #16704 ) ;
#7947=DIRECTION ( 'NONE',  ( -1.000000000000000000, -0.000000000000000000, -0.000000000000000000 ) ) ;
#7948=EDGE_LOOP ( 'NONE', ( #4008, #18047, #16319, #5513 ) ) ;
#7949=ORIENTED_EDGE ( 'NONE', *, *, #17215, .T. ) ;
#7952=EDGE_CURVE ( 'NONE', #5893, #4745, #12396, .T. ) ;
#7953=AXIS2_PLACEMENT_3D ( 'NONE', #1500, #11563, #19955 ) ;
#7956=ORIENTED_EDGE ( 'NONE', *, *, #3615, .T. ) ;
#7957=CARTESIAN_POINT ( 'NONE',  ( 10.00000000000000000, 0.000000000000000000, 0.000000000000000000 ) ) ;
#7958=ORIENTED_EDGE ( 'NONE', *, *, #6756, .T. ) ;
#7959=CARTESIAN_POINT ( 'NONE',  ( 10.00000000000000000, -8.925965667929485647, 92.06933331948778232 ) ) ;
#7960=DIRECTION ( 'NONE',  ( 0.000000000000000000, 0.4694715627858916940, -0.8829475928589264333 ) ) ;
#7961=DIRECTION ( 'NONE',  ( -1.000000000000000000, 0.000000000000000000, 0.000000000000000000 ) ) ;
#7962=DIRECTION ( 'NONE',  ( 1.000000000000000000, 0.000000000000000000, 0.000000000000000000 ) ) ;
#7963=DIRECTION ( 'NONE',  ( 0.000000000000000000, 0.000000000000000000, 1.000000000000000000 ) ) ;
#7964=AXIS2_PLACEMENT_3D ( 'NONE', #11643, #15163, #6458 ) ;
#7965=CARTESIAN_POINT ( 'NONE',  ( 5.000000000000002665, 87.92084725184953697, -3.731570516142035387 ) ) ;
#7966=ADVANCED_FACE ( 'NONE', ( #15839 ), #19046, .F. ) ;
#7967=DIRECTION ( 'NONE',  ( 1.000000000000000000, 0.000000000000000000, 0.000000000000000000 ) ) ;
#7971=AXIS2_PLACEMENT_3D ( 'NONE', #917, #21152, #19152 ) ;
#7975=ORIENTED_EDGE ( 'NONE', *, *, #11192, .T. ) ;
#7976=DIRECTION ( 'NONE',  ( 0.000000000000000000, -0.6427876096865458022, 0.7660444431189726844 ) ) ;
#7981=EDGE_CURVE ( 'NONE', #12259, #2865, #15269, .T. ) ;
#7982=FACE_OUTER_BOUND ( 'NONE', #426, .T. ) ;
#7983=ORIENTED_EDGE ( 'NONE', *, *, #17821, .T. ) ;
#7984=ORIENTED_EDGE ( 'NONE', *, *, #19959, .T. ) ;
#7986=AXIS2_PLACEMENT_3D ( 'NONE', #3993, #9504, #7526 ) ;
#7987=DIRECTION ( 'NONE',  ( -1.000000000000000000, 0.000000000000000000, 0.000000000000000000 ) ) ;
#7988=EDGE_CURVE ( 'NONE', #14447, #2288, #12101, .T. ) ;
#7989=ORIENTED_EDGE ( 'NONE', *, *, #16793, .T. ) ;
#7990=CIRCLE ( 'NONE', #4105, 44.99999999999999289 ) ;
#7991=ORIENTED_EDGE ( 'NONE', *, *, #17997, .F. ) ;
#7993=VECTOR ( 'NONE', #18920, 1000.000000000000000 ) ;
#7994=CARTESIAN_POINT ( 'NONE',  ( 10.00000000000000000, 0.000000000000000000, 0.000000000000000000 ) ) ;
#7996=LINE ( 'NONE', #21471, #18294 ) ;
#7997=DIRECTION ( 'NONE',  ( 1.000000000000000000, 0.000000000000000000, 0.000000000000000000 ) ) ;
#8000=CARTESIAN_POINT ( 'NONE',  ( -10.00000000000000000, 0.000000000000000000, 0.000000000000000000 ) ) ;
#8001=EDGE_CURVE ( 'NONE', #14362, #9395, #472, .T. ) ;
#8003=VERTEX_POINT ( 'NONE', #2029 ) ;
#8004=EDGE_CURVE ( 'NONE', #21544, #3268, #8575, .T. ) ;
#8005=ORIENTED_EDGE ( 'NONE', *, *, #5585, .T. ) ;
#8008=CARTESIAN_POINT ( 'NONE',  ( 10.00000000000000000, 31.15801000616834315, 79.14775961996400611 ) ) ;
#8009=DIRECTION ( 'NONE',  ( 1.000000000000000000, 0.000000000000000000, 0.000000000000000000 ) ) ;
#8010=DIRECTION ( 'NONE',  ( 1.000000000000000000, 0.000000000000000000, 0.000000000000000000 ) ) ;
#8011=VERTEX_POINT ( 'NONE', #12076 ) ;
#8013=VERTEX_POINT ( 'NONE', #5350 ) ;
#8016=ORIENTED_EDGE ( 'NONE', *, *, #1917, .F. ) ;
#8019=VERTEX_POINT ( 'NONE', #12617 ) ;
#8020=VECTOR ( 'NONE', #686, 1000.000000000000000 ) ;
#8023=AXIS2_PLACEMENT_3D ( 'NONE', #5295, #320, #10682 ) ;
#8026=AXIS2_PLACEMENT_3D ( 'NONE', #1313, #16229, #19534 ) ;
#8027=DIRECTION ( 'NONE',  ( 1.000000000000000000, 0.000000000000000000, 0.000000000000000000 ) ) ;
#8028=LINE ( 'NONE', #10106, #18739 ) ;
#8036=LINE ( 'NONE', #5039, #5541 ) ;
#8037=ORIENTED_EDGE ( 'NONE', *, *, #5938, .F. ) ;
#8038=AXIS2_PLACEMENT_3D ( 'NONE', #4525, #2963, #11355 ) ;
#8039=CARTESIAN_POINT ( 'NONE',  ( 0.000000000000000000, 0.000000000000000000, -88.00000000000000000 ) ) ;
#8042=DIRECTION ( 'NONE',  ( -1.000000000000000000, 0.000000000000000000, 0.000000000000000000 ) ) ;
#8047=VERTEX_POINT ( 'NONE', #1026 ) ;
#8048=CYLINDRICAL_SURFACE ( 'NONE', #3405, 44.99999999999999289 ) ;
#8049=ORIENTED_EDGE ( 'NONE', *, *, #13154, .F. ) ;
#8052=LINE ( 'NONE', #9796, #8925 ) ;
#8053=CARTESIAN_POINT ( 'NONE',  ( 5.000000000000002665, -6.797690662954623875, -87.73705831432221203 ) ) ;
#8055=AXIS2_PLACEMENT_3D ( 'NONE', #6569, #3338, #18051 ) ;
#8060=AXIS2_PLACEMENT_3D ( 'NONE', #12742, #10463, #2691 ) ;
#8061=DIRECTION ( 'NONE',  ( -1.000000000000000000, 0.000000000000000000, 0.000000000000000000 ) ) ;
#8062=DIRECTION ( 'NONE',  ( -1.000000000000000000, -0.000000000000000000, -0.000000000000000000 ) ) ;
#8063=CARTESIAN_POINT ( 'NONE',  ( 10.00000000000000000, -19.83954325428602061, -82.71385593638713374 ) ) ;
#8065=EDGE_LOOP ( 'NONE', ( #11725, #2678, #877, #13458 ) ) ;
#8067=ORIENTED_EDGE ( 'NONE', *, *, #15120, .T. ) ;
#8068=VERTEX_POINT ( 'NONE', #4450 ) ;
#8069=VECTOR ( 'NONE', #17228, 1000.000000000000000 ) ;
#8074=DIRECTION ( 'NONE',  ( -1.000000000000000000, -0.000000000000000000, -0.000000000000000000 ) ) ;
#8075=LINE ( 'NONE', #5084, #4333 ) ;
#8076=CARTESIAN_POINT ( 'NONE',  ( 10.00000000000000000, -46.89573839703331259, 79.73220629831473616 ) ) ;
#8078=CARTESIAN_POINT ( 'NONE',  ( 10.00000000000000000, 12.90135963484197212, -87.04915231966633371 ) ) ;
#8080=CARTESIAN_POINT ( 'NONE',  ( 5.000000000000002665, -85.22372865846305956, 21.92979875759598585 ) ) ;
#8081=DIRECTION ( 'NONE',  ( 0.000000000000000000, -0.9510565162951565288, 0.3090169943749382364 ) ) ;
#8082=EDGE_CURVE ( 'NONE', #2668, #8737, #12462, .T. ) ;
#8083=AXIS2_PLACEMENT_3D ( 'NONE', #19639, #1181, #7923 ) ;
#8087=AXIS2_PLACEMENT_3D ( 'NONE', #12368, #2636, #9369 ) ;
#8088=LINE ( 'NONE', #18582, #12902 ) ;
#8090=EDGE_CURVE ( 'NONE', #8367, #14246, #14594, .T. ) ;
#8093=ORIENTED_EDGE ( 'NONE', *, *, #10492, .T. ) ;
#8096=VERTEX_POINT ( 'NONE', #2896 ) ;
#8102=AXIS2_PLACEMENT_3D ( 'NONE', #10004, #16747, #1834 ) ;
#8103=CIRCLE ( 'NONE', #17282, 88.00000000000000000 ) ;
#8104=CARTESIAN_POINT ( 'NONE',  ( 0.000000000000000000, -75.27139873020848881, -53.76477968147889896 ) ) ;
#8106=CARTESIAN_POINT ( 'NONE',  ( 10.00000000000000000, -29.29369617358527833, 87.74003855418389719 ) ) ;
#8107=CARTESIAN_POINT ( 'NONE',  ( 5.000000000000000000, 72.58367602204255320, -49.75550195834793499 ) ) ;
#8108=FACE_OUTER_BOUND ( 'NONE', #635, .T. ) ;
#8111=DIRECTION ( 'NONE',  ( 0.000000000000000000, 0.000000000000000000, 1.000000000000000000 ) ) ;
#8112=EDGE_CURVE ( 'NONE', #13772, #1807, #10964, .T. ) ;
#8113=ADVANCED_FACE ( 'NONE', ( #17711 ), #9292, .F. ) ;
#8114=EDGE_CURVE ( 'NONE', #1263, #17806, #9279, .T. ) ;
#8115=EDGE_LOOP ( 'NONE', ( #2327, #17201, #21285, #21104 ) ) ;
#8116=ADVANCED_FACE ( 'NONE', ( #906 ), #19693, .F. ) ;
#8117=ORIENTED_EDGE ( 'NONE', *, *, #14688, .T. ) ;
#8118=CIRCLE ( 'NONE', #14413, 44.99999999999999289 ) ;
#8119=DIRECTION ( 'NONE',  ( -1.000000000000000000, 0.000000000000000000, 0.000000000000000000 ) ) ;
#8121=VERTEX_POINT ( 'NONE', #21464 ) ;
#8122=DIRECTION ( 'NONE',  ( -1.000000000000000000, 0.000000000000000000, -0.000000000000000000 ) ) ;
#8123=ORIENTED_EDGE ( 'NONE', *, *, #17967, .F. ) ;
#8127=ORIENTED_EDGE ( 'NONE', *, *, #5067, .F. ) ;
#8132=EDGE_CURVE ( 'NONE', #5399, #5100, #6014, .T. ) ;
#8133=CARTESIAN_POINT ( 'NONE',  ( 10.00000000000000000, -15.51843147776405729, 83.63233659819645993 ) ) ;
#8134=DIRECTION ( 'NONE',  ( 0.000000000000000000, 0.000000000000000000, 1.000000000000000000 ) ) ;
#8135=CARTESIAN_POINT ( 'NONE',  ( 10.00000000000000000, 0.000000000000000000, 0.000000000000000000 ) ) ;
#8136=AXIS2_PLACEMENT_3D ( 'NONE', #7766, #12612, #1124 ) ;
#8138=DIRECTION ( 'NONE',  ( 0.000000000000000000, -0.2756373558170062132, 0.9612616959383167847 ) ) ;
#8139=CARTESIAN_POINT ( 'NONE',  ( 10.00000000000000000, -3.728035544476815399, 84.97818067823770605 ) ) ;
#8140=UNCERTAINTY_MEASURE_WITH_UNIT (LENGTH_MEASURE( 1.000000000000000082E-05 ), #15750, 'distance_accuracy_value', 'NONE');
#8141=ORIENTED_EDGE ( 'NONE', *, *, #14682, .F. ) ;
#8142=DIRECTION ( 'NONE',  ( 0.000000000000000000, -0.9848077530122096857, 0.1736481776669207000 ) ) ;
#8143=EDGE_CURVE ( 'NONE', #17311, #4876, #5772, .T. ) ;
#8144=CYLINDRICAL_SURFACE ( 'NONE', #20648, 44.99999999999999289 ) ;
#8145=ORIENTED_EDGE ( 'NONE', *, *, #3265, .T. ) ;
#8146=DIRECTION ( 'NONE',  ( 1.000000000000000000, 0.000000000000000000, 0.000000000000000000 ) ) ;
#8149=AXIS2_PLACEMENT_3D ( 'NONE', #6985, #238, #13821 ) ;
#8150=CARTESIAN_POINT ( 'NONE',  ( 0.000000000000000000, -87.96697768756403946, 2.410567674970269358 ) ) ;
#8151=EDGE_LOOP ( 'NONE', ( #2324, #15446, #825, #21280 ) ) ;
#8153=EDGE_CURVE ( 'NONE', #6675, #8963, #2588, .T. ) ;
#8155=VERTEX_POINT ( 'NONE', #7540 ) ;
#8158=VERTEX_POINT ( 'NONE', #14272 ) ;
#8159=DIRECTION ( 'NONE',  ( 1.000000000000000000, -0.000000000000000000, 0.000000000000000000 ) ) ;
#8160=LINE ( 'NONE', #11463, #11477 ) ;
#8163=EDGE_CURVE ( 'NONE', #4539, #10355, #11185, .T. ) ;
#8164=( NAMED_UNIT ( * ) SI_UNIT ( $, .STERADIAN. ) SOLID_ANGLE_UNIT ( ) );
#8165=EDGE_CURVE ( 'NONE', #3581, #9256, #14232, .T. ) ;
#8168=CARTESIAN_POINT ( 'NONE',  ( 0.000000000000000000, 23.62010150527335028, -84.77081340225880979 ) ) ;
#8172=VERTEX_POINT ( 'NONE', #15098 ) ;
#8176=VECTOR ( 'NONE', #5473, 1000.000000000000000 ) ;
#8178=ORIENTED_EDGE ( 'NONE', *, *, #6537, .F. ) ;
#8179=CYLINDRICAL_SURFACE ( 'NONE', #16180, 44.99999999999999289 ) ;
#8180=VERTEX_POINT ( 'NONE', #6829 ) ;
#8181=DIRECTION ( 'NONE',  ( -1.000000000000000000, -0.000000000000000000, -0.000000000000000000 ) ) ;
#8183=CARTESIAN_POINT ( 'NONE',  ( 10.00000000000000000, 0.000000000000000000, 0.000000000000000000 ) ) ;
#8184=CYLINDRICAL_SURFACE ( 'NONE', #7723, 44.99999999999999289 ) ;
#8186=DIRECTION ( 'NONE',  ( 0.000000000000000000, -0.7880107536067145757, -0.6156614753256675066 ) ) ;
#8187=DIRECTION ( 'NONE',  ( 0.000000000000000000, 0.000000000000000000, 1.000000000000000000 ) ) ;
#8188=ORIENTED_EDGE ( 'NONE', *, *, #20822, .T. ) ;
#8189=CARTESIAN_POINT ( 'NONE',  ( 0.000000000000000000, -66.01871308925419157, -64.79170103523090063 ) ) ;
#8190=ORIENTED_EDGE ( 'NONE', *, *, #9710, .F. ) ;
#8192=CARTESIAN_POINT ( 'NONE',  ( 0.000000000000000000, -83.89484365856928605, 26.56417150042919673 ) ) ;
#8193=ORIENTED_EDGE ( 'NONE', *, *, #11805, .F. ) ;
#8194=DIRECTION ( 'NONE',  ( -1.000000000000000000, 0.000000000000000000, -0.000000000000000000 ) ) ;
#8195=EDGE_LOOP ( 'NONE', ( #21561, #3504, #20638, #12105 ) ) ;
#8197=EDGE_CURVE ( 'NONE', #10882, #20413, #14941, .T. ) ;
#8198=DIRECTION ( 'NONE',  ( 0.000000000000000000, 0.000000000000000000, 1.000000000000000000 ) ) ;
#8199=VERTEX_POINT ( 'NONE', #5277 ) ;
#8200=EDGE_CURVE ( 'NONE', #12235, #378, #5426, .T. ) ;
#8201=DIRECTION ( 'NONE',  ( -1.000000000000000000, 0.000000000000000000, 0.000000000000000000 ) ) ;
#8202=CARTESIAN_POINT ( 'NONE',  ( 10.00000000000000000, 35.34277389771654043, -85.48288328206348297 ) ) ;
#8203=CIRCLE ( 'NONE', #2191, 44.99999999999998579 ) ;
#8204=DIRECTION ( 'NONE',  ( -1.000000000000000000, 0.000000000000000000, 0.000000000000000000 ) ) ;
#8206=CARTESIAN_POINT ( 'NONE',  ( 5.000000000000002665, 29.47587714451039531, 82.91666097089130005 ) ) ;
#8207=ADVANCED_FACE ( 'NONE', ( #21841 ), #18538, .F. ) ;
#8208=DIRECTION ( 'NONE',  ( -1.000000000000000000, -0.000000000000000000, 0.000000000000000000 ) ) ;
#8211=AXIS2_PLACEMENT_3D ( 'NONE', #13697, #5408, #3860 ) ;
#8213=CIRCLE ( 'NONE', #12428, 88.00000000000000000 ) ;
#8214=CARTESIAN_POINT ( 'NONE',  ( 5.000000000000002665, -83.48638250753209888, -27.82128566055197538 ) ) ;
#8216=AXIS2_PLACEMENT_3D ( 'NONE', #20548, #1869, #17239 ) ;
#8217=ORIENTED_EDGE ( 'NONE', *, *, #16107, .T. ) ;
#8218=DIRECTION ( 'NONE',  ( 1.000000000000000000, 0.000000000000000000, -0.000000000000000000 ) ) ;
#8221=ORIENTED_EDGE ( 'NONE', *, *, #6106, .F. ) ;
#8222=AXIS2_PLACEMENT_3D ( 'NONE', #16350, #9595, #6324 ) ;
#8229=CARTESIAN_POINT ( 'NONE',  ( 10.00000000000000000, 78.80192417387927151, 39.16958956249325752 ) ) ;
#8231=ORIENTED_EDGE ( 'NONE', *, *, #19847, .F. ) ;
#8232=LINE ( 'NONE', #13192, #2270 ) ;
#8233=DIRECTION ( 'NONE',  ( -1.000000000000000000, -0.000000000000000000, -0.000000000000000000 ) ) ;
#8234=DIRECTION ( 'NONE',  ( -1.000000000000000000, -0.000000000000000000, -0.000000000000000000 ) ) ;
#8235=CARTESIAN_POINT ( 'NONE',  ( 10.00000000000000000, 0.6609040254611577847, 87.99751818016873983 ) ) ;
#8236=CARTESIAN_POINT ( 'NONE',  ( 0.000000000000000000, -30.71797041605865175, 82.46457599186540222 ) ) ;
#8237=CARTESIAN_POINT ( 'NONE',  ( 5.000000000000002665, -73.32282170386815778, -48.65967342042856103 ) ) ;
#8238=AXIS2_PLACEMENT_3D ( 'NONE', #16324, #15897, #18006 ) ;
#8239=ORIENTED_EDGE ( 'NONE', *, *, #17997, .T. ) ;
#8241=EDGE_CURVE ( 'NONE', #17170, #5244, #192, .T. ) ;
#8242=CIRCLE ( 'NONE', #8924, 92.50100000000000477 ) ;
#8244=ORIENTED_EDGE ( 'NONE', *, *, #4279, .T. ) ;
#8245=CIRCLE ( 'NONE', #7897, 44.99999999999999289 ) ;
#8246=EDGE_CURVE ( 'NONE', #13331, #15908, #8245, .T. ) ;
#8247=FACE_OUTER_BOUND ( 'NONE', #7606, .T. ) ;
#8248=ORIENTED_EDGE ( 'NONE', *, *, #8143, .T. ) ;
#8250=DIRECTION ( 'NONE',  ( 0.000000000000000000, 0.000000000000000000, 1.000000000000000000 ) ) ;
#8252=FACE_OUTER_BOUND ( 'NONE', #7948, .T. ) ;
#8256=EDGE_LOOP ( 'NONE', ( #2918, #20379, #19524, #5207 ) ) ;
#8259=ORIENTED_EDGE ( 'NONE', *, *, #6393, .T. ) ;
#8263=CARTESIAN_POINT ( 'NONE',  ( 0.000000000000000000, -86.77540292929691645, -14.62974526292806843 ) ) ;
#8265=CARTESIAN_POINT ( 'NONE',  ( 10.00000000000000000, -30.71797041605865175, 82.46457599186540222 ) ) ;
#8268=DIRECTION ( 'NONE',  ( -1.000000000000000000, -0.000000000000000000, -0.000000000000000000 ) ) ;
#8269=CARTESIAN_POINT ( 'NONE',  ( 10.00000000000000000, -81.34229909304657724, -33.57723005635448743 ) ) ;
#8271=EDGE_CURVE ( 'NONE', #3795, #18196, #15995, .T. ) ;
#8272=CIRCLE ( 'NONE', #7214, 44.99999999999999289 ) ;
#8275=EDGE_CURVE ( 'NONE', #21543, #1099, #6841, .T. ) ;
#8278=ORIENTED_EDGE ( 'NONE', *, *, #18911, .F. ) ;
#8279=CARTESIAN_POINT ( 'NONE',  ( 0.000000000000000000, 0.000000000000000000, 0.000000000000000000 ) ) ;
#8280=ORIENTED_EDGE ( 'NONE', *, *, #18483, .F. ) ;
#8281=CIRCLE ( 'NONE', #6175, 44.99999999999999289 ) ;
#8283=VERTEX_POINT ( 'NONE', #5702 ) ;
#8285=ORIENTED_EDGE ( 'NONE', *, *, #11916, .F. ) ;
#8286=DIRECTION ( 'NONE',  ( -1.000000000000000000, 0.000000000000000000, 0.000000000000000000 ) ) ;
#8289=ORIENTED_EDGE ( 'NONE', *, *, #5184, .F. ) ;
#8290=DIRECTION ( 'NONE',  ( -1.000000000000000000, 0.000000000000000000, 0.000000000000000000 ) ) ;
#8291=AXIS2_PLACEMENT_3D ( 'NONE', #21114, #13933, #2218 ) ;
#8292=DIRECTION ( 'NONE',  ( 0.000000000000000000, 0.000000000000000000, -1.000000000000000000 ) ) ;
#8293=FACE_OUTER_BOUND ( 'NONE', #17761, .T. ) ;
#8294=DIRECTION ( 'NONE',  ( 0.000000000000000000, 0.8290375725550390706, 0.5591929034707507906 ) ) ;
#8296=AXIS2_PLACEMENT_3D ( 'NONE', #1083, #10696, #4399 ) ;
#8299=ORIENTED_EDGE ( 'NONE', *, *, #6465, .T. ) ;
#8300=EDGE_CURVE ( 'NONE', #7517, #10208, #19398, .T. ) ;
#8302=AXIS2_PLACEMENT_3D ( 'NONE', #19839, #14873, #21716 ) ;
#8306=EDGE_CURVE ( 'NONE', #20360, #16218, #7258, .T. ) ;
#8308=VECTOR ( 'NONE', #11639, 1000.000000000000000 ) ;
#8309=CARTESIAN_POINT ( 'NONE',  ( 0.000000000000000000, 0.000000000000000000, 0.000000000000000000 ) ) ;
#8311=LINE ( 'NONE', #21780, #20429 ) ;
#8314=CARTESIAN_POINT ( 'NONE',  ( 0.000000000000000000, 2.208823992044147033, 85.03123271466937183 ) ) ;
#8315=ORIENTED_EDGE ( 'NONE', *, *, #2884, .T. ) ;
#8317=DIRECTION ( 'NONE',  ( 0.000000000000000000, 0.000000000000000000, 1.000000000000000000 ) ) ;
#8318=DIRECTION ( 'NONE',  ( -1.000000000000000000, -0.000000000000000000, -0.000000000000000000 ) ) ;
#8319=CARTESIAN_POINT ( 'NONE',  ( 0.000000000000000000, 0.000000000000000000, 0.000000000000000000 ) ) ;
#8321=AXIS2_PLACEMENT_3D ( 'NONE', #5253, #13755, #10539 ) ;
#8322=DIRECTION ( 'NONE',  ( -1.000000000000000000, 0.000000000000000000, -0.000000000000000000 ) ) ;
#8323=LINE ( 'NONE', #4575, #6924 ) ;
#8324=CARTESIAN_POINT ( 'NONE',  ( 0.000000000000000000, -84.19736439813830486, 38.30455363800903257 ) ) ;
#8325=AXIS2_PLACEMENT_3D ( 'NONE', #17693, #12172, #18922 ) ;
#8326=ORIENTED_EDGE ( 'NONE', *, *, #13414, .F. ) ;
#8327=ADVANCED_FACE ( 'NONE', ( #20838, #4261 ), #5816, .F. ) ;
#8333=CARTESIAN_POINT ( 'NONE',  ( 10.00000000000000000, -45.60224695560626174, 80.47900393021710386 ) ) ;
#8337=ORIENTED_EDGE ( 'NONE', *, *, #12994, .F. ) ;
#8339=VERTEX_POINT ( 'NONE', #3932 ) ;
#8340=VERTEX_POINT ( 'NONE', #509 ) ;
#8341=DIRECTION ( 'NONE',  ( -1.000000000000000000, -0.000000000000000000, -0.000000000000000000 ) ) ;
#8343=ORIENTED_EDGE ( 'NONE', *, *, #919, .F. ) ;
#8348=CARTESIAN_POINT ( 'NONE',  ( 10.00000000000000000, 47.19205848891868271, -74.27590198428072199 ) ) ;
#8351=ORIENTED_EDGE ( 'NONE', *, *, #21534, .T. ) ;
#8352=CARTESIAN_POINT ( 'NONE',  ( 10.00000000000000000, 51.76708072107978609, -67.49339815138442589 ) ) ;
#8353=DIRECTION ( 'NONE',  ( 1.000000000000000000, 0.000000000000000000, 0.000000000000000000 ) ) ;
#8355=VERTEX_POINT ( 'NONE', #16076 ) ;
#8356=DIRECTION ( 'NONE',  ( -1.000000000000000000, -0.000000000000000000, -0.000000000000000000 ) ) ;
#8359=DIRECTION ( 'NONE',  ( -1.000000000000000000, 0.000000000000000000, 0.000000000000000000 ) ) ;
#8361=EDGE_CURVE ( 'NONE', #9927, #16102, #20251, .T. ) ;
#8365=ORIENTED_EDGE ( 'NONE', *, *, #19121, .F. ) ;
#8366=CIRCLE ( 'NONE', #3785, 92.50099999999999056 ) ;
#8367=VERTEX_POINT ( 'NONE', #14099 ) ;
#8371=EDGE_CURVE ( 'NONE', #5897, #3353, #19168, .T. ) ;
#8373=CARTESIAN_POINT ( 'NONE',  ( 0.000000000000000000, 0.000000000000000000, 0.000000000000000000 ) ) ;
#8375=CYLINDRICAL_SURFACE ( 'NONE', #9700, 45.00000000000000000 ) ;
#8376=LINE ( 'NONE', #8053, #13510 ) ;
#8377=CARTESIAN_POINT ( 'NONE',  ( 10.00000000000000000, -0.6609040254617754018, 87.99751818016873983 ) ) ;
#8379=CARTESIAN_POINT ( 'NONE',  ( 0.000000000000000000, 43.18649929580192293, 73.28107340219430910 ) ) ;
#8380=AXIS2_PLACEMENT_3D ( 'NONE', #9154, #21205, #6075 ) ;
#8381=EDGE_CURVE ( 'NONE', #5874, #10147, #13541, .T. ) ;
#8383=EDGE_CURVE ( 'NONE', #15096, #19570, #120, .T. ) ;
#8384=CIRCLE ( 'NONE', #8741, 88.00000000000000000 ) ;
#8386=CIRCLE ( 'NONE', #9787, 92.50099999999999056 ) ;
#8387=DIRECTION ( 'NONE',  ( 1.000000000000000000, 0.000000000000000000, 0.000000000000000000 ) ) ;
#8390=EDGE_CURVE ( 'NONE', #9443, #19711, #6866, .T. ) ;
#8392=ORIENTED_EDGE ( 'NONE', *, *, #15158, .F. ) ;
#8393=DIRECTION ( 'NONE',  ( 0.000000000000000000, 0.000000000000000000, 1.000000000000000000 ) ) ;
#8394=ORIENTED_EDGE ( 'NONE', *, *, #16200, .T. ) ;
#8395=ORIENTED_EDGE ( 'NONE', *, *, #18091, .T. ) ;
#8396=ORIENTED_EDGE ( 'NONE', *, *, #15133, .F. ) ;
#8397=ADVANCED_FACE ( 'NONE', ( #828 ), #20734, .F. ) ;
#8398=CYLINDRICAL_SURFACE ( 'NONE', #6679, 45.00000000000000000 ) ;
#8399=CIRCLE ( 'NONE', #14745, 88.00000000000000000 ) ;
#8402=VECTOR ( 'NONE', #14947, 1000.000000000000000 ) ;
#8404=CIRCLE ( 'NONE', #12630, 44.99999999999999289 ) ;
#8405=CYLINDRICAL_SURFACE ( 'NONE', #5036, 88.00000000000000000 ) ;
#8407=CYLINDRICAL_SURFACE ( 'NONE', #14209, 88.00000000000000000 ) ;
#8410=CARTESIAN_POINT ( 'NONE',  ( 10.00000000000000000, -21.65267340503310223, 89.93106657554424999 ) ) ;
#8412=DIRECTION ( 'NONE',  ( 1.000000000000000000, 0.000000000000000000, 0.000000000000000000 ) ) ;
#8414=VECTOR ( 'NONE', #19684, 1000.000000000000000 ) ;
#8415=ORIENTED_EDGE ( 'NONE', *, *, #7824, .T. ) ;
#8416=VECTOR ( 'NONE', #2892, 1000.000000000000000 ) ;
#8417=AXIS2_PLACEMENT_3D ( 'NONE', #2660, #4111, #14051 ) ;
#8418=EDGE_LOOP ( 'NONE', ( #9052, #17138, #15222, #17855 ) ) ;
#8419=DIRECTION ( 'NONE',  ( 0.000000000000000000, 0.3420201433256630508, 0.9396926207859105373 ) ) ;
#8421=CARTESIAN_POINT ( 'NONE',  ( 0.000000000000000000, 0.000000000000000000, 0.000000000000000000 ) ) ;
#8425=EDGE_CURVE ( 'NONE', #11066, #15191, #7544, .T. ) ;
#8427=ORIENTED_EDGE ( 'NONE', *, *, #8650, .F. ) ;
#8428=EDGE_CURVE ( 'NONE', #16416, #5623, #6513, .T. ) ;
#8429=CARTESIAN_POINT ( 'NONE',  ( 10.00000000000000000, 82.02147376274669455, 42.76579056660889933 ) ) ;
#8430=AXIS2_PLACEMENT_3D ( 'NONE', #15227, #12135, #20446 ) ;
#8433=AXIS2_PLACEMENT_3D ( 'NONE', #6935, #13980, #8795 ) ;
#8435=ADVANCED_FACE ( 'NONE', ( #5923 ), #12649, .F. ) ;
#8437=CIRCLE ( 'NONE', #20076, 92.50100000000000477 ) ;
#8438=AXIS2_PLACEMENT_3D ( 'NONE', #19537, #16449, #21538 ) ;
#8439=ADVANCED_FACE ( 'NONE', ( #14752 ), #12867, .F. ) ;
#8441=DIRECTION ( 'NONE',  ( -1.000000000000000000, -0.000000000000000000, -0.000000000000000000 ) ) ;
#8442=CYLINDRICAL_SURFACE ( 'NONE', #20747, 88.00000000000000000 ) ;
#8444=CARTESIAN_POINT ( 'NONE',  ( 10.00000000000000000, -90.63195040374199607, 18.50093422002390398 ) ) ;
#8446=CARTESIAN_POINT ( 'NONE',  ( 5.000000000000002665, -79.38136668499713267, -37.98155635597392887 ) ) ;
#8447=VERTEX_POINT ( 'NONE', #4366 ) ;
#8450=LINE ( 'NONE', #18063, #7752 ) ;
#8451=ORIENTED_EDGE ( 'NONE', *, *, #4865, .T. ) ;
#8452=VERTEX_POINT ( 'NONE', #14423 ) ;
#8453=CARTESIAN_POINT ( 'NONE',  ( 0.000000000000000000, 0.000000000000000000, 0.000000000000000000 ) ) ;
#8454=ORIENTED_EDGE ( 'NONE', *, *, #14036, .T. ) ;
#8455=ORIENTED_EDGE ( 'NONE', *, *, #10393, .F. ) ;
#8457=DIRECTION ( 'NONE',  ( -1.000000000000000000, 0.000000000000000000, 0.000000000000000000 ) ) ;
#8459=CYLINDRICAL_SURFACE ( 'NONE', #5819, 44.99999999999999289 ) ;
#8463=DIRECTION ( 'NONE',  ( -1.000000000000000000, 0.000000000000000000, -0.000000000000000000 ) ) ;
#8464=DIRECTION ( 'NONE',  ( -1.000000000000000000, 0.000000000000000000, -0.000000000000000000 ) ) ;
#8467=EDGE_LOOP ( 'NONE', ( #3328, #7989, #15868, #2734 ) ) ;
#8468=CIRCLE ( 'NONE', #7071, 45.00000000000000000 ) ;
#8469=CARTESIAN_POINT ( 'NONE',  ( 10.00000000000000000, 51.76708072107885528, 67.49339815138510801 ) ) ;
#8470=CARTESIAN_POINT ( 'NONE',  ( 10.00000000000000000, 77.39385041987151226, -35.28996114464630551 ) ) ;
#8471=ORIENTED_EDGE ( 'NONE', *, *, #2768, .T. ) ;
#8472=DIRECTION ( 'NONE',  ( 0.000000000000000000, 0.5299192642332061221, -0.8480480961564251796 ) ) ;
#8473=ORIENTED_EDGE ( 'NONE', *, *, #6921, .T. ) ;
#8474=CYLINDRICAL_SURFACE ( 'NONE', #19716, 88.00000000000000000 ) ;
#8475=VERTEX_POINT ( 'NONE', #21387 ) ;
#8476=CYLINDRICAL_SURFACE ( 'NONE', #14857, 44.99999999999999289 ) ;
#8477=ORIENTED_EDGE ( 'NONE', *, *, #415, .F. ) ;
#8478=ORIENTED_EDGE ( 'NONE', *, *, #9189, .F. ) ;
#8479=ORIENTED_EDGE ( 'NONE', *, *, #13407, .T. ) ;
#8480=CIRCLE ( 'NONE', #4248, 88.00000000000000000 ) ;
#8481=CARTESIAN_POINT ( 'NONE',  ( 10.00000000000000000, -65.64563793391792501, -54.09103124042881916 ) ) ;
#8483=DIRECTION ( 'NONE',  ( -1.000000000000000000, -0.000000000000000000, -0.000000000000000000 ) ) ;
#8484=DIRECTION ( 'NONE',  ( -1.000000000000000000, -0.000000000000000000, -0.000000000000000000 ) ) ;
#8487=DIRECTION ( 'NONE',  ( 0.000000000000000000, 0.000000000000000000, -1.000000000000000000 ) ) ;
#8488=CARTESIAN_POINT ( 'NONE',  ( 0.000000000000000000, -81.97107881582179800, -22.71412948308650925 ) ) ;
#8492=DIRECTION ( 'NONE',  ( -1.000000000000000000, -0.000000000000000000, -0.000000000000000000 ) ) ;
#8493=DIRECTION ( 'NONE',  ( -1.000000000000000000, -0.000000000000000000, -0.000000000000000000 ) ) ;
#8496=ORIENTED_EDGE ( 'NONE', *, *, #675, .T. ) ;
#8497=DIRECTION ( 'NONE',  ( 0.000000000000000000, -0.7880107536067146867, -0.6156614753256676176 ) ) ;
#8499=CARTESIAN_POINT ( 'NONE',  ( 0.000000000000000000, 0.000000000000000000, 0.000000000000000000 ) ) ;
#8501=ORIENTED_EDGE ( 'NONE', *, *, #7840, .T. ) ;
#8502=ORIENTED_EDGE ( 'NONE', *, *, #5716, .T. ) ;
#8503=DIRECTION ( 'NONE',  ( 0.000000000000000000, 0.4067366430758009854, -0.9135454576426005335 ) ) ;
#8505=CARTESIAN_POINT ( 'NONE',  ( 0.000000000000000000, 72.53479564998846740, -44.42851404693280415 ) ) ;
#8507=EDGE_CURVE ( 'NONE', #18557, #9877, #1555, .T. ) ;
#8508=CARTESIAN_POINT ( 'NONE',  ( 0.000000000000000000, -9.646732466565913100, 84.51112348751846071 ) ) ;
#8509=EDGE_CURVE ( 'NONE', #18330, #4091, #13182, .T. ) ;
#8512=DIRECTION ( 'NONE',  ( 1.000000000000000000, 0.000000000000000000, 0.000000000000000000 ) ) ;
#8513=CARTESIAN_POINT ( 'NONE',  ( 10.00000000000000000, 41.21966518005955038, 82.80926399530301296 ) ) ;
#8514=DIRECTION ( 'NONE',  ( 0.000000000000000000, 0.000000000000000000, 1.000000000000000000 ) ) ;
#8516=CYLINDRICAL_SURFACE ( 'NONE', #9029, 45.00000000000000000 ) ;
#8518=ORIENTED_EDGE ( 'NONE', *, *, #9163, .F. ) ;
#8521=FACE_OUTER_BOUND ( 'NONE', #7334, .T. ) ;
#8523=DIRECTION ( 'NONE',  ( 0.000000000000000000, 0.000000000000000000, 1.000000000000000000 ) ) ;
#8524=VERTEX_POINT ( 'NONE', #1161 ) ;
#8525=ORIENTED_EDGE ( 'NONE', *, *, #1112, .T. ) ;
#8526=CARTESIAN_POINT ( 'NONE',  ( 10.00000000000000000, 69.74988376404020585, 53.65588238863360715 ) ) ;
#8527=EDGE_CURVE ( 'NONE', #15310, #3214, #16721, .T. ) ;
#8528=ORIENTED_EDGE ( 'NONE', *, *, #517, .T. ) ;
#8530=DIRECTION ( 'NONE',  ( 1.000000000000000000, 0.000000000000000000, 0.000000000000000000 ) ) ;
#8531=EDGE_CURVE ( 'NONE', #19278, #2087, #138, .T. ) ;
#8534=AXIS2_PLACEMENT_3D ( 'NONE', #19184, #12014, #18868 ) ;
#8537=CARTESIAN_POINT ( 'NONE',  ( 10.00000000000000000, 35.18804927320642406, -80.65854690202642985 ) ) ;
#8539=EDGE_LOOP ( 'NONE', ( #10493, #12104, #5827, #8239 ) ) ;
#8544=DIRECTION ( 'NONE',  ( 1.000000000000000000, 0.000000000000000000, 0.000000000000000000 ) ) ;
#8545=VERTEX_POINT ( 'NONE', #4691 ) ;
#8546=DIRECTION ( 'NONE',  ( -1.000000000000000000, 0.000000000000000000, 0.000000000000000000 ) ) ;
#8548=EDGE_CURVE ( 'NONE', #13890, #4009, #15666, .T. ) ;
#8549=ORIENTED_EDGE ( 'NONE', *, *, #1205, .F. ) ;
#8551=AXIS2_PLACEMENT_3D ( 'NONE', #2442, #10507, #360 ) ;
#8552=ORIENTED_EDGE ( 'NONE', *, *, #4369, .F. ) ;
#8556=ORIENTED_EDGE ( 'NONE', *, *, #7331, .F. ) ;
#8558=DIRECTION ( 'NONE',  ( 0.000000000000000000, 0.000000000000000000, 1.000000000000000000 ) ) ;
#8559=CARTESIAN_POINT ( 'NONE',  ( 0.000000000000000000, -84.12297548659712731, 32.40974838672912028 ) ) ;
#8561=CARTESIAN_POINT ( 'NONE',  ( 10.00000000000000000, -70.37753541435978377, 60.02863908169610596 ) ) ;
#8562=AXIS2_PLACEMENT_3D ( 'NONE', #18760, #17214, #7059 ) ;
#8565=EDGE_LOOP ( 'NONE', ( #19499, #9944, #12134, #4644 ) ) ;
#8566=DIRECTION ( 'NONE',  ( 0.000000000000000000, 0.000000000000000000, 1.000000000000000000 ) ) ;
#8569=FACE_OUTER_BOUND ( 'NONE', #15631, .T. ) ;
#8570=VERTEX_POINT ( 'NONE', #4925 ) ;
#8571=CIRCLE ( 'NONE', #17389, 44.99999999999998579 ) ;
#8572=CYLINDRICAL_SURFACE ( 'NONE', #18694, 44.99999999999999289 ) ;
#8573=LINE ( 'NONE', #8888, #1382 ) ;
#8574=EDGE_LOOP ( 'NONE', ( #1434, #10718, #9356, #10934 ) ) ;
#8575=CIRCLE ( 'NONE', #20921, 88.00000000000000000 ) ;
#8577=DIRECTION ( 'NONE',  ( 0.000000000000000000, 0.000000000000000000, 1.000000000000000000 ) ) ;
#8578=ORIENTED_EDGE ( 'NONE', *, *, #10642, .F. ) ;
#8579=ORIENTED_EDGE ( 'NONE', *, *, #10813, .T. ) ;
#8580=ORIENTED_EDGE ( 'NONE', *, *, #20447, .T. ) ;
#8583=DIRECTION ( 'NONE',  ( 1.000000000000000000, 0.000000000000000000, 0.000000000000000000 ) ) ;
#8585=CARTESIAN_POINT ( 'NONE',  ( 10.00000000000000000, -2.208823992044743445, 85.03123271466935762 ) ) ;
#8586=CARTESIAN_POINT ( 'NONE',  ( 0.000000000000000000, 79.66702613806732813, 29.80527447819576636 ) ) ;
#8592=VECTOR ( 'NONE', #7046, 1000.000000000000000 ) ;
#8594=CARTESIAN_POINT ( 'NONE',  ( 0.000000000000000000, -71.33759994381919967, -58.88447872959059737 ) ) ;
#8596=VERTEX_POINT ( 'NONE', #13419 ) ;
#8597=AXIS2_PLACEMENT_3D ( 'NONE', #13782, #20624, #20522 ) ;
#8598=LINE ( 'NONE', #13473, #10533 ) ;
#8599=ORIENTED_EDGE ( 'NONE', *, *, #16589, .F. ) ;
#8602=CIRCLE ( 'NONE', #18494, 44.99999999999999289 ) ;
#8604=AXIS2_PLACEMENT_3D ( 'NONE', #6040, #11319, #14529 ) ;
#8606=DIRECTION ( 'NONE',  ( 0.000000000000000000, 0.000000000000000000, 1.000000000000000000 ) ) ;
#8611=LINE ( 'NONE', #13585, #5405 ) ;
#8612=CARTESIAN_POINT ( 'NONE',  ( 0.000000000000000000, 0.000000000000000000, 0.000000000000000000 ) ) ;
#8614=CARTESIAN_POINT ( 'NONE',  ( 0.000000000000000000, 0.000000000000000000, 0.000000000000000000 ) ) ;
#8617=EDGE_LOOP ( 'NONE', ( #3580, #11335, #14181, #11240 ) ) ;
#8620=DIRECTION ( 'NONE',  ( -1.000000000000000000, -0.000000000000000000, -0.000000000000000000 ) ) ;
#8623=ORIENTED_EDGE ( 'NONE', *, *, #5910, .T. ) ;
#8624=CARTESIAN_POINT ( 'NONE',  ( 10.00000000000000000, 27.00677879429026618, 80.65868421664441712 ) ) ;
#8626=ORIENTED_EDGE ( 'NONE', *, *, #13126, .F. ) ;
#8627=ORIENTED_EDGE ( 'NONE', *, *, #17266, .F. ) ;
#8629=AXIS2_PLACEMENT_3D ( 'NONE', #382, #7020, #7121 ) ;
#8630=DIRECTION ( 'NONE',  ( -1.000000000000000000, -0.000000000000000000, -0.000000000000000000 ) ) ;
#8635=DIRECTION ( 'NONE',  ( 0.000000000000000000, 0.000000000000000000, 1.000000000000000000 ) ) ;
#8638=CARTESIAN_POINT ( 'NONE',  ( 10.00000000000000000, -10.41137886060045226, -91.91321010181856366 ) ) ;
#8639=DIRECTION ( 'NONE',  ( -1.000000000000000000, -0.000000000000000000, -0.000000000000000000 ) ) ;
#8642=AXIS2_PLACEMENT_3D ( 'NONE', #8063, #16776, #11699 ) ;
#8646=EDGE_CURVE ( 'NONE', #6638, #7563, #6800, .T. ) ;
#8648=AXIS2_PLACEMENT_3D ( 'NONE', #3720, #10342, #17208 ) ;
#8649=DIRECTION ( 'NONE',  ( -1.000000000000000000, -0.000000000000000000, 0.000000000000000000 ) ) ;
#8650=EDGE_CURVE ( 'NONE', #14884, #14755, #18617, .T. ) ;
#8651=CARTESIAN_POINT ( 'NONE',  ( 0.000000000000000000, 0.000000000000000000, 0.000000000000000000 ) ) ;
#8653=VECTOR ( 'NONE', #13305, 1000.000000000000000 ) ;
#8654=DIRECTION ( 'NONE',  ( -1.000000000000000000, 0.000000000000000000, 0.000000000000000000 ) ) ;
#8657=DIRECTION ( 'NONE',  ( 0.000000000000000000, -0.4067366430757887175, -0.9135454576426059736 ) ) ;
#8659=AXIS2_PLACEMENT_3D ( 'NONE', #18198, #8353, #19743 ) ;
#8661=DIRECTION ( 'NONE',  ( 0.000000000000000000, 0.000000000000000000, 1.000000000000000000 ) ) ;
#8663=CIRCLE ( 'NONE', #17848, 88.00000000000000000 ) ;
#8664=AXIS2_PLACEMENT_3D ( 'NONE', #17510, #16051, #5678 ) ;
#8665=EDGE_CURVE ( 'NONE', #18379, #13984, #4728, .T. ) ;
#8666=CIRCLE ( 'NONE', #211, 44.99999999999999289 ) ;
#8668=CARTESIAN_POINT ( 'NONE',  ( 10.00000000000000000, 78.80192417387979731, -39.16958956249220591 ) ) ;
#8669=LINE ( 'NONE', #13639, #5500 ) ;
#8671=DIRECTION ( 'NONE',  ( -1.000000000000000000, -0.000000000000000000, -0.000000000000000000 ) ) ;
#8674=ORIENTED_EDGE ( 'NONE', *, *, #3940, .F. ) ;
#8675=ADVANCED_FACE ( 'NONE', ( #10214 ), #267, .F. ) ;
#8676=DIRECTION ( 'NONE',  ( 1.000000000000000000, 0.000000000000000000, 0.000000000000000000 ) ) ;
#8677=DIRECTION ( 'NONE',  ( 0.000000000000000000, 0.06975647374412555224, -0.9975640502598241977 ) ) ;
#8678=ORIENTED_EDGE ( 'NONE', *, *, #10714, .F. ) ;
#8680=AXIS2_PLACEMENT_3D ( 'NONE', #7457, #813, #20927 ) ;
#8681=AXIS2_PLACEMENT_3D ( 'NONE', #34, #10294, #11849 ) ;
#8682=CARTESIAN_POINT ( 'NONE',  ( 0.000000000000000000, 0.000000000000000000, 0.000000000000000000 ) ) ;
#8683=AXIS2_PLACEMENT_3D ( 'NONE', #3778, #2127, #14150 ) ;
#8687=CYLINDRICAL_SURFACE ( 'NONE', #13391, 44.99999999999998579 ) ;
#8688=ORIENTED_EDGE ( 'NONE', *, *, #17886, .T. ) ;
#8689=ORIENTED_EDGE ( 'NONE', *, *, #4573, .F. ) ;
#8696=CARTESIAN_POINT ( 'NONE',  ( 5.000000000000002665, 11.59241532900744787, -87.23311244498727035 ) ) ;
#8697=FACE_OUTER_BOUND ( 'NONE', #9337, .T. ) ;
#8699=CARTESIAN_POINT ( 'NONE',  ( 0.000000000000000000, 84.33453774737657227, 11.08490790852157559 ) ) ;
#8700=EDGE_CURVE ( 'NONE', #11814, #8596, #857, .T. ) ;
#8705=CARTESIAN_POINT ( 'NONE',  ( 10.00000000000000000, -23.10190250628894404, 89.56973317806591695 ) ) ;
#8706=DIRECTION ( 'NONE',  ( -1.000000000000000000, -0.000000000000000000, -0.000000000000000000 ) ) ;
#8707=ADVANCED_FACE ( 'NONE', ( #12080 ), #17062, .F. ) ;
#8708=VERTEX_POINT ( 'NONE', #6589 ) ;
#8710=LINE ( 'NONE', #18444, #5996 ) ;
#8711=CARTESIAN_POINT ( 'NONE',  ( 10.00000000000000000, 0.000000000000000000, 0.000000000000000000 ) ) ;
#8712=DIRECTION ( 'NONE',  ( -1.000000000000000000, 0.000000000000000000, -0.000000000000000000 ) ) ;
#8713=ORIENTED_EDGE ( 'NONE', *, *, #12604, .T. ) ;
#8714=AXIS2_PLACEMENT_3D ( 'NONE', #8614, #13589, #17243 ) ;
#8716=VECTOR ( 'NONE', #2084, 1000.000000000000000 ) ;
#8718=DIRECTION ( 'NONE',  ( 0.000000000000000000, 0.000000000000000000, 1.000000000000000000 ) ) ;
#8719=ORIENTED_EDGE ( 'NONE', *, *, #1270, .T. ) ;
#8721=EDGE_LOOP ( 'NONE', ( #8188, #18172, #7643, #7367 ) ) ;
#8722=CARTESIAN_POINT ( 'NONE',  ( 10.00000000000000000, 71.72924546250010280, -45.71766382684594276 ) ) ;
#8726=LINE ( 'NONE', #18890, #18099 ) ;
#8728=AXIS2_PLACEMENT_3D ( 'NONE', #18227, #16448, #6306 ) ;
#8729=FACE_OUTER_BOUND ( 'NONE', #20018, .T. ) ;
#8731=LINE ( 'NONE', #3968, #12156 ) ;
#8732=CARTESIAN_POINT ( 'NONE',  ( 0.000000000000000000, 77.39385041987100067, 35.28996114464738554 ) ) ;
#8733=DIRECTION ( 'NONE',  ( 1.000000000000000000, 0.000000000000000000, 0.000000000000000000 ) ) ;
#8736=ORIENTED_EDGE ( 'NONE', *, *, #7319, .T. ) ;
#8737=VERTEX_POINT ( 'NONE', #7341 ) ;
#8738=AXIS2_PLACEMENT_3D ( 'NONE', #12468, #761, #4082 ) ;
#8739=CARTESIAN_POINT ( 'NONE',  ( 10.00000000000000000, 41.21966518006070146, -82.80926399530243032 ) ) ;
#8740=ORIENTED_EDGE ( 'NONE', *, *, #14819, .F. ) ;
#8741=AXIS2_PLACEMENT_3D ( 'NONE', #8682, #13863, #11886 ) ;
#8742=EDGE_LOOP ( 'NONE', ( #20910, #6498, #11510, #15033 ) ) ;
#8744=DIRECTION ( 'NONE',  ( 0.000000000000000000, 0.000000000000000000, 1.000000000000000000 ) ) ;
#8745=ORIENTED_EDGE ( 'NONE', *, *, #21533, .T. ) ;
#8749=EDGE_CURVE ( 'NONE', #3486, #1974, #14256, .T. ) ;
#8750=DIRECTION ( 'NONE',  ( 1.000000000000000000, -0.000000000000000000, 0.000000000000000000 ) ) ;
#8751=CARTESIAN_POINT ( 'NONE',  ( 10.00000000000000000, 33.95793648385814123, 86.04239391578002483 ) ) ;
#8753=DIRECTION ( 'NONE',  ( 0.000000000000000000, 0.000000000000000000, 1.000000000000000000 ) ) ;
#8754=CIRCLE ( 'NONE', #11567, 92.50100000000000477 ) ;
#8755=CIRCLE ( 'NONE', #18298, 88.00000000000000000 ) ;
#8756=ORIENTED_EDGE ( 'NONE', *, *, #4300, .T. ) ;
#8759=DIRECTION ( 'NONE',  ( 0.000000000000000000, 0.9945218953682736229, -0.1045284632676503761 ) ) ;
#8765=AXIS2_PLACEMENT_3D ( 'NONE', #17791, #14477, #17583 ) ;
#8767=ORIENTED_EDGE ( 'NONE', *, *, #3418, .T. ) ;
#8768=VECTOR ( 'NONE', #18770, 1000.000000000000000 ) ;
#8769=EDGE_LOOP ( 'NONE', ( #21427, #9618, #21346, #10382 ) ) ;
#8771=AXIS2_PLACEMENT_3D ( 'NONE', #14930, #3002, #16368 ) ;
#8772=LINE ( 'NONE', #10534, #2909 ) ;
#8773=CIRCLE ( 'NONE', #1714, 88.00000000000000000 ) ;
#8774=LINE ( 'NONE', #5143, #5474 ) ;
#8775=CARTESIAN_POINT ( 'NONE',  ( 0.000000000000000000, 83.35585896458643163, -16.94078559807864792 ) ) ;
#8778=LINE ( 'NONE', #15516, #20666 ) ;
#8779=EDGE_CURVE ( 'NONE', #19086, #3139, #14276, .T. ) ;
#8780=FACE_OUTER_BOUND ( 'NONE', #13872, .T. ) ;
#8781=DIRECTION ( 'NONE',  ( -1.000000000000000000, 0.000000000000000000, 0.000000000000000000 ) ) ;
#8782=CARTESIAN_POINT ( 'NONE',  ( 10.00000000000000000, -21.31452625070983231, 82.34610137166113475 ) ) ;
#8783=EDGE_CURVE ( 'NONE', #1843, #20663, #16738, .T. ) ;
#8784=CIRCLE ( 'NONE', #15483, 92.50100000000000477 ) ;
#8787=AXIS2_PLACEMENT_3D ( 'NONE', #7495, #5954, #4398 ) ;
#8789=ORIENTED_EDGE ( 'NONE', *, *, #6942, .F. ) ;
#8791=CYLINDRICAL_SURFACE ( 'NONE', #17912, 92.50100000000000477 ) ;
#8792=EDGE_CURVE ( 'NONE', #752, #12349, #14972, .T. ) ;
#8793=EDGE_LOOP ( 'NONE', ( #4830, #21812, #9293, #20754 ) ) ;
#8795=DIRECTION ( 'NONE',  ( 0.000000000000000000, 0.000000000000000000, 1.000000000000000000 ) ) ;
#8796=ORIENTED_EDGE ( 'NONE', *, *, #11255, .T. ) ;
#8798=EDGE_CURVE ( 'NONE', #17227, #9309, #9314, .T. ) ;
#8799=ORIENTED_EDGE ( 'NONE', *, *, #4517, .T. ) ;
#8800=ORIENTED_EDGE ( 'NONE', *, *, #2532, .T. ) ;
#8803=ORIENTED_EDGE ( 'NONE', *, *, #3844, .F. ) ;
#8804=DIRECTION ( 'NONE',  ( 0.000000000000000000, -0.8987940462991619306, -0.4383711467890878399 ) ) ;
#8805=AXIS2_PLACEMENT_3D ( 'NONE', #5899, #17826, #19587 ) ;
#8806=CARTESIAN_POINT ( 'NONE',  ( 0.000000000000000000, -23.62010150527165919, -84.77081340225927875 ) ) ;
#8807=DIRECTION ( 'NONE',  ( 0.000000000000000000, -0.9510565162951565288, 0.3090169943749382919 ) ) ;
#8811=DIRECTION ( 'NONE',  ( -1.000000000000000000, 0.000000000000000000, 0.000000000000000000 ) ) ;
#8812=EDGE_CURVE ( 'NONE', #13330, #21564, #14071, .T. ) ;
#8814=ORIENTED_EDGE ( 'NONE', *, *, #9, .F. ) ;
#8815=CYLINDRICAL_SURFACE ( 'NONE', #684, 88.00000000000000000 ) ;
#8817=DIRECTION ( 'NONE',  ( 0.000000000000000000, -0.2756373558169869509, -0.9612616959383223358 ) ) ;
#8818=EDGE_CURVE ( 'NONE', #5168, #4256, #3680, .T. ) ;
#8821=ORIENTED_EDGE ( 'NONE', *, *, #13477, .F. ) ;
#8822=AXIS2_PLACEMENT_3D ( 'NONE', #11859, #5126, #18607 ) ;
#8823=DIRECTION ( 'NONE',  ( -1.000000000000000000, -0.000000000000000000, 0.000000000000000000 ) ) ;
#8826=ORIENTED_EDGE ( 'NONE', *, *, #15537, .T. ) ;
#8828=EDGE_CURVE ( 'NONE', #1297, #16358, #7119, .T. ) ;
#8829=ORIENTED_EDGE ( 'NONE', *, *, #17755, .T. ) ;
#8830=CARTESIAN_POINT ( 'NONE',  ( 0.000000000000000000, 71.33759994381961178, 58.88447872959011420 ) ) ;
#8831=DIRECTION ( 'NONE',  ( 0.000000000000000000, 0.4067366430758011520, -0.9135454576426004225 ) ) ;
#8832=CARTESIAN_POINT ( 'NONE',  ( 10.00000000000000000, -84.12297548659712731, 32.40974838672912028 ) ) ;
#8833=FACE_OUTER_BOUND ( 'NONE', #19037, .T. ) ;
#8836=CARTESIAN_POINT ( 'NONE',  ( 10.00000000000000000, 0.000000000000000000, 0.000000000000000000 ) ) ;
#8837=DIRECTION ( 'NONE',  ( -1.000000000000000000, 0.000000000000000000, 0.000000000000000000 ) ) ;
#8840=DIRECTION ( 'NONE',  ( -1.000000000000000000, 0.000000000000000000, 0.000000000000000000 ) ) ;
#8841=ORIENTED_EDGE ( 'NONE', *, *, #5316, .T. ) ;
#8844=ORIENTED_EDGE ( 'NONE', *, *, #2861, .T. ) ;
#8845=ORIENTED_EDGE ( 'NONE', *, *, #21212, .F. ) ;
#8846=DIRECTION ( 'NONE',  ( 0.000000000000000000, 0.000000000000000000, 1.000000000000000000 ) ) ;
#8847=ORIENTED_EDGE ( 'NONE', *, *, #9960, .T. ) ;
#8849=ORIENTED_EDGE ( 'NONE', *, *, #15554, .T. ) ;
#8850=DIRECTION ( 'NONE',  ( 1.000000000000000000, 0.000000000000000000, 0.000000000000000000 ) ) ;
#8851=ORIENTED_EDGE ( 'NONE', *, *, #10419, .T. ) ;
#8852=CARTESIAN_POINT ( 'NONE',  ( 0.000000000000000000, 0.000000000000000000, 0.000000000000000000 ) ) ;
#8853=DIRECTION ( 'NONE',  ( 1.000000000000000000, -0.000000000000000000, 0.000000000000000000 ) ) ;
#8854=DIRECTION ( 'NONE',  ( 0.000000000000000000, 0.4694715627858917495, -0.8829475928589264333 ) ) ;
#8855=CARTESIAN_POINT ( 'NONE',  ( 0.000000000000000000, 81.32027326007924728, -44.08455690948973427 ) ) ;
#8856=LINE ( 'NONE', #1799, #2336 ) ;
#8860=ORIENTED_EDGE ( 'NONE', *, *, #8390, .T. ) ;
#8861=CARTESIAN_POINT ( 'NONE',  ( 10.00000000000000000, -43.18649929580143976, -73.28107340219457910 ) ) ;
#8864=EDGE_CURVE ( 'NONE', #1297, #17743, #2624, .T. ) ;
#8865=CARTESIAN_POINT ( 'NONE',  ( 0.000000000000000000, -47.19205848891816402, 74.27590198428104884 ) ) ;
#8866=EDGE_LOOP ( 'NONE', ( #10993, #16457, #8944, #14114 ) ) ;
#8870=VERTEX_POINT ( 'NONE', #379 ) ;
#8873=CARTESIAN_POINT ( 'NONE',  ( 5.000000000000002665, 17.64925110578469258, 86.21197095186350623 ) ) ;
#8875=DIRECTION ( 'NONE',  ( 1.000000000000000000, 0.000000000000000000, 0.000000000000000000 ) ) ;
#8876=DIRECTION ( 'NONE',  ( 1.000000000000000000, 0.000000000000000000, 0.000000000000000000 ) ) ;
#8877=DIRECTION ( 'NONE',  ( 0.000000000000000000, -0.9945218953682744001, 0.1045284632676437564 ) ) ;
#8882=FACE_OUTER_BOUND ( 'NONE', #5629, .T. ) ;
#8884=DIRECTION ( 'NONE',  ( 0.000000000000000000, 0.000000000000000000, 1.000000000000000000 ) ) ;
#8885=ORIENTED_EDGE ( 'NONE', *, *, #14559, .T. ) ;
#8886=CARTESIAN_POINT ( 'NONE',  ( 10.00000000000000000, 69.25892805976580746, -49.38005998797770246 ) ) ;
#8888=CARTESIAN_POINT ( 'NONE',  ( 10.00000000000000000, -66.01871308925505843, 64.79170103522997692 ) ) ;
#8889=ORIENTED_EDGE ( 'NONE', *, *, #9710, .T. ) ;
#8890=ORIENTED_EDGE ( 'NONE', *, *, #11572, .T. ) ;
#8891=VERTEX_POINT ( 'NONE', #15938 ) ;
#8892=ORIENTED_EDGE ( 'NONE', *, *, #9628, .T. ) ;
#8893=CARTESIAN_POINT ( 'NONE',  ( 5.000000000000002665, 35.18804927320529430, 80.65854690202691302 ) ) ;
#8894=ORIENTED_EDGE ( 'NONE', *, *, #17166, .F. ) ;
#8895=DIRECTION ( 'NONE',  ( 1.000000000000000000, -0.000000000000000000, 0.000000000000000000 ) ) ;
#8896=CYLINDRICAL_SURFACE ( 'NONE', #10502, 92.50100000000000477 ) ;
#8897=DIRECTION ( 'NONE',  ( 1.000000000000000000, 0.000000000000000000, 0.000000000000000000 ) ) ;
#8898=DIRECTION ( 'NONE',  ( 0.000000000000000000, 0.5299192642331997938, 0.8480480961564290654 ) ) ;
#8899=DIRECTION ( 'NONE',  ( -1.000000000000000000, -0.000000000000000000, -0.000000000000000000 ) ) ;
#8900=EDGE_CURVE ( 'NONE', #4889, #239, #8281, .T. ) ;
#8902=CARTESIAN_POINT ( 'NONE',  ( 10.00000000000000000, -69.25892805976475586, -49.38005998797915908 ) ) ;
#8905=DIRECTION ( 'NONE',  ( -1.000000000000000000, -0.000000000000000000, -0.000000000000000000 ) ) ;
#8906=AXIS2_PLACEMENT_3D ( 'NONE', #18575, #4870, #11497 ) ;
#8909=DIRECTION ( 'NONE',  ( -1.000000000000000000, -0.000000000000000000, -0.000000000000000000 ) ) ;
#8912=CARTESIAN_POINT ( 'NONE',  ( 0.000000000000000000, 0.000000000000000000, 0.000000000000000000 ) ) ;
#8914=EDGE_CURVE ( 'NONE', #10156, #16787, #6017, .T. ) ;
#8915=EDGE_LOOP ( 'NONE', ( #13096, #18121, #14848, #12005 ) ) ;
#8916=DIRECTION ( 'NONE',  ( 0.000000000000000000, 0.000000000000000000, 1.000000000000000000 ) ) ;
#8919=EDGE_LOOP ( 'NONE', ( #10186, #5291, #20088, #9141 ) ) ;
#8921=DIRECTION ( 'NONE',  ( 1.000000000000000000, 0.000000000000000000, 0.000000000000000000 ) ) ;
#8923=CARTESIAN_POINT ( 'NONE',  ( 0.000000000000000000, 0.000000000000000000, 0.000000000000000000 ) ) ;
#8924=AXIS2_PLACEMENT_3D ( 'NONE', #11668, #4933, #12577 ) ;
#8925=VECTOR ( 'NONE', #18437, 1000.000000000000000 ) ;
#8927=DIRECTION ( 'NONE',  ( -1.000000000000000000, 0.000000000000000000, 0.000000000000000000 ) ) ;
#8928=CARTESIAN_POINT ( 'NONE',  ( 10.00000000000000000, 3.728035544476225649, 84.97818067823770605 ) ) ;
#8929=EDGE_CURVE ( 'NONE', #10036, #8447, #7776, .T. ) ;
#8930=FACE_OUTER_BOUND ( 'NONE', #14037, .T. ) ;
#8931=CARTESIAN_POINT ( 'NONE',  ( -10.00000000000000000, 0.000000000000000000, 0.000000000000000000 ) ) ;
#8933=CARTESIAN_POINT ( 'NONE',  ( -10.00000000000000000, 0.000000000000000000, 0.000000000000000000 ) ) ;
#8935=LINE ( 'NONE', #5745, #13729 ) ;
#8937=ORIENTED_EDGE ( 'NONE', *, *, #12856, .F. ) ;
#8939=DIRECTION ( 'NONE',  ( 1.000000000000000000, 0.000000000000000000, -0.000000000000000000 ) ) ;
#8940=AXIS2_PLACEMENT_3D ( 'NONE', #4133, #10868, #11083 ) ;
#8941=VERTEX_POINT ( 'NONE', #12733 ) ;
#8942=VERTEX_POINT ( 'NONE', #9521 ) ;
#8943=VECTOR ( 'NONE', #5489, 1000.000000000000000 ) ;
#8944=ORIENTED_EDGE ( 'NONE', *, *, #18910, .F. ) ;
#8945=CYLINDRICAL_SURFACE ( 'NONE', #19090, 88.00000000000000000 ) ;
#8948=ORIENTED_EDGE ( 'NONE', *, *, #4517, .F. ) ;
#8950=DIRECTION ( 'NONE',  ( 0.000000000000000000, -0.6427876096865456912, 0.7660444431189725734 ) ) ;
#8951=VECTOR ( 'NONE', #12340, 1000.000000000000000 ) ;
#8957=FACE_OUTER_BOUND ( 'NONE', #15741, .T. ) ;
#8958=CARTESIAN_POINT ( 'NONE',  ( 0.000000000000000000, 0.000000000000000000, 0.000000000000000000 ) ) ;
#8959=EDGE_CURVE ( 'NONE', #19484, #5341, #16493, .T. ) ;
#8961=CARTESIAN_POINT ( 'NONE',  ( 0.000000000000000000, -84.90234713953981327, -5.175025661884713912 ) ) ;
#8963=VERTEX_POINT ( 'NONE', #911 ) ;
#8965=AXIS2_PLACEMENT_3D ( 'NONE', #7665, #3913, #14283 ) ;
#8967=CIRCLE ( 'NONE', #7913, 45.00000000000000000 ) ;
#8968=CARTESIAN_POINT ( 'NONE',  ( 10.00000000000000000, 84.33453774737672859, -11.08490790852044405 ) ) ;
#8970=DIRECTION ( 'NONE',  ( 0.000000000000000000, 0.5299192642332061221, -0.8480480961564251796 ) ) ;
#8971=ORIENTED_EDGE ( 'NONE', *, *, #20816, .F. ) ;
#8972=LINE ( 'NONE', #17285, #2924 ) ;
#8973=ORIENTED_EDGE ( 'NONE', *, *, #20850, .F. ) ;
#8975=DIRECTION ( 'NONE',  ( 0.000000000000000000, 0.000000000000000000, 1.000000000000000000 ) ) ;
#8977=CARTESIAN_POINT ( 'NONE',  ( 10.00000000000000000, 0.000000000000000000, 0.000000000000000000 ) ) ;
#8978=CARTESIAN_POINT ( 'NONE',  ( 0.000000000000000000, 91.49386717542239467, -13.61276130276895735 ) ) ;
#8979=AXIS2_PLACEMENT_3D ( 'NONE', #1752, #90, #18874 ) ;
#8980=CYLINDRICAL_SURFACE ( 'NONE', #220, 44.99999999999999289 ) ;
#8981=DIRECTION ( 'NONE',  ( 0.000000000000000000, 0.000000000000000000, 1.000000000000000000 ) ) ;
#8982=ADVANCED_FACE ( 'NONE', ( #16377 ), #6233, .F. ) ;
#8983=AXIS2_PLACEMENT_3D ( 'NONE', #16880, #2651, #18219 ) ;
#8984=DIRECTION ( 'NONE',  ( -1.000000000000000000, 0.000000000000000000, -0.000000000000000000 ) ) ;
#8987=VERTEX_POINT ( 'NONE', #12949 ) ;
#8988=CIRCLE ( 'NONE', #8296, 92.50100000000003320 ) ;
#8991=CARTESIAN_POINT ( 'NONE',  ( 10.00000000000000000, -75.45728100697571961, -39.26051685139143643 ) ) ;
#8994=VECTOR ( 'NONE', #17327, 1000.000000000000000 ) ;
#8995=CARTESIAN_POINT ( 'NONE',  ( 10.00000000000000000, -87.44637528609668209, 9.855528870798345054 ) ) ;
#8996=VERTEX_POINT ( 'NONE', #19696 ) ;
#8998=FILL_AREA_STYLE_COLOUR ( '', #16274 ) ;
#8999=AXIS2_PLACEMENT_3D ( 'NONE', #18050, #17942, #13064 ) ;
#9000=ORIENTED_EDGE ( 'NONE', *, *, #21625, .F. ) ;
#9008=DIRECTION ( 'NONE',  ( 0.000000000000000000, 0.8290375725550428454, -0.5591929034707450175 ) ) ;
#9011=CYLINDRICAL_SURFACE ( 'NONE', #17604, 44.99999999999999289 ) ;
#9015=ORIENTED_EDGE ( 'NONE', *, *, #12692, .F. ) ;
#9016=AXIS2_PLACEMENT_3D ( 'NONE', #11875, #5573, #12309 ) ;
#9019=DIRECTION ( 'NONE',  ( -1.000000000000000000, -0.000000000000000000, 0.000000000000000000 ) ) ;
#9021=FACE_OUTER_BOUND ( 'NONE', #9352, .T. ) ;
#9025=FACE_OUTER_BOUND ( 'NONE', #17411, .T. ) ;
#9027=EDGE_CURVE ( 'NONE', #12349, #17637, #6450, .T. ) ;
#9028=ORIENTED_EDGE ( 'NONE', *, *, #16658, .T. ) ;
#9029=AXIS2_PLACEMENT_3D ( 'NONE', #11718, #13377, #13475 ) ;
#9030=ORIENTED_EDGE ( 'NONE', *, *, #1044, .F. ) ;
#9031=FACE_OUTER_BOUND ( 'NONE', #10967, .T. ) ;
#9032=CIRCLE ( 'NONE', #8681, 44.99999999999999289 ) ;
#9033=ORIENTED_EDGE ( 'NONE', *, *, #18509, .F. ) ;
#9034=AXIS2_PLACEMENT_3D ( 'NONE', #9797, #4843, #8487 ) ;
#9037=LINE ( 'NONE', #17122, #19149 ) ;
#9038=DIRECTION ( 'NONE',  ( 1.000000000000000000, -0.000000000000000000, 0.000000000000000000 ) ) ;
#9039=EDGE_CURVE ( 'NONE', #14663, #2607, #1458, .T. ) ;
#9042=DIRECTION ( 'NONE',  ( -1.000000000000000000, -0.000000000000000000, 0.000000000000000000 ) ) ;
#9043=DIRECTION ( 'NONE',  ( 0.000000000000000000, 0.000000000000000000, 1.000000000000000000 ) ) ;
#9044=EDGE_CURVE ( 'NONE', #14874, #19013, #14936, .T. ) ;
#9045=DIRECTION ( 'NONE',  ( -1.000000000000000000, 0.000000000000000000, -0.000000000000000000 ) ) ;
#9046=DIRECTION ( 'NONE',  ( 0.000000000000000000, 0.000000000000000000, 1.000000000000000000 ) ) ;
#9048=CIRCLE ( 'NONE', #9384, 44.99999999999999289 ) ;
#9051=ORIENTED_EDGE ( 'NONE', *, *, #10970, .F. ) ;
#9052=ORIENTED_EDGE ( 'NONE', *, *, #5250, .F. ) ;
#9055=CARTESIAN_POINT ( 'NONE',  ( 10.00000000000000000, -76.53853822674008711, 43.42639941457088781 ) ) ;
#9057=ORIENTED_EDGE ( 'NONE', *, *, #992, .T. ) ;
#9058=ORIENTED_EDGE ( 'NONE', *, *, #595, .F. ) ;
#9062=AXIS2_PLACEMENT_3D ( 'NONE', #17430, #3736, #1857 ) ;
#9065=FACE_OUTER_BOUND ( 'NONE', #15364, .T. ) ;
#9066=LINE ( 'NONE', #5438, #13946 ) ;
#9067=DIRECTION ( 'NONE',  ( 0.000000000000000000, 0.000000000000000000, 1.000000000000000000 ) ) ;
#9068=CARTESIAN_POINT ( 'NONE',  ( 0.000000000000000000, 0.000000000000000000, 0.000000000000000000 ) ) ;
#9071=CARTESIAN_POINT ( 'NONE',  ( 10.00000000000000000, 29.47587714451039531, 82.91666097089130005 ) ) ;
#9072=EDGE_CURVE ( 'NONE', #2087, #10036, #19581, .T. ) ;
#9073=EDGE_LOOP ( 'NONE', ( #371, #5757, #20440, #20178 ) ) ;
#9074=DIRECTION ( 'NONE',  ( -1.000000000000000000, -0.000000000000000000, -0.000000000000000000 ) ) ;
#9075=AXIS2_PLACEMENT_3D ( 'NONE', #17569, #19111, #2422 ) ;
#9079=VECTOR ( 'NONE', #9442, 1000.000000000000000 ) ;
#9083=DIRECTION ( 'NONE',  ( -1.000000000000000000, 0.000000000000000000, 0.000000000000000000 ) ) ;
#9084=ADVANCED_FACE ( 'NONE', ( #5516 ), #540, .F. ) ;
#9085=ORIENTED_EDGE ( 'NONE', *, *, #14904, .F. ) ;
#9087=DIRECTION ( 'NONE',  ( 0.000000000000000000, 0.7431448254773909134, 0.6691306063588619013 ) ) ;
#9089=ORIENTED_EDGE ( 'NONE', *, *, #13237, .F. ) ;
#9090=ADVANCED_FACE ( 'NONE', ( #9955 ), #4781, .F. ) ;
#9092=EDGE_CURVE ( 'NONE', #7542, #6615, #7584, .T. ) ;
#9093=AXIS2_PLACEMENT_3D ( 'NONE', #16598, #20243, #5106 ) ;
#9096=LINE ( 'NONE', #4457, #7000 ) ;
#9097=CIRCLE ( 'NONE', #12284, 44.99999999999999289 ) ;
#9099=CIRCLE ( 'NONE', #17925, 44.99999999999999289 ) ;
#9102=LINE ( 'NONE', #6244, #13245 ) ;
#9103=CARTESIAN_POINT ( 'NONE',  ( 10.00000000000000000, 89.12061559554334167, 24.77803214283572686 ) ) ;
#9105=CARTESIAN_POINT ( 'NONE',  ( 5.000000000000000000, 52.25832601289194201, -70.80301803122729609 ) ) ;
#9106=ORIENTED_EDGE ( 'NONE', *, *, #10253, .F. ) ;
#9107=LINE ( 'NONE', #12637, #14019 ) ;
#9108=VERTEX_POINT ( 'NONE', #18999 ) ;
#9110=DIRECTION ( 'NONE',  ( -1.000000000000000000, -0.000000000000000000, -0.000000000000000000 ) ) ;
#9113=DIRECTION ( 'NONE',  ( 0.000000000000000000, 0.000000000000000000, 1.000000000000000000 ) ) ;
#9114=CIRCLE ( 'NONE', #3478, 88.00000000000000000 ) ;
#9115=VERTEX_POINT ( 'NONE', #20142 ) ;
#9121=ORIENTED_EDGE ( 'NONE', *, *, #2878, .T. ) ;
#9124=DIRECTION ( 'NONE',  ( -1.000000000000000000, -0.000000000000000000, -0.000000000000000000 ) ) ;
#9125=DIRECTION ( 'NONE',  ( 1.000000000000000000, 0.000000000000000000, 0.000000000000000000 ) ) ;
#9126=DIRECTION ( 'NONE',  ( 0.000000000000000000, 0.000000000000000000, 1.000000000000000000 ) ) ;
#9128=AXIS2_PLACEMENT_3D ( 'NONE', #964, #10907, #21188 ) ;
#9129=ORIENTED_EDGE ( 'NONE', *, *, #10002, .T. ) ;
#9132=CARTESIAN_POINT ( 'NONE',  ( 0.000000000000000000, 0.000000000000000000, 0.000000000000000000 ) ) ;
#9134=EDGE_LOOP ( 'NONE', ( #20138, #13028, #1883, #7225 ) ) ;
#9135=ORIENTED_EDGE ( 'NONE', *, *, #14796, .F. ) ;
#9138=AXIS2_PLACEMENT_3D ( 'NONE', #1955, #21030, #18652 ) ;
#9139=ORIENTED_EDGE ( 'NONE', *, *, #13124, .F. ) ;
#9141=ORIENTED_EDGE ( 'NONE', *, *, #15686, .T. ) ;
#9142=AXIS2_PLACEMENT_3D ( 'NONE', #5590, #502, #13766 ) ;
#9143=LINE ( 'NONE', #16105, #15377 ) ;
#9144=CIRCLE ( 'NONE', #4567, 88.00000000000000000 ) ;
#9148=DIRECTION ( 'NONE',  ( -1.000000000000000000, -0.000000000000000000, 0.000000000000000000 ) ) ;
#9151=CARTESIAN_POINT ( 'NONE',  ( 10.00000000000000000, 56.34908017029559346, 63.71789861856471049 ) ) ;
#9152=LINE ( 'NONE', #15899, #3432 ) ;
#9154=CARTESIAN_POINT ( 'NONE',  ( 0.000000000000000000, 84.12297548659704205, 12.59025161327141618 ) ) ;
#9157=CARTESIAN_POINT ( 'NONE',  ( 10.00000000000000000, 0.000000000000000000, 0.000000000000000000 ) ) ;
#9158=ORIENTED_EDGE ( 'NONE', *, *, #19905, .T. ) ;
#9159=ORIENTED_EDGE ( 'NONE', *, *, #21494, .T. ) ;
#9161=ORIENTED_EDGE ( 'NONE', *, *, #2940, .T. ) ;
#9163=EDGE_CURVE ( 'NONE', #15191, #4590, #193, .T. ) ;
#9164=VERTEX_POINT ( 'NONE', #10594 ) ;
#9165=FACE_OUTER_BOUND ( 'NONE', #13656, .T. ) ;
#9166=ORIENTED_EDGE ( 'NONE', *, *, #3982, .T. ) ;
#9167=VECTOR ( 'NONE', #17167, 1000.000000000000000 ) ;
#9168=CARTESIAN_POINT ( 'NONE',  ( 10.00000000000000000, 0.000000000000000000, 0.000000000000000000 ) ) ;
#9169=CARTESIAN_POINT ( 'NONE',  ( 10.00000000000000000, 0.000000000000000000, 0.000000000000000000 ) ) ;
#9173=CARTESIAN_POINT ( 'NONE',  ( 10.00000000000000000, 0.000000000000000000, 0.000000000000000000 ) ) ;
#9174=DIRECTION ( 'NONE',  ( 0.000000000000000000, 0.000000000000000000, 1.000000000000000000 ) ) ;
#9175=EDGE_CURVE ( 'NONE', #16026, #5950, #14647, .T. ) ;
#9176=CARTESIAN_POINT ( 'NONE',  ( 10.00000000000000000, -78.83848282823873888, -48.38314403117582430 ) ) ;
#9177=VERTEX_POINT ( 'NONE', #15565 ) ;
#9178=EDGE_CURVE ( 'NONE', #8545, #17704, #12246, .T. ) ;
#9181=LINE ( 'NONE', #9393, #21813 ) ;
#9182=DIRECTION ( 'NONE',  ( -1.000000000000000000, -0.000000000000000000, -0.000000000000000000 ) ) ;
#9183=EDGE_CURVE ( 'NONE', #16361, #7513, #17449, .T. ) ;
#9184=ORIENTED_EDGE ( 'NONE', *, *, #9072, .F. ) ;
#9185=ADVANCED_FACE ( 'NONE', ( #11141 ), #860, .F. ) ;
#9186=CARTESIAN_POINT ( 'NONE',  ( 10.00000000000000000, 79.66702613806774025, -29.80527447819464371 ) ) ;
#9188=CARTESIAN_POINT ( 'NONE',  ( 10.00000000000000000, 60.65655256511237781, 59.63197188857542841 ) ) ;
#9189=EDGE_CURVE ( 'NONE', #5362, #11867, #1243, .T. ) ;
#9190=CIRCLE ( 'NONE', #3563, 44.99999999999999289 ) ;
#9191=ORIENTED_EDGE ( 'NONE', *, *, #5166, .T. ) ;
#9194=DIRECTION ( 'NONE',  ( 1.000000000000000000, 0.000000000000000000, 0.000000000000000000 ) ) ;
#9198=MECHANICAL_DESIGN_GEOMETRIC_PRESENTATION_REPRESENTATION('',(#11697),#13085);
#9199=LINE ( 'NONE', #5791, #19550 ) ;
#9200=DIRECTION ( 'NONE',  ( -1.000000000000000000, 0.000000000000000000, 0.000000000000000000 ) ) ;
#9201=CARTESIAN_POINT ( 'NONE',  ( 10.00000000000000000, -91.70173545986527586, 12.13370160540012499 ) ) ;
#9203=DIRECTION ( 'NONE',  ( 0.000000000000000000, 0.000000000000000000, 1.000000000000000000 ) ) ;
#9204=ORIENTED_EDGE ( 'NONE', *, *, #12799, .T. ) ;
#9206=DIRECTION ( 'NONE',  ( 0.000000000000000000, 0.000000000000000000, 1.000000000000000000 ) ) ;
#9207=ORIENTED_EDGE ( 'NONE', *, *, #3313, .T. ) ;
#9210=ORIENTED_EDGE ( 'NONE', *, *, #15270, .T. ) ;
#9212=VECTOR ( 'NONE', #17071, 1000.000000000000000 ) ;
#9213=DIRECTION ( 'NONE',  ( 0.000000000000000000, 0.000000000000000000, 1.000000000000000000 ) ) ;
#9214=ORIENTED_EDGE ( 'NONE', *, *, #20032, .F. ) ;
#9217=ORIENTED_EDGE ( 'NONE', *, *, #9281, .T. ) ;
#9218=ORIENTED_EDGE ( 'NONE', *, *, #9437, .T. ) ;
#9223=CYLINDRICAL_SURFACE ( 'NONE', #3461, 44.99999999999998579 ) ;
#9227=EDGE_LOOP ( 'NONE', ( #20929, #10006, #3600, #22 ) ) ;
#9229=DIRECTION ( 'NONE',  ( -1.000000000000000000, -0.000000000000000000, -0.000000000000000000 ) ) ;
#9233=VECTOR ( 'NONE', #14692, 1000.000000000000000 ) ;
#9235=ORIENTED_EDGE ( 'NONE', *, *, #17055, .F. ) ;
#9237=ORIENTED_EDGE ( 'NONE', *, *, #4169, .T. ) ;
#9238=ORIENTED_EDGE ( 'NONE', *, *, #14210, .T. ) ;
#9239=ORIENTED_EDGE ( 'NONE', *, *, #6546, .T. ) ;
#9240=DIRECTION ( 'NONE',  ( 1.000000000000000000, 0.000000000000000000, 0.000000000000000000 ) ) ;
#9246=CIRCLE ( 'NONE', #2212, 45.00000000000000000 ) ;
#9248=CARTESIAN_POINT ( 'NONE',  ( 10.00000000000000000, 78.04699792498210797, -49.64978465107211747 ) ) ;
#9249=DIRECTION ( 'NONE',  ( 1.000000000000000000, 0.000000000000000000, 0.000000000000000000 ) ) ;
#9250=AXIS2_PLACEMENT_3D ( 'NONE', #21418, #13022, #19766 ) ;
#9251=DIRECTION ( 'NONE',  ( 1.000000000000000000, -0.000000000000000000, -0.000000000000000000 ) ) ;
#9252=DIRECTION ( 'NONE',  ( 1.000000000000000000, 0.000000000000000000, 0.000000000000000000 ) ) ;
#9253=CARTESIAN_POINT ( 'NONE',  ( 10.00000000000000000, -56.34908017029602689, 63.71789861856433390 ) ) ;
#9255=CIRCLE ( 'NONE', #8216, 44.99999999999998579 ) ;
#9256=VERTEX_POINT ( 'NONE', #19103 ) ;
#9259=AXIS2_PLACEMENT_3D ( 'NONE', #2195, #12250, #10372 ) ;
#9260=VECTOR ( 'NONE', #4956, 1000.000000000000000 ) ;
#9261=ORIENTED_EDGE ( 'NONE', *, *, #16892, .F. ) ;
#9266=CARTESIAN_POINT ( 'NONE',  ( 10.00000000000000000, -33.95793648385871677, 86.04239391577979745 ) ) ;
#9267=CARTESIAN_POINT ( 'NONE',  ( 0.000000000000000000, -72.53479564998815476, 44.42851404693331574 ) ) ;
#9268=CARTESIAN_POINT ( 'NONE',  ( 10.00000000000000000, -41.21966518006011881, 82.80926399530274296 ) ) ;
#9270=DIRECTION ( 'NONE',  ( 0.000000000000000000, 0.06975647374412546897, -0.9975640502598241977 ) ) ;
#9271=DIRECTION ( 'NONE',  ( 0.000000000000000000, -0.1391731009600725433, 0.9902680687415692518 ) ) ;
#9272=CYLINDRICAL_SURFACE ( 'NONE', #1996, 45.00000000000000000 ) ;
#9273=FACE_OUTER_BOUND ( 'NONE', #1156, .T. ) ;
#9274=CARTESIAN_POINT ( 'NONE',  ( 10.00000000000000000, 81.32027326007866463, 44.08455690949082850 ) ) ;
#9275=CARTESIAN_POINT ( 'NONE',  ( 10.00000000000000000, -68.36541360927154187, -50.60987712331774446 ) ) ;
#9276=AXIS2_PLACEMENT_3D ( 'NONE', #18414, #3259, #20065 ) ;
#9277=EDGE_CURVE ( 'NONE', #16302, #20772, #17557, .T. ) ;
#9278=ORIENTED_EDGE ( 'NONE', *, *, #14531, .F. ) ;
#9279=CIRCLE ( 'NONE', #16708, 88.00000000000000000 ) ;
#9280=DIRECTION ( 'NONE',  ( 1.000000000000000000, 0.000000000000000000, 0.000000000000000000 ) ) ;
#9281=EDGE_CURVE ( 'NONE', #14246, #12590, #8988, .T. ) ;
#9282=DIRECTION ( 'NONE',  ( 0.000000000000000000, 0.000000000000000000, 1.000000000000000000 ) ) ;
#9283=FACE_OUTER_BOUND ( 'NONE', #2241, .T. ) ;
#9286=DIRECTION ( 'NONE',  ( -1.000000000000000000, -0.000000000000000000, 0.000000000000000000 ) ) ;
#9288=ORIENTED_EDGE ( 'NONE', *, *, #12198, .T. ) ;
#9292=CYLINDRICAL_SURFACE ( 'NONE', #11411, 92.50100000000000477 ) ;
#9293=ORIENTED_EDGE ( 'NONE', *, *, #11060, .F. ) ;
#9294=EDGE_LOOP ( 'NONE', ( #10198, #2821, #6524, #21562 ) ) ;
#9298=CARTESIAN_POINT ( 'NONE',  ( 5.000000000000000000, 85.22372865846293166, 21.92979875759657560 ) ) ;
#9299=DIRECTION ( 'NONE',  ( -1.000000000000000000, -0.000000000000000000, -0.000000000000000000 ) ) ;
#9300=DIRECTION ( 'NONE',  ( 1.000000000000000000, 0.000000000000000000, 0.000000000000000000 ) ) ;
#9301=LINE ( 'NONE', #2474, #13924 ) ;
#9302=CYLINDRICAL_SURFACE ( 'NONE', #17405, 45.00000000000000000 ) ;
#9304=DIRECTION ( 'NONE',  ( -1.000000000000000000, -0.000000000000000000, -0.000000000000000000 ) ) ;
#9305=AXIS2_PLACEMENT_3D ( 'NONE', #19479, #17394, #19379 ) ;
#9306=EDGE_CURVE ( 'NONE', #17849, #14874, #19927, .T. ) ;
#9307=EDGE_CURVE ( 'NONE', #16742, #20271, #2744, .T. ) ;
#9308=EDGE_CURVE ( 'NONE', #9851, #12482, #6543, .T. ) ;
#9309=VERTEX_POINT ( 'NONE', #9358 ) ;
#9312=EDGE_CURVE ( 'NONE', #13478, #14138, #10917, .T. ) ;
#9313=ORIENTED_EDGE ( 'NONE', *, *, #12404, .F. ) ;
#9314=CIRCLE ( 'NONE', #2275, 88.00000000000000000 ) ;
#9320=EDGE_CURVE ( 'NONE', #16026, #13465, #15992, .T. ) ;
#9321=AXIS2_PLACEMENT_3D ( 'NONE', #4343, #12739, #2358 ) ;
#9323=VERTEX_POINT ( 'NONE', #2627 ) ;
#9324=CIRCLE ( 'NONE', #16748, 88.00000000000000000 ) ;
#9326=DIRECTION ( 'NONE',  ( 0.000000000000000000, 0.5877852522924740253, -0.8090169943749466741 ) ) ;
#9328=ORIENTED_EDGE ( 'NONE', *, *, #14624, .T. ) ;
#9330=VECTOR ( 'NONE', #17718, 1000.000000000000000 ) ;
#9331=DIRECTION ( 'NONE',  ( 1.000000000000000000, 0.000000000000000000, 0.000000000000000000 ) ) ;
#9334=CARTESIAN_POINT ( 'NONE',  ( 0.000000000000000000, -87.17509410653646285, 30.93441398372555540 ) ) ;
#9337=EDGE_LOOP ( 'NONE', ( #608, #19925, #12243, #2705 ) ) ;
#9338=CARTESIAN_POINT ( 'NONE',  ( 10.00000000000000000, 9.646732466565339337, 84.51112348751853176 ) ) ;
#9339=EDGE_CURVE ( 'NONE', #2427, #4091, #6897, .T. ) ;
#9342=CARTESIAN_POINT ( 'NONE',  ( 10.00000000000000000, -69.25892805976543798, 49.38005998797819274 ) ) ;
#9343=AXIS2_PLACEMENT_3D ( 'NONE', #5110, #20144, #246 ) ;
#9346=ORIENTED_EDGE ( 'NONE', *, *, #12564, .T. ) ;
#9347=DIRECTION ( 'NONE',  ( -1.000000000000000000, 0.000000000000000000, 0.000000000000000000 ) ) ;
#9349=VERTEX_POINT ( 'NONE', #19761 ) ;
#9351=ORIENTED_EDGE ( 'NONE', *, *, #8792, .F. ) ;
#9352=EDGE_LOOP ( 'NONE', ( #18042, #8343, #17061, #13898 ) ) ;
#9353=CIRCLE ( 'NONE', #3964, 92.50100000000003320 ) ;
#9356=ORIENTED_EDGE ( 'NONE', *, *, #10171, .F. ) ;
#9357=DIRECTION ( 'NONE',  ( 1.000000000000000000, 0.000000000000000000, 0.000000000000000000 ) ) ;
#9358=CARTESIAN_POINT ( 'NONE',  ( 0.000000000000000000, 87.44637528609675314, -9.855528870797693131 ) ) ;
#9360=AXIS2_PLACEMENT_3D ( 'NONE', #11884, #1829, #15299 ) ;
#9361=EDGE_CURVE ( 'NONE', #17526, #1297, #9692, .T. ) ;
#9362=AXIS2_PLACEMENT_3D ( 'NONE', #15722, #5778, #7536 ) ;
#9367=DIRECTION ( 'NONE',  ( -1.000000000000000000, 0.000000000000000000, -0.000000000000000000 ) ) ;
#9369=DIRECTION ( 'NONE',  ( 0.000000000000000000, 0.8290375725550390706, 0.5591929034707506796 ) ) ;
#9370=DIRECTION ( 'NONE',  ( 0.000000000000000000, 0.9510565162951523099, 0.3090169943749513926 ) ) ;
#9371=VERTEX_POINT ( 'NONE', #14557 ) ;
#9372=ORIENTED_EDGE ( 'NONE', *, *, #5184, .T. ) ;
#9373=EDGE_LOOP ( 'NONE', ( #20303, #17545, #8427, #16921 ) ) ;
#9377=DIRECTION ( 'NONE',  ( -1.000000000000000000, -0.000000000000000000, -0.000000000000000000 ) ) ;
#9378=EDGE_LOOP ( 'NONE', ( #9660, #12898, #323, #6232 ) ) ;
#9379=DIRECTION ( 'NONE',  ( 1.000000000000000000, 0.000000000000000000, 0.000000000000000000 ) ) ;
#9380=CARTESIAN_POINT ( 'NONE',  ( 0.000000000000000000, 0.000000000000000000, 0.000000000000000000 ) ) ;
#9382=CARTESIAN_POINT ( 'NONE',  ( 0.000000000000000000, 0.000000000000000000, 0.000000000000000000 ) ) ;
#9383=LINE ( 'NONE', #19451, #18651 ) ;
#9384=AXIS2_PLACEMENT_3D ( 'NONE', #9923, #8909, #17329 ) ;
#9385=CARTESIAN_POINT ( 'NONE',  ( 0.000000000000000000, 80.18694381077108346, 28.37681241246682973 ) ) ;
#9388=CARTESIAN_POINT ( 'NONE',  ( 10.00000000000000000, 0.000000000000000000, 0.000000000000000000 ) ) ;
#9390=EDGE_LOOP ( 'NONE', ( #20324, #1132, #21296, #17698 ) ) ;
#9391=CARTESIAN_POINT ( 'NONE',  ( 5.000000000000000000, 69.74988376404020585, 53.65588238863360715 ) ) ;
#9393=CARTESIAN_POINT ( 'NONE',  ( 10.00000000000000000, 91.70173545986537533, -12.13370160539944287 ) ) ;
#9394=CARTESIAN_POINT ( 'NONE',  ( 0.000000000000000000, 0.000000000000000000, 0.000000000000000000 ) ) ;
#9395=VERTEX_POINT ( 'NONE', #8263 ) ;
#9396=DIRECTION ( 'NONE',  ( 0.000000000000000000, 0.000000000000000000, 1.000000000000000000 ) ) ;
#9397=VERTEX_POINT ( 'NONE', #19859 ) ;
#9398=ORIENTED_EDGE ( 'NONE', *, *, #3131, .F. ) ;
#9401=DIRECTION ( 'NONE',  ( -1.000000000000000000, 0.000000000000000000, 0.000000000000000000 ) ) ;
#9404=ORIENTED_EDGE ( 'NONE', *, *, #16868, .F. ) ;
#9408=DIRECTION ( 'NONE',  ( 0.000000000000000000, 0.6946583704589935904, 0.7193398003386546335 ) ) ;
#9410=CARTESIAN_POINT ( 'NONE',  ( 10.00000000000000000, 60.65655256511316651, -59.63197188857461128 ) ) ;
#9413=CARTESIAN_POINT ( 'NONE',  ( 5.000000000000002665, 18.94217447942559573, 85.93715160505956874 ) ) ;
#9414=CARTESIAN_POINT ( 'NONE',  ( 10.00000000000000000, 0.000000000000000000, 0.000000000000000000 ) ) ;
#9416=AXIS2_PLACEMENT_3D ( 'NONE', #10554, #68, #20722 ) ;
#9418=CIRCLE ( 'NONE', #12610, 44.99999999999999289 ) ;
#9419=DIRECTION ( 'NONE',  ( -1.000000000000000000, 0.000000000000000000, 0.000000000000000000 ) ) ;
#9421=CYLINDRICAL_SURFACE ( 'NONE', #4502, 44.99999999999999289 ) ;
#9424=VERTEX_POINT ( 'NONE', #12900 ) ;
#9426=ORIENTED_EDGE ( 'NONE', *, *, #8271, .F. ) ;
#9427=ORIENTED_EDGE ( 'NONE', *, *, #8381, .T. ) ;
#9429=AXIS2_PLACEMENT_3D ( 'NONE', #5158, #10327, #13542 ) ;
#9430=EDGE_CURVE ( 'NONE', #12184, #8096, #4515, .T. ) ;
#9432=CIRCLE ( 'NONE', #15804, 44.99999999999998579 ) ;
#9434=CARTESIAN_POINT ( 'NONE',  ( 10.00000000000000000, -9.646732466564730046, -84.51112348751858860 ) ) ;
#9436=ORIENTED_EDGE ( 'NONE', *, *, #1086, .F. ) ;
#9437=EDGE_CURVE ( 'NONE', #2378, #16156, #4775, .T. ) ;
#9438=CARTESIAN_POINT ( 'NONE',  ( 10.00000000000000000, -29.47587714450981622, -82.91666097089152743 ) ) ;
#9439=CYLINDRICAL_SURFACE ( 'NONE', #293, 88.00000000000000000 ) ;
#9441=DIRECTION ( 'NONE',  ( 1.000000000000000000, 0.000000000000000000, 0.000000000000000000 ) ) ;
#9442=DIRECTION ( 'NONE',  ( -1.000000000000000000, -0.000000000000000000, 0.000000000000000000 ) ) ;
#9443=VERTEX_POINT ( 'NONE', #11250 ) ;
#9444=CARTESIAN_POINT ( 'NONE',  ( 0.000000000000000000, 27.87320266523557777, 88.20158487341770126 ) ) ;
#9445=ADVANCED_FACE ( 'NONE', ( #16322 ), #10016, .F. ) ;
#9446=CIRCLE ( 'NONE', #16164, 92.50100000000000477 ) ;
#9448=CARTESIAN_POINT ( 'NONE',  ( 10.00000000000000000, 35.34277389771534672, 85.48288328206398035 ) ) ;
#9449=AXIS2_PLACEMENT_3D ( 'NONE', #4223, #14157, #9282 ) ;
#9451=CIRCLE ( 'NONE', #3128, 44.99999999999999289 ) ;
#9453=DIRECTION ( 'NONE',  ( 0.000000000000000000, 0.9993908270190958731, -0.03489949670249761771 ) ) ;
#9454=ORIENTED_EDGE ( 'NONE', *, *, #2702, .T. ) ;
#9462=EDGE_CURVE ( 'NONE', #1449, #18403, #14291, .T. ) ;
#9463=DIRECTION ( 'NONE',  ( 1.000000000000000000, 0.000000000000000000, 0.000000000000000000 ) ) ;
#9466=AXIS2_PLACEMENT_3D ( 'NONE', #20760, #5198, #17007 ) ;
#9467=EDGE_CURVE ( 'NONE', #3479, #17932, #8160, .T. ) ;
#9468=DIRECTION ( 'NONE',  ( 0.000000000000000000, 0.000000000000000000, 1.000000000000000000 ) ) ;
#9469=CARTESIAN_POINT ( 'NONE',  ( 10.00000000000000000, 6.797690662956386021, -87.73705831432209834 ) ) ;
#9470=AXIS2_PLACEMENT_3D ( 'NONE', #12029, #3624, #10357 ) ;
#9473=AXIS2_PLACEMENT_3D ( 'NONE', #5206, #15350, #3543 ) ;
#9475=DIRECTION ( 'NONE',  ( 1.000000000000000000, 0.000000000000000000, 0.000000000000000000 ) ) ;
#9476=DIRECTION ( 'NONE',  ( 0.000000000000000000, -0.6427876096865300370, -0.7660444431189857850 ) ) ;
#9477=DIRECTION ( 'NONE',  ( 1.000000000000000000, 0.000000000000000000, 0.000000000000000000 ) ) ;
#9479=EDGE_CURVE ( 'NONE', #8452, #6908, #15348, .T. ) ;
#9480=EDGE_CURVE ( 'NONE', #16476, #21544, #7600, .T. ) ;
#9481=CARTESIAN_POINT ( 'NONE',  ( -10.00000000000000000, 0.000000000000000000, 0.000000000000000000 ) ) ;
#9482=AXIS2_PLACEMENT_3D ( 'NONE', #15100, #13115, #16654 ) ;
#9484=AXIS2_PLACEMENT_3D ( 'NONE', #14660, #13002, #12562 ) ;
#9485=ORIENTED_EDGE ( 'NONE', *, *, #6527, .T. ) ;
#9486=EDGE_CURVE ( 'NONE', #13543, #15275, #19948, .T. ) ;
#9487=AXIS2_PLACEMENT_3D ( 'NONE', #841, #3845, #10579 ) ;
#9490=ORIENTED_EDGE ( 'NONE', *, *, #19998, .F. ) ;
#9494=ORIENTED_EDGE ( 'NONE', *, *, #1993, .F. ) ;
#9496=DIRECTION ( 'NONE',  ( 0.000000000000000000, -0.2079116908177468248, -0.9781476007338083534 ) ) ;
#9497=CIRCLE ( 'NONE', #20804, 88.00000000000000000 ) ;
#9499=CARTESIAN_POINT ( 'NONE',  ( 5.000000000000002665, -35.18804927320473297, -80.65854690202716881 ) ) ;
#9500=FACE_OUTER_BOUND ( 'NONE', #6968, .T. ) ;
#9501=AXIS2_PLACEMENT_3D ( 'NONE', #19040, #7333, #18721 ) ;
#9502=AXIS2_PLACEMENT_3D ( 'NONE', #21398, #16091, #11230 ) ;
#9503=CARTESIAN_POINT ( 'NONE',  ( 10.00000000000000000, -84.19736439813780748, -38.30455363801015523 ) ) ;
#9504=DIRECTION ( 'NONE',  ( -1.000000000000000000, -0.000000000000000000, -0.000000000000000000 ) ) ;
#9506=ORIENTED_EDGE ( 'NONE', *, *, #15582, .T. ) ;
#9507=CARTESIAN_POINT ( 'NONE',  ( 10.00000000000000000, -56.34908017029602689, 63.71789861856433390 ) ) ;
#9508=EDGE_LOOP ( 'NONE', ( #15360, #6794, #9551, #17548 ) ) ;
#9509=EDGE_CURVE ( 'NONE', #5155, #18369, #10409, .T. ) ;
#9510=CYLINDRICAL_SURFACE ( 'NONE', #5245, 44.99999999999999289 ) ;
#9511=DIRECTION ( 'NONE',  ( -1.000000000000000000, -0.000000000000000000, -0.000000000000000000 ) ) ;
#9513=CIRCLE ( 'NONE', #14467, 44.99999999999999289 ) ;
#9514=DIRECTION ( 'NONE',  ( -1.000000000000000000, -0.000000000000000000, -0.000000000000000000 ) ) ;
#9518=DIRECTION ( 'NONE',  ( 0.000000000000000000, 0.000000000000000000, 1.000000000000000000 ) ) ;
#9519=EDGE_LOOP ( 'NONE', ( #4368, #18235, #529, #1735 ) ) ;
#9520=VERTEX_POINT ( 'NONE', #13557 ) ;
#9521=CARTESIAN_POINT ( 'NONE',  ( 10.00000000000000000, -6.797690662955810481, 87.73705831432212676 ) ) ;
#9524=CARTESIAN_POINT ( 'NONE',  ( 10.00000000000000000, -52.34334029047821701, -76.26670130689538496 ) ) ;
#9525=DIRECTION ( 'NONE',  ( -1.000000000000000000, 0.000000000000000000, -0.000000000000000000 ) ) ;
#9527=CARTESIAN_POINT ( 'NONE',  ( 0.000000000000000000, -12.90135963484139658, 87.04915231966639055 ) ) ;
#9528=CARTESIAN_POINT ( 'NONE',  ( 10.00000000000000000, 0.000000000000000000, 0.000000000000000000 ) ) ;
#9530=EDGE_LOOP ( 'NONE', ( #9697, #17148, #19634, #18900 ) ) ;
#9532=ADVANCED_FACE ( 'NONE', ( #3606 ), #5379, .F. ) ;
#9534=CARTESIAN_POINT ( 'NONE',  ( 10.00000000000000000, -12.90135963484139658, 87.04915231966639055 ) ) ;
#9535=DIRECTION ( 'NONE',  ( 1.000000000000000000, 0.000000000000000000, 0.000000000000000000 ) ) ;
#9539=ORIENTED_EDGE ( 'NONE', *, *, #4618, .F. ) ;
#9540=ORIENTED_EDGE ( 'NONE', *, *, #8153, .F. ) ;
#9541=EDGE_LOOP ( 'NONE', ( #2365, #12757, #10661, #14975 ) ) ;
#9544=CARTESIAN_POINT ( 'NONE',  ( 0.000000000000000000, 0.000000000000000000, 0.000000000000000000 ) ) ;
#9545=ORIENTED_EDGE ( 'NONE', *, *, #2317, .T. ) ;
#9547=CARTESIAN_POINT ( 'NONE',  ( 10.00000000000000000, -70.37753541435978377, 60.02863908169610596 ) ) ;
#9548=CARTESIAN_POINT ( 'NONE',  ( 10.00000000000000000, -30.71797041605752554, -82.46457599186584275 ) ) ;
#9551=ORIENTED_EDGE ( 'NONE', *, *, #17320, .T. ) ;
#9552=CARTESIAN_POINT ( 'NONE',  ( 10.00000000000000000, 73.32282170386848463, 48.65967342042804944 ) ) ;
#9554=ADVANCED_FACE ( 'NONE', ( #196 ), #3508, .F. ) ;
#9558=CYLINDRICAL_SURFACE ( 'NONE', #11617, 88.00000000000000000 ) ;
#9559=FACE_OUTER_BOUND ( 'NONE', #9519, .T. ) ;
#9560=ORIENTED_EDGE ( 'NONE', *, *, #10813, .F. ) ;
#9562=VERTEX_POINT ( 'NONE', #5280 ) ;
#9563=VERTEX_POINT ( 'NONE', #8806 ) ;
#9565=EDGE_LOOP ( 'NONE', ( #398, #1497, #17657, #9586 ) ) ;
#9569=CARTESIAN_POINT ( 'NONE',  ( 10.00000000000000000, -52.25832601289145884, 70.80301803122767978 ) ) ;
#9572=CARTESIAN_POINT ( 'NONE',  ( 0.000000000000000000, 56.05743251323954013, -67.83483072893743326 ) ) ;
#9574=CARTESIAN_POINT ( 'NONE',  ( 10.00000000000000000, 41.87002153499110335, 74.04114219178059386 ) ) ;
#9576=EDGE_CURVE ( 'NONE', #1586, #8180, #10028, .T. ) ;
#9577=EDGE_CURVE ( 'NONE', #14952, #1865, #18653, .T. ) ;
#9579=CARTESIAN_POINT ( 'NONE',  ( 0.000000000000000000, -56.34908017029602689, 63.71789861856433390 ) ) ;
#9580=ORIENTED_EDGE ( 'NONE', *, *, #4026, .T. ) ;
#9581=EDGE_CURVE ( 'NONE', #10412, #19966, #6522, .T. ) ;
#9582=ORIENTED_EDGE ( 'NONE', *, *, #7342, .T. ) ;
#9583=ORIENTED_EDGE ( 'NONE', *, *, #4484, .T. ) ;
#9584=EDGE_CURVE ( 'NONE', #13159, #1625, #1956, .T. ) ;
#9585=AXIS2_PLACEMENT_3D ( 'NONE', #19026, #3660, #15591 ) ;
#9586=ORIENTED_EDGE ( 'NONE', *, *, #4967, .T. ) ;
#9587=ORIENTED_EDGE ( 'NONE', *, *, #21199, .F. ) ;
#9588=ADVANCED_FACE ( 'NONE', ( #305 ), #405, .F. ) ;
#9589=CYLINDRICAL_SURFACE ( 'NONE', #18313, 88.00000000000000000 ) ;
#9593=CARTESIAN_POINT ( 'NONE',  ( 0.000000000000000000, -85.22372865846278955, -21.92979875759713693 ) ) ;
#9595=DIRECTION ( 'NONE',  ( -1.000000000000000000, -0.000000000000000000, -0.000000000000000000 ) ) ;
#9598=EDGE_CURVE ( 'NONE', #6056, #13893, #16878, .T. ) ;
#9599=DIRECTION ( 'NONE',  ( 0.000000000000000000, 0.000000000000000000, -1.000000000000000000 ) ) ;
#9600=DIRECTION ( 'NONE',  ( -1.000000000000000000, -0.000000000000000000, -0.000000000000000000 ) ) ;
#9602=ORIENTED_EDGE ( 'NONE', *, *, #1666, .F. ) ;
#9605=ADVANCED_FACE ( 'NONE', ( #15543 ), #7143, .F. ) ;
#9607=CIRCLE ( 'NONE', #9982, 92.50100000000000477 ) ;
#9608=VERTEX_POINT ( 'NONE', #19079 ) ;
#9610=DIRECTION ( 'NONE',  ( 1.000000000000000000, 0.000000000000000000, 0.000000000000000000 ) ) ;
#9612=CARTESIAN_POINT ( 'NONE',  ( 10.00000000000000000, -75.27139873020921357, 53.76477968147791131 ) ) ;
#9613=ORIENTED_EDGE ( 'NONE', *, *, #17427, .F. ) ;
#9617=VECTOR ( 'NONE', #13019, 1000.000000000000000 ) ;
#9618=ORIENTED_EDGE ( 'NONE', *, *, #6548, .T. ) ;
#9621=EDGE_CURVE ( 'NONE', #14609, #18291, #3675, .T. ) ;
#9622=CARTESIAN_POINT ( 'NONE',  ( 10.00000000000000000, 85.05652083079336023, -0.7600687895862878740 ) ) ;
#9627=CARTESIAN_POINT ( 'NONE',  ( 0.000000000000000000, -61.33825423015729683, 69.23910433415923649 ) ) ;
#9628=EDGE_CURVE ( 'NONE', #15096, #10277, #14314, .T. ) ;
#9629=FACE_OUTER_BOUND ( 'NONE', #15937, .T. ) ;
#9630=AXIS2_PLACEMENT_3D ( 'NONE', #15638, #14196, #9326 ) ;
#9631=EDGE_CURVE ( 'NONE', #7099, #19664, #9659, .T. ) ;
#9633=CARTESIAN_POINT ( 'NONE',  ( 10.00000000000000000, -43.18649929580143976, -73.28107340219457910 ) ) ;
#9634=DIRECTION ( 'NONE',  ( -1.000000000000000000, -0.000000000000000000, -0.000000000000000000 ) ) ;
#9635=ORIENTED_EDGE ( 'NONE', *, *, #7613, .F. ) ;
#9638=DIRECTION ( 'NONE',  ( -1.000000000000000000, -0.000000000000000000, -0.000000000000000000 ) ) ;
#9639=AXIS2_PLACEMENT_3D ( 'NONE', #10295, #1901, #13730 ) ;
#9640=CARTESIAN_POINT ( 'NONE',  ( 0.000000000000000000, -3.974475837764314345, -92.41557521768193340 ) ) ;
#9641=DIRECTION ( 'NONE',  ( -1.000000000000000000, -0.000000000000000000, -0.000000000000000000 ) ) ;
#9643=ORIENTED_EDGE ( 'NONE', *, *, #16125, .F. ) ;
#9644=AXIS2_PLACEMENT_3D ( 'NONE', #9434, #16191, #1057 ) ;
#9645=EDGE_LOOP ( 'NONE', ( #5045, #1323, #5566, #1150 ) ) ;
#9646=EDGE_LOOP ( 'NONE', ( #7984, #15599, #9635, #11243 ) ) ;
#9649=CARTESIAN_POINT ( 'NONE',  ( 0.000000000000000000, 83.48638250753229784, 27.82128566055142826 ) ) ;
#9651=AXIS2_PLACEMENT_3D ( 'NONE', #7781, #20820, #19153 ) ;
#9653=LINE ( 'NONE', #6378, #7649 ) ;
#9654=CARTESIAN_POINT ( 'NONE',  ( 0.000000000000000000, 0.000000000000000000, 0.000000000000000000 ) ) ;
#9655=CARTESIAN_POINT ( 'NONE',  ( 0.000000000000000000, -64.95266917914277371, -59.37298010463037912 ) ) ;
#9656=DIRECTION ( 'NONE',  ( 0.000000000000000000, 0.000000000000000000, 1.000000000000000000 ) ) ;
#9657=CARTESIAN_POINT ( 'NONE',  ( 10.00000000000000000, 0.000000000000000000, 0.000000000000000000 ) ) ;
#9659=CIRCLE ( 'NONE', #511, 92.50100000000000477 ) ;
#9660=ORIENTED_EDGE ( 'NONE', *, *, #1052, .T. ) ;
#9663=FACE_OUTER_BOUND ( 'NONE', #10326, .T. ) ;
#9664=VERTEX_POINT ( 'NONE', #17417 ) ;
#9666=ORIENTED_EDGE ( 'NONE', *, *, #21107, .F. ) ;
#9667=VECTOR ( 'NONE', #17016, 1000.000000000000000 ) ;
#9670=CARTESIAN_POINT ( 'NONE',  ( 10.00000000000000000, -68.36541360927220978, 50.60987712331682076 ) ) ;
#9671=VERTEX_POINT ( 'NONE', #734 ) ;
#9673=AXIS2_PLACEMENT_3D ( 'NONE', #8133, #6479, #4812 ) ;
#9674=ORIENTED_EDGE ( 'NONE', *, *, #4468, .T. ) ;
#9676=CARTESIAN_POINT ( 'NONE',  ( 0.000000000000000000, -24.89070495400676819, -84.40647372620527733 ) ) ;
#9677=VECTOR ( 'NONE', #19049, 1000.000000000000000 ) ;
#9678=ORIENTED_EDGE ( 'NONE', *, *, #1624, .T. ) ;
#9681=CARTESIAN_POINT ( 'NONE',  ( 10.00000000000000000, 69.25892805976512534, 49.38005998797868301 ) ) ;
#9682=ADVANCED_FACE ( 'NONE', ( #7472 ), #12334, .F. ) ;
#9684=CIRCLE ( 'NONE', #181, 92.50100000000003320 ) ;
#9685=DIRECTION ( 'NONE',  ( 0.000000000000000000, 0.000000000000000000, 1.000000000000000000 ) ) ;
#9686=CARTESIAN_POINT ( 'NONE',  ( 10.00000000000000000, 0.000000000000000000, 0.000000000000000000 ) ) ;
#9687=EDGE_CURVE ( 'NONE', #453, #215, #2168, .T. ) ;
#9688=CIRCLE ( 'NONE', #6912, 44.99999999999999289 ) ;
#9690=DIRECTION ( 'NONE',  ( 0.000000000000000000, 0.000000000000000000, -1.000000000000000000 ) ) ;
#9692=CIRCLE ( 'NONE', #4758, 44.99999999999999289 ) ;
#9695=ORIENTED_EDGE ( 'NONE', *, *, #17755, .F. ) ;
#9696=VERTEX_POINT ( 'NONE', #14201 ) ;
#9697=ORIENTED_EDGE ( 'NONE', *, *, #3982, .F. ) ;
#9698=CIRCLE ( 'NONE', #12531, 44.99999999999999289 ) ;
#9699=AXIS2_PLACEMENT_3D ( 'NONE', #4801, #8010, #13077 ) ;
#9700=AXIS2_PLACEMENT_3D ( 'NONE', #15103, #21849, #6736 ) ;
#9702=CIRCLE ( 'NONE', #15361, 44.99999999999998579 ) ;
#9703=CARTESIAN_POINT ( 'NONE',  ( 10.00000000000000000, -77.39385041987173963, 35.28996114464576550 ) ) ;
#9706=EDGE_CURVE ( 'NONE', #5372, #18348, #20948, .T. ) ;
#9709=DIRECTION ( 'NONE',  ( -1.000000000000000000, -0.000000000000000000, -0.000000000000000000 ) ) ;
#9710=EDGE_CURVE ( 'NONE', #19677, #6016, #10999, .T. ) ;
#9711=CARTESIAN_POINT ( 'NONE',  ( 10.00000000000000000, 81.34229909304724515, -33.57723005635285318 ) ) ;
#9712=CARTESIAN_POINT ( 'NONE',  ( 10.00000000000000000, -32.56745702629687855, -78.57830605990686479 ) ) ;
#9713=CARTESIAN_POINT ( 'NONE',  ( 0.000000000000000000, 23.62010150527222052, 84.77081340225913664 ) ) ;
#9716=CYLINDRICAL_SURFACE ( 'NONE', #14056, 88.00000000000000000 ) ;
#9717=CIRCLE ( 'NONE', #17503, 92.50100000000000477 ) ;
#9718=ORIENTED_EDGE ( 'NONE', *, *, #3505, .T. ) ;
#9719=CIRCLE ( 'NONE', #4033, 92.50099999999999056 ) ;
#9720=AXIS2_PLACEMENT_3D ( 'NONE', #10749, #19378, #7346 ) ;
#9721=CARTESIAN_POINT ( 'NONE',  ( -10.00000000000000000, 0.000000000000000000, 0.000000000000000000 ) ) ;
#9724=VERTEX_POINT ( 'NONE', #4040 ) ;
#9727=DIRECTION ( 'NONE',  ( 0.000000000000000000, 0.000000000000000000, 1.000000000000000000 ) ) ;
#9729=DIRECTION ( 'NONE',  ( 1.000000000000000000, 0.000000000000000000, 0.000000000000000000 ) ) ;
#9730=ORIENTED_EDGE ( 'NONE', *, *, #12972, .F. ) ;
#9731=VERTEX_POINT ( 'NONE', #10889 ) ;
#9734=VERTEX_POINT ( 'NONE', #19180 ) ;
#9737=CIRCLE ( 'NONE', #11864, 45.00000000000000000 ) ;
#9742=CARTESIAN_POINT ( 'NONE',  ( 10.00000000000000000, 0.000000000000000000, 0.000000000000000000 ) ) ;
#9743=CARTESIAN_POINT ( 'NONE',  ( 0.000000000000000000, 75.45728100697598961, 39.26051685139091063 ) ) ;
#9744=FACE_OUTER_BOUND ( 'NONE', #3760, .T. ) ;
#9746=CARTESIAN_POINT ( 'NONE',  ( 10.00000000000000000, 52.96496548042942010, -66.55750800669305534 ) ) ;
#9749=EDGE_CURVE ( 'NONE', #20733, #19144, #5602, .T. ) ;
#9753=AXIS2_PLACEMENT_3D ( 'NONE', #21554, #19891, #7963 ) ;
#9754=DIRECTION ( 'NONE',  ( -1.000000000000000000, 0.000000000000000000, 0.000000000000000000 ) ) ;
#9755=DIRECTION ( 'NONE',  ( 0.000000000000000000, 0.7880107536067233465, -0.6156614753256567374 ) ) ;
#9756=ORIENTED_EDGE ( 'NONE', *, *, #9621, .T. ) ;
#9757=EDGE_CURVE ( 'NONE', #13772, #7164, #17440, .T. ) ;
#9758=CARTESIAN_POINT ( 'NONE',  ( 0.000000000000000000, 92.22057093985031884, 7.197311757040840696 ) ) ;
#9760=EDGE_CURVE ( 'NONE', #879, #6607, #852, .T. ) ;
#9764=ORIENTED_EDGE ( 'NONE', *, *, #15537, .F. ) ;
#9767=ORIENTED_EDGE ( 'NONE', *, *, #2307, .T. ) ;
#9768=VECTOR ( 'NONE', #6860, 1000.000000000000000 ) ;
#9769=DIRECTION ( 'NONE',  ( -1.000000000000000000, 0.000000000000000000, 0.000000000000000000 ) ) ;
#9770=CARTESIAN_POINT ( 'NONE',  ( 10.00000000000000000, -85.05652083079337444, 0.7600687895857258791 ) ) ;
#9771=AXIS2_PLACEMENT_3D ( 'NONE', #1728, #14976, #3269 ) ;
#9772=CYLINDRICAL_SURFACE ( 'NONE', #12552, 92.50100000000000477 ) ;
#9774=AXIS2_PLACEMENT_3D ( 'NONE', #12466, #10922, #438 ) ;
#9775=CARTESIAN_POINT ( 'NONE',  ( 0.000000000000000000, 64.95266917914317162, 59.37298010462993858 ) ) ;
#9777=ORIENTED_EDGE ( 'NONE', *, *, #9576, .T. ) ;
#9778=CARTESIAN_POINT ( 'NONE',  ( 10.00000000000000000, 0.000000000000000000, 0.000000000000000000 ) ) ;
#9779=CARTESIAN_POINT ( 'NONE',  ( 10.00000000000000000, 31.15801000616942673, -79.14775961996359399 ) ) ;
#9783=VECTOR ( 'NONE', #9251, 1000.000000000000000 ) ;
#9784=CARTESIAN_POINT ( 'NONE',  ( -10.00000000000000000, 0.000000000000000000, 0.000000000000000000 ) ) ;
#9785=AXIS2_PLACEMENT_3D ( 'NONE', #20608, #15527, #2052 ) ;
#9787=AXIS2_PLACEMENT_3D ( 'NONE', #4959, #13674, #1749 ) ;
#9788=EDGE_LOOP ( 'NONE', ( #16803, #7309, #21641, #8315 ) ) ;
#9792=FACE_OUTER_BOUND ( 'NONE', #17931, .T. ) ;
#9793=EDGE_LOOP ( 'NONE', ( #12854, #10363, #6855, #8248 ) ) ;
#9795=CARTESIAN_POINT ( 'NONE',  ( 10.00000000000000000, 0.000000000000000000, 0.000000000000000000 ) ) ;
#9796=CARTESIAN_POINT ( 'NONE',  ( 5.000000000000002665, -30.71797041605864464, 82.46457599186540222 ) ) ;
#9797=CARTESIAN_POINT ( 'NONE',  ( 0.000000000000000000, -84.33453774737664332, 11.08490790852103380 ) ) ;
#9798=PRESENTATION_STYLE_ASSIGNMENT (( #14793 ) ) ;
#9800=AXIS2_PLACEMENT_3D ( 'NONE', #4241, #9299, #14280 ) ;
#9801=VECTOR ( 'NONE', #146, 1000.000000000000000 ) ;
#9802=DIRECTION ( 'NONE',  ( 0.000000000000000000, -0.06975647374411146628, -0.9975640502598251969 ) ) ;
#9803=CYLINDRICAL_SURFACE ( 'NONE', #2911, 92.50100000000000477 ) ;
#9804=AXIS2_PLACEMENT_3D ( 'NONE', #20621, #18753, #306 ) ;
#9806=FACE_OUTER_BOUND ( 'NONE', #2188, .T. ) ;
#9807=DIRECTION ( 'NONE',  ( -1.000000000000000000, 0.000000000000000000, 0.000000000000000000 ) ) ;
#9808=FACE_OUTER_BOUND ( 'NONE', #15793, .T. ) ;
#9809=DIRECTION ( 'NONE',  ( 1.000000000000000000, 0.000000000000000000, 0.000000000000000000 ) ) ;
#9811=ORIENTED_EDGE ( 'NONE', *, *, #555, .F. ) ;
#9812=EDGE_CURVE ( 'NONE', #12235, #21050, #2968, .T. ) ;
#9813=ORIENTED_EDGE ( 'NONE', *, *, #3559, .T. ) ;
#9814=VERTEX_POINT ( 'NONE', #17975 ) ;
#9816=ORIENTED_EDGE ( 'NONE', *, *, #19063, .F. ) ;
#9817=CIRCLE ( 'NONE', #16883, 44.99999999999999289 ) ;
#9818=CIRCLE ( 'NONE', #315, 44.99999999999998579 ) ;
#9823=DIRECTION ( 'NONE',  ( -1.000000000000000000, -0.000000000000000000, -0.000000000000000000 ) ) ;
#9824=ORIENTED_EDGE ( 'NONE', *, *, #6756, .F. ) ;
#9825=CARTESIAN_POINT ( 'NONE',  ( 10.00000000000000000, -67.05625154133410604, -63.71729851637880415 ) ) ;
#9828=DIRECTION ( 'NONE',  ( 1.000000000000000000, 0.000000000000000000, 0.000000000000000000 ) ) ;
#9832=FACE_OUTER_BOUND ( 'NONE', #4833, .T. ) ;
#9833=CIRCLE ( 'NONE', #15838, 88.00000000000000000 ) ;
#9835=CIRCLE ( 'NONE', #332, 45.00000000000000000 ) ;
#9838=CYLINDRICAL_SURFACE ( 'NONE', #3743, 88.00000000000000000 ) ;
#9840=EDGE_CURVE ( 'NONE', #19664, #6016, #5450, .T. ) ;
#9842=ORIENTED_EDGE ( 'NONE', *, *, #16472, .F. ) ;
#9843=DIRECTION ( 'NONE',  ( 0.000000000000000000, 0.000000000000000000, 1.000000000000000000 ) ) ;
#9850=CYLINDRICAL_SURFACE ( 'NONE', #12263, 44.99999999999999289 ) ;
#9851=VERTEX_POINT ( 'NONE', #9438 ) ;
#9853=DIRECTION ( 'NONE',  ( 0.000000000000000000, 0.5877852522924689183, 0.8090169943749504489 ) ) ;
#9855=AXIS2_PLACEMENT_3D ( 'NONE', #2278, #4270, #7588 ) ;
#9856=DIRECTION ( 'NONE',  ( 0.000000000000000000, 0.000000000000000000, 1.000000000000000000 ) ) ;
#9857=ADVANCED_FACE ( 'NONE', ( #19728 ), #11553, .F. ) ;
#9860=CARTESIAN_POINT ( 'NONE',  ( 10.00000000000000000, 11.59241532900744787, -87.23311244498727035 ) ) ;
#9861=CARTESIAN_POINT ( 'NONE',  ( 10.00000000000000000, 0.000000000000000000, 0.000000000000000000 ) ) ;
#9863=CARTESIAN_POINT ( 'NONE',  ( 10.00000000000000000, 25.56104204395304080, 81.12843256239672485 ) ) ;
#9866=EDGE_CURVE ( 'NONE', #19686, #7874, #8967, .T. ) ;
#9869=CIRCLE ( 'NONE', #16234, 45.00000000000000000 ) ;
#9870=VECTOR ( 'NONE', #10323, 1000.000000000000000 ) ;
#9871=CYLINDRICAL_SURFACE ( 'NONE', #16504, 92.50100000000000477 ) ;
#9872=ADVANCED_FACE ( 'NONE', ( #16408 ), #19829, .F. ) ;
#9873=DIRECTION ( 'NONE',  ( -1.000000000000000000, -0.000000000000000000, -0.000000000000000000 ) ) ;
#9876=VERTEX_POINT ( 'NONE', #18072 ) ;
#9877=VERTEX_POINT ( 'NONE', #2927 ) ;
#9878=CYLINDRICAL_SURFACE ( 'NONE', #1163, 44.99999999999999289 ) ;
#9881=DIRECTION ( 'NONE',  ( 1.000000000000000000, 0.000000000000000000, 0.000000000000000000 ) ) ;
#9884=EDGE_CURVE ( 'NONE', #8891, #3599, #8232, .T. ) ;
#9886=CARTESIAN_POINT ( 'NONE',  ( 10.00000000000000000, 16.79755869217650144, 90.96305306542258506 ) ) ;
#9887=FACE_OUTER_BOUND ( 'NONE', #7089, .T. ) ;
#9888=AXIS2_PLACEMENT_3D ( 'NONE', #7864, #14600, #19361 ) ;
#9894=ORIENTED_EDGE ( 'NONE', *, *, #12333, .T. ) ;
#9897=DIRECTION ( 'NONE',  ( -1.000000000000000000, 0.000000000000000000, -0.000000000000000000 ) ) ;
#9899=CARTESIAN_POINT ( 'NONE',  ( 10.00000000000000000, 91.49386717542239467, -13.61276130276895557 ) ) ;
#9900=ORIENTED_EDGE ( 'NONE', *, *, #13116, .T. ) ;
#9901=ADVANCED_FACE ( 'NONE', ( #3045 ), #16524, .F. ) ;
#9903=CIRCLE ( 'NONE', #4611, 45.00000000000000000 ) ;
#9904=CARTESIAN_POINT ( 'NONE',  ( 10.00000000000000000, -85.05652083079338865, -0.7600687895868707411 ) ) ;
#9907=ORIENTED_EDGE ( 'NONE', *, *, #18891, .F. ) ;
#9910=ORIENTED_EDGE ( 'NONE', *, *, #8959, .F. ) ;
#9911=CARTESIAN_POINT ( 'NONE',  ( 0.000000000000000000, 61.71252885873465033, -58.53847642588533517 ) ) ;
#9917=DIRECTION ( 'NONE',  ( -1.000000000000000000, 0.000000000000000000, -0.000000000000000000 ) ) ;
#9920=ADVANCED_FACE ( 'NONE', ( #13308 ), #13851, .F. ) ;
#9923=CARTESIAN_POINT ( 'NONE',  ( 0.000000000000000000, 51.76708072107885528, 67.49339815138510801 ) ) ;
#9927=VERTEX_POINT ( 'NONE', #6709 ) ;
#9928=ORIENTED_EDGE ( 'NONE', *, *, #3394, .F. ) ;
#9929=VECTOR ( 'NONE', #493, 1000.000000000000000 ) ;
#9931=VERTEX_POINT ( 'NONE', #164 ) ;
#9932=CARTESIAN_POINT ( 'NONE',  ( 10.00000000000000000, -39.87723064937176076, 83.46401306393555330 ) ) ;
#9933=ORIENTED_EDGE ( 'NONE', *, *, #21745, .F. ) ;
#9934=DIRECTION ( 'NONE',  ( -1.000000000000000000, -0.000000000000000000, -0.000000000000000000 ) ) ;
#9935=DIRECTION ( 'NONE',  ( -1.000000000000000000, -0.000000000000000000, -0.000000000000000000 ) ) ;
#9936=ADVANCED_FACE ( 'NONE', ( #3480 ), #1602, .F. ) ;
#9937=CARTESIAN_POINT ( 'NONE',  ( 10.00000000000000000, -67.05625154133495869, 63.71729851637790176 ) ) ;
#9938=DIRECTION ( 'NONE',  ( -1.000000000000000000, -0.000000000000000000, -0.000000000000000000 ) ) ;
#9939=FACE_OUTER_BOUND ( 'NONE', #7464, .T. ) ;
#9940=DIRECTION ( 'NONE',  ( 0.000000000000000000, -9.251858538542971828E-16, -1.000000000000000000 ) ) ;
#9942=ORIENTED_EDGE ( 'NONE', *, *, #11752, .T. ) ;
#9944=ORIENTED_EDGE ( 'NONE', *, *, #3499, .F. ) ;
#9945=EDGE_LOOP ( 'NONE', ( #9288, #4985, #18634, #15936 ) ) ;
#9947=CIRCLE ( 'NONE', #19135, 88.00000000000000000 ) ;
#9948=EDGE_LOOP ( 'NONE', ( #9894, #18747, #5397, #4440 ) ) ;
#9950=VERTEX_POINT ( 'NONE', #15072 ) ;
#9951=ORIENTED_EDGE ( 'NONE', *, *, #9577, .F. ) ;
#9953=CARTESIAN_POINT ( 'NONE',  ( 10.00000000000000000, -27.00677879428973682, -80.65868421664460186 ) ) ;
#9955=FACE_OUTER_BOUND ( 'NONE', #11839, .T. ) ;
#9956=CARTESIAN_POINT ( 'NONE',  ( 10.00000000000000000, 91.70173545986517638, 12.13370160540072362 ) ) ;
#9957=AXIS2_PLACEMENT_3D ( 'NONE', #6883, #10187, #132 ) ;
#9959=CARTESIAN_POINT ( 'NONE',  ( 10.00000000000000000, 0.000000000000000000, 0.000000000000000000 ) ) ;
#9960=EDGE_CURVE ( 'NONE', #6192, #783, #18510, .T. ) ;
#9961=CARTESIAN_POINT ( 'NONE',  ( 0.000000000000000000, -23.10190250628894404, 89.56973317806591695 ) ) ;
#9963=CARTESIAN_POINT ( 'NONE',  ( 0.000000000000000000, 0.000000000000000000, 0.000000000000000000 ) ) ;
#9964=DIRECTION ( 'NONE',  ( 1.000000000000000000, 0.000000000000000000, 0.000000000000000000 ) ) ;
#9968=DIRECTION ( 'NONE',  ( 0.000000000000000000, 0.000000000000000000, 1.000000000000000000 ) ) ;
#9971=VECTOR ( 'NONE', #1442, 1000.000000000000000 ) ;
#9972=ORIENTED_EDGE ( 'NONE', *, *, #11267, .T. ) ;
#9973=DIRECTION ( 'NONE',  ( 1.000000000000000000, 0.000000000000000000, -0.000000000000000000 ) ) ;
#9974=ORIENTED_EDGE ( 'NONE', *, *, #1769, .T. ) ;
#9978=EDGE_LOOP ( 'NONE', ( #6707, #18117, #2347, #16336 ) ) ;
#9981=DIRECTION ( 'NONE',  ( 0.000000000000000000, 0.000000000000000000, 1.000000000000000000 ) ) ;
#9982=AXIS2_PLACEMENT_3D ( 'NONE', #701, #15725, #17501 ) ;
#9989=ADVANCED_FACE ( 'NONE', ( #12083 ), #8459, .F. ) ;
#9990=DIRECTION ( 'NONE',  ( -1.000000000000000000, 0.000000000000000000, 0.000000000000000000 ) ) ;
#9991=CARTESIAN_POINT ( 'NONE',  ( 10.00000000000000000, 0.000000000000000000, 0.000000000000000000 ) ) ;
#9992=DIRECTION ( 'NONE',  ( 0.000000000000000000, 0.000000000000000000, 1.000000000000000000 ) ) ;
#9993=EDGE_CURVE ( 'NONE', #5530, #2619, #8774, .T. ) ;
#9994=AXIS2_PLACEMENT_3D ( 'NONE', #15212, #13226, #18221 ) ;
#9995=ORIENTED_EDGE ( 'NONE', *, *, #276, .T. ) ;
#9996=DIRECTION ( 'NONE',  ( -1.000000000000000000, 0.000000000000000000, 0.000000000000000000 ) ) ;
#9998=CARTESIAN_POINT ( 'NONE',  ( 0.000000000000000000, 27.00677879429135331, -80.65868421664406185 ) ) ;
#10001=DIRECTION ( 'NONE',  ( 0.000000000000000000, 0.000000000000000000, 1.000000000000000000 ) ) ;
#10002=EDGE_CURVE ( 'NONE', #6908, #5130, #20167, .T. ) ;
#10004=CARTESIAN_POINT ( 'NONE',  ( 0.000000000000000000, 15.51843147776349063, 83.63233659819657362 ) ) ;
#10005=DIRECTION ( 'NONE',  ( -1.000000000000000000, -0.000000000000000000, -0.000000000000000000 ) ) ;
#10006=ORIENTED_EDGE ( 'NONE', *, *, #21344, .F. ) ;
#10008=EDGE_CURVE ( 'NONE', #8011, #7101, #13635, .T. ) ;
#10009=AXIS2_PLACEMENT_3D ( 'NONE', #14107, #9441, #16198 ) ;
#10010=ORIENTED_EDGE ( 'NONE', *, *, #16868, .T. ) ;
#10011=EDGE_LOOP ( 'NONE', ( #303, #6636, #9217, #7958 ) ) ;
#10013=ORIENTED_EDGE ( 'NONE', *, *, #10086, .T. ) ;
#10016=CYLINDRICAL_SURFACE ( 'NONE', #18897, 44.99999999999999289 ) ;
#10017=CARTESIAN_POINT ( 'NONE',  ( 0.000000000000000000, 29.29369617358583255, -87.74003855418371245 ) ) ;
#10019=( NAMED_UNIT ( * ) PLANE_ANGLE_UNIT ( ) SI_UNIT ( $, .RADIAN. ) );
#10022=DIRECTION ( 'NONE',  ( 0.000000000000000000, -0.4694715627858797591, -0.8829475928589327616 ) ) ;
#10023=CYLINDRICAL_SURFACE ( 'NONE', #17632, 44.99999999999999289 ) ;
#10026=DIRECTION ( 'NONE',  ( 1.000000000000000000, 0.000000000000000000, 0.000000000000000000 ) ) ;
#10028=CIRCLE ( 'NONE', #16017, 45.00000000000000000 ) ;
#10029=VERTEX_POINT ( 'NONE', #11763 ) ;
#10031=ORIENTED_EDGE ( 'NONE', *, *, #17211, .T. ) ;
#10032=CARTESIAN_POINT ( 'NONE',  ( 10.00000000000000000, 3.728035544477412255, -84.97818067823766341 ) ) ;
#10034=AXIS2_PLACEMENT_3D ( 'NONE', #20385, #18729, #3583 ) ;
#10035=ORIENTED_EDGE ( 'NONE', *, *, #4083, .T. ) ;
#10036=VERTEX_POINT ( 'NONE', #10315 ) ;
#10037=EDGE_CURVE ( 'NONE', #21406, #19754, #6538, .T. ) ;
#10038=ADVANCED_FACE ( 'NONE', ( #4929 ), #4240, .F. ) ;
#10039=VERTEX_POINT ( 'NONE', #5900 ) ;
#10040=FACE_OUTER_BOUND ( 'NONE', #695, .T. ) ;
#10041=CIRCLE ( 'NONE', #521, 88.00000000000000000 ) ;
#10043=DIRECTION ( 'NONE',  ( 0.000000000000000000, 3.546545773108138773E-15, -1.000000000000000000 ) ) ;
#10045=CARTESIAN_POINT ( 'NONE',  ( 10.00000000000000000, 0.000000000000000000, 0.000000000000000000 ) ) ;
#10047=AXIS2_PLACEMENT_3D ( 'NONE', #20596, #10971, #21032 ) ;
#10048=CIRCLE ( 'NONE', #528, 44.99999999999998579 ) ;
#10049=CARTESIAN_POINT ( 'NONE',  ( 0.000000000000000000, 16.79755869217650144, 90.96305306542258506 ) ) ;
#10052=CARTESIAN_POINT ( 'NONE',  ( 0.000000000000000000, -18.94217447942500598, -85.93715160505971085 ) ) ;
#10054=ORIENTED_EDGE ( 'NONE', *, *, #15783, .T. ) ;
#10056=AXIS2_PLACEMENT_3D ( 'NONE', #9528, #20923, #16606 ) ;
#10059=CIRCLE ( 'NONE', #545, 92.50100000000001899 ) ;
#10060=ORIENTED_EDGE ( 'NONE', *, *, #17047, .F. ) ;
#10061=CIRCLE ( 'NONE', #7944, 88.00000000000000000 ) ;
#10062=DIRECTION ( 'NONE',  ( -1.000000000000000000, 0.000000000000000000, -0.000000000000000000 ) ) ;
#10064=DIRECTION ( 'NONE',  ( 0.000000000000000000, 0.000000000000000000, 1.000000000000000000 ) ) ;
#10066=ORIENTED_EDGE ( 'NONE', *, *, #21759, .F. ) ;
#10068=CARTESIAN_POINT ( 'NONE',  ( 10.00000000000000000, 0.000000000000000000, 0.000000000000000000 ) ) ;
#10069=ORIENTED_EDGE ( 'NONE', *, *, #4777, .T. ) ;
#10072=CARTESIAN_POINT ( 'NONE',  ( 10.00000000000000000, -15.51843147776295950, -83.63233659819665888 ) ) ;
#10073=DIRECTION ( 'NONE',  ( -1.000000000000000000, -0.000000000000000000, -0.000000000000000000 ) ) ;
#10074=CIRCLE ( 'NONE', #3727, 88.00000000000000000 ) ;
#10075=DIRECTION ( 'NONE',  ( 0.000000000000000000, -0.4067366430757887730, -0.9135454576426059736 ) ) ;
#10076=CIRCLE ( 'NONE', #13613, 45.00000000000000711 ) ;
#10077=AXIS2_PLACEMENT_3D ( 'NONE', #10640, #21252, #14399 ) ;
#10079=DIRECTION ( 'NONE',  ( -1.000000000000000000, 0.000000000000000000, -0.000000000000000000 ) ) ;
#10080=LINE ( 'NONE', #3343, #20043 ) ;
#10081=CIRCLE ( 'NONE', #21031, 88.00000000000000000 ) ;
#10082=ORIENTED_EDGE ( 'NONE', *, *, #14082, .T. ) ;
#10084=CYLINDRICAL_SURFACE ( 'NONE', #8822, 92.50100000000000477 ) ;
#10085=ORIENTED_EDGE ( 'NONE', *, *, #17435, .F. ) ;
#10086=EDGE_CURVE ( 'NONE', #12373, #2852, #12497, .T. ) ;
#10087=CIRCLE ( 'NONE', #574, 92.50100000000001899 ) ;
#10088=CARTESIAN_POINT ( 'NONE',  ( 10.00000000000000000, -85.22372865846305956, 21.92979875759597874 ) ) ;
#10089=ORIENTED_EDGE ( 'NONE', *, *, #2034, .F. ) ;
#10090=AXIS2_PLACEMENT_3D ( 'NONE', #3228, #1140, #14836 ) ;
#10093=ORIENTED_EDGE ( 'NONE', *, *, #12403, .F. ) ;
#10094=DIRECTION ( 'NONE',  ( -1.000000000000000000, -0.000000000000000000, -0.000000000000000000 ) ) ;
#10096=ORIENTED_EDGE ( 'NONE', *, *, #13922, .T. ) ;
#10098=CARTESIAN_POINT ( 'NONE',  ( 10.00000000000000000, -68.36541360927220978, 50.60987712331682076 ) ) ;
#10099=EDGE_CURVE ( 'NONE', #3139, #10994, #1582, .T. ) ;
#10101=DIRECTION ( 'NONE',  ( 0.000000000000000000, 0.000000000000000000, 1.000000000000000000 ) ) ;
#10103=DIRECTION ( 'NONE',  ( -1.000000000000000000, 0.000000000000000000, 0.000000000000000000 ) ) ;
#10104=CARTESIAN_POINT ( 'NONE',  ( 0.000000000000000000, -3.728035544476815399, 84.97818067823770605 ) ) ;
#10106=CARTESIAN_POINT ( 'NONE',  ( 5.000000000000000000, 65.83713140174729972, 58.39068529131218099 ) ) ;
#10107=AXIS2_PLACEMENT_3D ( 'NONE', #14468, #6077, #763 ) ;
#10110=CYLINDRICAL_SURFACE ( 'NONE', #1925, 44.99999999999999289 ) ;
#10113=CYLINDRICAL_SURFACE ( 'NONE', #19658, 88.00000000000000000 ) ;
#10114=ORIENTED_EDGE ( 'NONE', *, *, #18141, .F. ) ;
#10115=EDGE_CURVE ( 'NONE', #19966, #17806, #10638, .T. ) ;
#10118=CARTESIAN_POINT ( 'NONE',  ( 10.00000000000000000, -29.29369617358527833, 87.74003855418389719 ) ) ;
#10123=ORIENTED_EDGE ( 'NONE', *, *, #19078, .T. ) ;
#10125=AXIS2_PLACEMENT_3D ( 'NONE', #21721, #8146, #3057 ) ;
#10126=ORIENTED_EDGE ( 'NONE', *, *, #16876, .T. ) ;
#10127=DIRECTION ( 'NONE',  ( 0.000000000000000000, 0.9271838545667857590, 0.3746065934159160671 ) ) ;
#10128=AXIS2_PLACEMENT_3D ( 'NONE', #3864, #5963, #20981 ) ;
#10129=EDGE_LOOP ( 'NONE', ( #6319, #3003, #17174, #15603 ) ) ;
#10131=CARTESIAN_POINT ( 'NONE',  ( 10.00000000000000000, -74.74361964203257003, 40.60271866773520344 ) ) ;
#10132=CARTESIAN_POINT ( 'NONE',  ( 0.000000000000000000, 0.000000000000000000, 0.000000000000000000 ) ) ;
#10133=CARTESIAN_POINT ( 'NONE',  ( 5.000000000000002665, -87.44637528609668209, 9.855528870798345054 ) ) ;
#10135=ADVANCED_FACE ( 'NONE', ( #14074 ), #2355, .F. ) ;
#10138=CYLINDRICAL_SURFACE ( 'NONE', #20461, 88.00000000000000000 ) ;
#10139=CIRCLE ( 'NONE', #21432, 44.99999999999999289 ) ;
#10144=ORIENTED_EDGE ( 'NONE', *, *, #12048, .T. ) ;
#10145=DIRECTION ( 'NONE',  ( 0.000000000000000000, 0.000000000000000000, 1.000000000000000000 ) ) ;
#10146=EDGE_CURVE ( 'NONE', #2267, #8367, #14279, .T. ) ;
#10147=VERTEX_POINT ( 'NONE', #2245 ) ;
#10149=VERTEX_POINT ( 'NONE', #19376 ) ;
#10151=ORIENTED_EDGE ( 'NONE', *, *, #12209, .F. ) ;
#10153=CARTESIAN_POINT ( 'NONE',  ( 10.00000000000000000, -36.60317927562628881, 76.78148674856751654 ) ) ;
#10156=VERTEX_POINT ( 'NONE', #2569 ) ;
#10157=FACE_OUTER_BOUND ( 'NONE', #10651, .T. ) ;
#10158=CIRCLE ( 'NONE', #7001, 45.00000000000000000 ) ;
#10159=CIRCLE ( 'NONE', #7686, 44.99999999999999289 ) ;
#10161=EDGE_CURVE ( 'NONE', #21676, #13846, #2637, .T. ) ;
#10162=DIRECTION ( 'NONE',  ( 0.000000000000000000, -0.8987940462991711454, 0.4383711467890689661 ) ) ;
#10164=CYLINDRICAL_SURFACE ( 'NONE', #6531, 44.99999999999999289 ) ;
#10165=EDGE_CURVE ( 'NONE', #1066, #14735, #14170, .T. ) ;
#10166=CARTESIAN_POINT ( 'NONE',  ( 10.00000000000000000, -84.12297548659712731, -12.59025161327086906 ) ) ;
#10167=AXIS2_PLACEMENT_3D ( 'NONE', #19028, #10073, #463 ) ;
#10169=ADVANCED_FACE ( 'NONE', ( #18943 ), #20817, .F. ) ;
#10171=EDGE_CURVE ( 'NONE', #7364, #8570, #20915, .T. ) ;
#10172=DIRECTION ( 'NONE',  ( 0.000000000000000000, -0.3420201433256757073, 0.9396926207859057634 ) ) ;
#10176=CIRCLE ( 'NONE', #7361, 88.00000000000000000 ) ;
#10178=VERTEX_POINT ( 'NONE', #19264 ) ;
#10181=ORIENTED_EDGE ( 'NONE', *, *, #7850, .F. ) ;
#10184=EDGE_LOOP ( 'NONE', ( #17341, #7875, #15777, #12948 ) ) ;
#10185=DIRECTION ( 'NONE',  ( -1.000000000000000000, -0.000000000000000000, -0.000000000000000000 ) ) ;
#10186=ORIENTED_EDGE ( 'NONE', *, *, #11113, .F. ) ;
#10187=DIRECTION ( 'NONE',  ( -1.000000000000000000, -0.000000000000000000, 0.000000000000000000 ) ) ;
#10191=CIRCLE ( 'NONE', #11616, 88.00000000000000000 ) ;
#10192=DIRECTION ( 'NONE',  ( 1.000000000000000000, 0.000000000000000000, 0.000000000000000000 ) ) ;
#10198=ORIENTED_EDGE ( 'NONE', *, *, #21759, .T. ) ;
#10202=ORIENTED_EDGE ( 'NONE', *, *, #3608, .T. ) ;
#10206=PRODUCT_DEFINITION_SHAPE ( 'NONE', 'NONE',  #5646 ) ;
#10207=CIRCLE ( 'NONE', #13395, 44.99999999999999289 ) ;
#10208=VERTEX_POINT ( 'NONE', #7546 ) ;
#10210=ORIENTED_EDGE ( 'NONE', *, *, #9339, .T. ) ;
#10211=CYLINDRICAL_SURFACE ( 'NONE', #1176, 88.00000000000000000 ) ;
#10213=EDGE_LOOP ( 'NONE', ( #20480, #14636, #7390, #4881 ) ) ;
#10214=FACE_OUTER_BOUND ( 'NONE', #2402, .T. ) ;
#10216=ORIENTED_EDGE ( 'NONE', *, *, #4791, .F. ) ;
#10217=CARTESIAN_POINT ( 'NONE',  ( 10.00000000000000000, -62.44821182181136976, 68.23969402963483333 ) ) ;
#10218=CARTESIAN_POINT ( 'NONE',  ( 10.00000000000000000, -52.25832601289046409, -70.80301803122840454 ) ) ;
#10219=DIRECTION ( 'NONE',  ( -1.000000000000000000, -0.000000000000000000, -0.000000000000000000 ) ) ;
#10221=CARTESIAN_POINT ( 'NONE',  ( 5.000000000000000000, 87.58454185039441597, 8.540961822681984117 ) ) ;
#10223=ADVANCED_FACE ( 'NONE', ( #12307 ), #11301, .F. ) ;
#10224=VECTOR ( 'NONE', #5235, 1000.000000000000000 ) ;
#10225=ORIENTED_EDGE ( 'NONE', *, *, #20015, .F. ) ;
#10226=AXIS2_PLACEMENT_3D ( 'NONE', #6389, #2936, #19954 ) ;
#10227=LINE ( 'NONE', #176, #9870 ) ;
#10228=DIRECTION ( 'NONE',  ( 0.000000000000000000, 0.000000000000000000, 1.000000000000000000 ) ) ;
#10229=EDGE_LOOP ( 'NONE', ( #20990, #12939, #8502, #9207 ) ) ;
#10230=DIRECTION ( 'NONE',  ( 1.000000000000000000, -0.000000000000000000, -0.000000000000000000 ) ) ;
#10231=EDGE_LOOP ( 'NONE', ( #9842, #18852, #8688, #2003 ) ) ;
#10233=DIRECTION ( 'NONE',  ( 0.000000000000000000, 0.000000000000000000, 1.000000000000000000 ) ) ;
#10235=DIRECTION ( 'NONE',  ( 0.000000000000000000, -0.9945218953682744001, 0.1045284632676437564 ) ) ;
#10236=ORIENTED_EDGE ( 'NONE', *, *, #1870, .F. ) ;
#10237=ORIENTED_EDGE ( 'NONE', *, *, #10837, .F. ) ;
#10241=ORIENTED_EDGE ( 'NONE', *, *, #2421, .T. ) ;
#10244=CARTESIAN_POINT ( 'NONE',  ( 10.00000000000000000, 40.72878876293147954, 78.00747250042462611 ) ) ;
#10245=DIRECTION ( 'NONE',  ( 0.000000000000000000, 0.000000000000000000, 1.000000000000000000 ) ) ;
#10247=ADVANCED_FACE ( 'NONE', ( #11526 ), #1250, .F. ) ;
#10250=CARTESIAN_POINT ( 'NONE',  ( 10.00000000000000000, 0.000000000000000000, 0.000000000000000000 ) ) ;
#10252=CIRCLE ( 'NONE', #385, 92.50100000000000477 ) ;
#10253=EDGE_CURVE ( 'NONE', #5782, #8283, #14397, .T. ) ;
#10259=VERTEX_POINT ( 'NONE', #4569 ) ;
#10260=ADVANCED_FACE ( 'NONE', ( #21356 ), #1034, .F. ) ;
#10264=DIRECTION ( 'NONE',  ( 0.000000000000000000, -0.9271838545667832054, -0.3746065934159225619 ) ) ;
#10266=CARTESIAN_POINT ( 'NONE',  ( 0.000000000000000000, 15.51843147776463638, -83.63233659819634624 ) ) ;
#10267=CARTESIAN_POINT ( 'NONE',  ( 10.00000000000000000, 0.000000000000000000, 0.000000000000000000 ) ) ;
#10268=EDGE_CURVE ( 'NONE', #15150, #4259, #21339, .T. ) ;
#10271=CARTESIAN_POINT ( 'NONE',  ( 10.00000000000000000, 18.94217447942673971, -85.93715160505934136 ) ) ;
#10274=CARTESIAN_POINT ( 'NONE',  ( 0.000000000000000000, 0.000000000000000000, 0.000000000000000000 ) ) ;
#10277=VERTEX_POINT ( 'NONE', #14614 ) ;
#10283=DIRECTION ( 'NONE',  ( -1.000000000000000000, 0.000000000000000000, 0.000000000000000000 ) ) ;
#10284=ORIENTED_EDGE ( 'NONE', *, *, #936, .T. ) ;
#10285=EDGE_LOOP ( 'NONE', ( #17517, #14141, #6881, #20875 ) ) ;
#10286=ORIENTED_EDGE ( 'NONE', *, *, #10037, .T. ) ;
#10288=LINE ( 'NONE', #5537, #13322 ) ;
#10289=ORIENTED_EDGE ( 'NONE', *, *, #3701, .T. ) ;
#10291=ADVANCED_FACE ( 'NONE', ( #4784 ), #12736, .F. ) ;
#10294=DIRECTION ( 'NONE',  ( 1.000000000000000000, 0.000000000000000000, 0.000000000000000000 ) ) ;
#10295=CARTESIAN_POINT ( 'NONE',  ( 10.00000000000000000, -52.96496548042899377, 66.55750800669339640 ) ) ;
#10299=EDGE_LOOP ( 'NONE', ( #16069, #4146, #12218, #9777 ) ) ;
#10300=CYLINDRICAL_SURFACE ( 'NONE', #7701, 44.99999999999999289 ) ;
#10301=DIRECTION ( 'NONE',  ( 0.000000000000000000, 0.000000000000000000, 1.000000000000000000 ) ) ;
#10302=ORIENTED_EDGE ( 'NONE', *, *, #342, .F. ) ;
#10303=CYLINDRICAL_SURFACE ( 'NONE', #21360, 45.00000000000000000 ) ;
#10307=CARTESIAN_POINT ( 'NONE',  ( 10.00000000000000000, 0.000000000000000000, 0.000000000000000000 ) ) ;
#10308=VERTEX_POINT ( 'NONE', #16495 ) ;
#10309=ORIENTED_EDGE ( 'NONE', *, *, #19459, .T. ) ;
#10310=EDGE_CURVE ( 'NONE', #11054, #15560, #18187, .T. ) ;
#10312=CARTESIAN_POINT ( 'NONE',  ( 10.00000000000000000, 0.000000000000000000, 0.000000000000000000 ) ) ;
#10313=EDGE_CURVE ( 'NONE', #19086, #7932, #16775, .T. ) ;
#10314=AXIS2_PLACEMENT_3D ( 'NONE', #11494, #4862, #16795 ) ;
#10315=CARTESIAN_POINT ( 'NONE',  ( 10.00000000000000000, -17.64925110578526812, 86.21197095186339254 ) ) ;
#10316=DIRECTION ( 'NONE',  ( -1.000000000000000000, 0.000000000000000000, 0.000000000000000000 ) ) ;
#10318=DIRECTION ( 'NONE',  ( 0.000000000000000000, -0.5299192642332118952, 0.8480480961564216269 ) ) ;
#10319=CIRCLE ( 'NONE', #11026, 45.00000000000000000 ) ;
#10322=ORIENTED_EDGE ( 'NONE', *, *, #21593, .T. ) ;
#10323=DIRECTION ( 'NONE',  ( -1.000000000000000000, 0.000000000000000000, 0.000000000000000000 ) ) ;
#10326=EDGE_LOOP ( 'NONE', ( #19436, #17789, #13748, #2642 ) ) ;
#10327=DIRECTION ( 'NONE',  ( -1.000000000000000000, -0.000000000000000000, 0.000000000000000000 ) ) ;
#10329=CIRCLE ( 'NONE', #7858, 88.00000000000000000 ) ;
#10331=DIRECTION ( 'NONE',  ( -1.000000000000000000, -0.000000000000000000, 0.000000000000000000 ) ) ;
#10332=VERTEX_POINT ( 'NONE', #20248 ) ;
#10333=CIRCLE ( 'NONE', #19155, 92.50100000000000477 ) ;
#10334=LINE ( 'NONE', #18853, #1089 ) ;
#10336=ORIENTED_EDGE ( 'NONE', *, *, #8197, .T. ) ;
#10337=ORIENTED_EDGE ( 'NONE', *, *, #5001, .F. ) ;
#10341=CIRCLE ( 'NONE', #21640, 44.99999999999998579 ) ;
#10342=DIRECTION ( 'NONE',  ( -1.000000000000000000, 0.000000000000000000, 0.000000000000000000 ) ) ;
#10343=DIRECTION ( 'NONE',  ( 0.000000000000000000, -1.788692650784974777E-14, -1.000000000000000000 ) ) ;
#10344=DIRECTION ( 'NONE',  ( 0.000000000000000000, 0.000000000000000000, 1.000000000000000000 ) ) ;
#10347=CIRCLE ( 'NONE', #11405, 88.00000000000000000 ) ;
#10348=FACE_OUTER_BOUND ( 'NONE', #13074, .T. ) ;
#10349=DIRECTION ( 'NONE',  ( 0.000000000000000000, 0.000000000000000000, 1.000000000000000000 ) ) ;
#10350=ORIENTED_EDGE ( 'NONE', *, *, #6090, .T. ) ;
#10352=DIRECTION ( 'NONE',  ( 0.000000000000000000, 0.000000000000000000, 1.000000000000000000 ) ) ;
#10353=DIRECTION ( 'NONE',  ( 0.000000000000000000, 0.000000000000000000, 1.000000000000000000 ) ) ;
#10354=CYLINDRICAL_SURFACE ( 'NONE', #8023, 92.50100000000000477 ) ;
#10355=VERTEX_POINT ( 'NONE', #4997 ) ;
#10357=DIRECTION ( 'NONE',  ( 0.000000000000000000, 0.5299192642331997938, 0.8480480961564290654 ) ) ;
#10360=ORIENTED_EDGE ( 'NONE', *, *, #16484, .F. ) ;
#10361=EDGE_CURVE ( 'NONE', #14927, #15756, #1897, .T. ) ;
#10363=ORIENTED_EDGE ( 'NONE', *, *, #456, .T. ) ;
#10364=DIRECTION ( 'NONE',  ( -1.000000000000000000, -0.000000000000000000, -0.000000000000000000 ) ) ;
#10366=ORIENTED_EDGE ( 'NONE', *, *, #3916, .F. ) ;
#10368=DIRECTION ( 'NONE',  ( 1.000000000000000000, 0.000000000000000000, -0.000000000000000000 ) ) ;
#10371=AXIS2_PLACEMENT_3D ( 'NONE', #14077, #601, #6023 ) ;
#10372=DIRECTION ( 'NONE',  ( 0.000000000000000000, 2.775557561562891351E-15, -1.000000000000000000 ) ) ;
#10377=AXIS2_PLACEMENT_3D ( 'NONE', #14103, #15874, #2271 ) ;
#10378=ORIENTED_EDGE ( 'NONE', *, *, #7064, .F. ) ;
#10379=AXIS2_PLACEMENT_3D ( 'NONE', #16960, #53, #14958 ) ;
#10380=CYLINDRICAL_SURFACE ( 'NONE', #12208, 92.50100000000000477 ) ;
#10381=ORIENTED_EDGE ( 'NONE', *, *, #16700, .F. ) ;
#10382=ORIENTED_EDGE ( 'NONE', *, *, #19273, .F. ) ;
#10383=DIRECTION ( 'NONE',  ( 1.000000000000000000, -0.000000000000000000, -0.000000000000000000 ) ) ;
#10384=ORIENTED_EDGE ( 'NONE', *, *, #13784, .F. ) ;
#10386=AXIS2_PLACEMENT_3D ( 'NONE', #6843, #12123, #10581 ) ;
#10387=EDGE_CURVE ( 'NONE', #13415, #4660, #13282, .T. ) ;
#10388=EDGE_CURVE ( 'NONE', #11272, #19710, #10061, .T. ) ;
#10390=VERTEX_POINT ( 'NONE', #15368 ) ;
#10391=VECTOR ( 'NONE', #7447, 1000.000000000000000 ) ;
#10392=CYLINDRICAL_SURFACE ( 'NONE', #19680, 92.50100000000000477 ) ;
#10393=EDGE_CURVE ( 'NONE', #4335, #6526, #11733, .T. ) ;
#10394=EDGE_LOOP ( 'NONE', ( #10066, #5722, #6610, #12505 ) ) ;
#10396=CARTESIAN_POINT ( 'NONE',  ( 10.00000000000000000, 0.000000000000000000, 0.000000000000000000 ) ) ;
#10399=DIRECTION ( 'NONE',  ( 0.000000000000000000, 0.000000000000000000, 1.000000000000000000 ) ) ;
#10401=DIRECTION ( 'NONE',  ( -1.000000000000000000, -0.000000000000000000, 0.000000000000000000 ) ) ;
#10403=CYLINDRICAL_SURFACE ( 'NONE', #10866, 92.50100000000000477 ) ;
#10404=CIRCLE ( 'NONE', #16398, 88.00000000000000000 ) ;
#10407=EDGE_CURVE ( 'NONE', #4687, #3326, #3712, .T. ) ;
#10409=CIRCLE ( 'NONE', #12180, 44.99999999999998579 ) ;
#10410=LINE ( 'NONE', #13621, #17579 ) ;
#10411=LINE ( 'NONE', #14158, #9167 ) ;
#10412=VERTEX_POINT ( 'NONE', #20033 ) ;
#10414=DIRECTION ( 'NONE',  ( 0.000000000000000000, 1.850371707708594760E-15, -1.000000000000000000 ) ) ;
#10415=ORIENTED_EDGE ( 'NONE', *, *, #17562, .T. ) ;
#10419=EDGE_CURVE ( 'NONE', #4590, #3028, #18553, .T. ) ;
#10420=ORIENTED_EDGE ( 'NONE', *, *, #7042, .T. ) ;
#10421=AXIS2_PLACEMENT_3D ( 'NONE', #12933, #6002, #21015 ) ;
#10422=EDGE_LOOP ( 'NONE', ( #19252, #13653, #11427, #2708 ) ) ;
#10424=DIRECTION ( 'NONE',  ( 1.000000000000000000, 0.000000000000000000, 0.000000000000000000 ) ) ;
#10425=CIRCLE ( 'NONE', #9362, 44.99999999999999289 ) ;
#10428=DIRECTION ( 'NONE',  ( -1.000000000000000000, -0.000000000000000000, -0.000000000000000000 ) ) ;
#10429=CARTESIAN_POINT ( 'NONE',  ( 10.00000000000000000, -78.04699792498179534, 49.64978465107262906 ) ) ;
#10430=CYLINDRICAL_SURFACE ( 'NONE', #14962, 92.50100000000000477 ) ;
#10433=ADVANCED_FACE ( 'NONE', ( #15052 ), #6992, .F. ) ;
#10434=ORIENTED_EDGE ( 'NONE', *, *, #18545, .T. ) ;
#10435=ADVANCED_FACE ( 'NONE', ( #14939 ), #15159, .F. ) ;
#10439=EDGE_CURVE ( 'NONE', #20835, #5395, #20999, .T. ) ;
#10441=VECTOR ( 'NONE', #20146, 1000.000000000000000 ) ;
#10443=CARTESIAN_POINT ( 'NONE',  ( 0.000000000000000000, 79.38136668499741688, 37.98155635597341728 ) ) ;
#10444=AXIS2_PLACEMENT_3D ( 'NONE', #3992, #5882, #2338 ) ;
#10445=ORIENTED_EDGE ( 'NONE', *, *, #20284, .F. ) ;
#10450=EDGE_CURVE ( 'NONE', #7150, #21231, #13608, .T. ) ;
#10451=ORIENTED_EDGE ( 'NONE', *, *, #14581, .F. ) ;
#10452=ORIENTED_EDGE ( 'NONE', *, *, #9189, .T. ) ;
#10454=VERTEX_POINT ( 'NONE', #17039 ) ;
#10455=CARTESIAN_POINT ( 'NONE',  ( -10.00000000000000000, 0.000000000000000000, 0.000000000000000000 ) ) ;
#10456=DIRECTION ( 'NONE',  ( -1.000000000000000000, -0.000000000000000000, -0.000000000000000000 ) ) ;
#10457=FACE_OUTER_BOUND ( 'NONE', #10231, .T. ) ;
#10459=CARTESIAN_POINT ( 'NONE',  ( 0.000000000000000000, 0.000000000000000000, 0.000000000000000000 ) ) ;
#10461=AXIS2_PLACEMENT_3D ( 'NONE', #11499, #6207, #6433 ) ;
#10462=CARTESIAN_POINT ( 'NONE',  ( 0.000000000000000000, -75.87763420127865288, 44.57111876559696384 ) ) ;
#10463=DIRECTION ( 'NONE',  ( -1.000000000000000000, -0.000000000000000000, -0.000000000000000000 ) ) ;
#10465=EDGE_LOOP ( 'NONE', ( #4412, #17248, #6449, #14610 ) ) ;
#10467=LINE ( 'NONE', #15326, #8994 ) ;
#10468=DIRECTION ( 'NONE',  ( 1.000000000000000000, 0.000000000000000000, 0.000000000000000000 ) ) ;
#10469=VERTEX_POINT ( 'NONE', #12059 ) ;
#10471=FACE_OUTER_BOUND ( 'NONE', #11686, .T. ) ;
#10472=CIRCLE ( 'NONE', #16466, 44.99999999999999289 ) ;
#10473=AXIS2_PLACEMENT_3D ( 'NONE', #11700, #10026, #19988 ) ;
#10474=EDGE_LOOP ( 'NONE', ( #13815, #14245, #14417, #13535 ) ) ;
#10475=CARTESIAN_POINT ( 'NONE',  ( 5.000000000000000000, -78.80192417387952730, 39.16958956249271040 ) ) ;
#10476=VERTEX_POINT ( 'NONE', #3663 ) ;
#10479=CARTESIAN_POINT ( 'NONE',  ( -10.00000000000000000, 0.000000000000000000, 0.000000000000000000 ) ) ;
#10480=DIRECTION ( 'NONE',  ( 0.000000000000000000, -0.9510565162951503115, -0.3090169943749573878 ) ) ;
#10481=CARTESIAN_POINT ( 'NONE',  ( 0.000000000000000000, -84.80486432185169576, -36.94008646920480743 ) ) ;
#10484=CIRCLE ( 'NONE', #19666, 44.99999999999999289 ) ;
#10485=CYLINDRICAL_SURFACE ( 'NONE', #15266, 44.99999999999999289 ) ;
#10486=CIRCLE ( 'NONE', #10125, 92.50100000000000477 ) ;
#10487=DIRECTION ( 'NONE',  ( 0.000000000000000000, 0.000000000000000000, 1.000000000000000000 ) ) ;
#10489=AXIS2_PLACEMENT_3D ( 'NONE', #15322, #16768, #11801 ) ;
#10492=EDGE_CURVE ( 'NONE', #12605, #4009, #17151, .T. ) ;
#10493=ORIENTED_EDGE ( 'NONE', *, *, #19905, .F. ) ;
#10497=EDGE_CURVE ( 'NONE', #6423, #10755, #10834, .T. ) ;
#10498=VERTEX_POINT ( 'NONE', #4103 ) ;
#10499=CIRCLE ( 'NONE', #3459, 44.99999999999999289 ) ;
#10501=ORIENTED_EDGE ( 'NONE', *, *, #10962, .F. ) ;
#10502=AXIS2_PLACEMENT_3D ( 'NONE', #15642, #513, #7261 ) ;
#10503=VERTEX_POINT ( 'NONE', #17480 ) ;
#10505=CARTESIAN_POINT ( 'NONE',  ( 10.00000000000000000, 39.87723064937233630, -83.46401306393528330 ) ) ;
#10507=DIRECTION ( 'NONE',  ( -1.000000000000000000, 0.000000000000000000, 0.000000000000000000 ) ) ;
#10509=DIRECTION ( 'NONE',  ( -1.000000000000000000, -0.000000000000000000, 0.000000000000000000 ) ) ;
#10510=CARTESIAN_POINT ( 'NONE',  ( 10.00000000000000000, 91.49386717542222414, 13.61276130277023810 ) ) ;
#10514=CIRCLE ( 'NONE', #18997, 44.99999999999999289 ) ;
#10515=AXIS2_PLACEMENT_3D ( 'NONE', #2246, #5357, #383 ) ;
#10517=AXIS2_PLACEMENT_3D ( 'NONE', #4116, #17496, #2669 ) ;
#10519=CIRCLE ( 'NONE', #5960, 44.99999999999999289 ) ;
#10520=LINE ( 'NONE', #3349, #16168 ) ;
#10522=ORIENTED_EDGE ( 'NONE', *, *, #10676, .F. ) ;
#10523=FACE_OUTER_BOUND ( 'NONE', #7835, .T. ) ;
#10524=ORIENTED_EDGE ( 'NONE', *, *, #5811, .F. ) ;
#10525=EDGE_CURVE ( 'NONE', #14824, #1075, #9066, .T. ) ;
#10526=AXIS2_PLACEMENT_3D ( 'NONE', #20863, #12572, #5732 ) ;
#10530=ORIENTED_EDGE ( 'NONE', *, *, #19205, .T. ) ;
#10533=VECTOR ( 'NONE', #13350, 1000.000000000000000 ) ;
#10534=CARTESIAN_POINT ( 'NONE',  ( 5.000000000000000000, -75.87763420127865288, 44.57111876559696384 ) ) ;
#10539=DIRECTION ( 'NONE',  ( 0.000000000000000000, -3.376928366568185319E-14, -1.000000000000000000 ) ) ;
#10540=DIRECTION ( 'NONE',  ( 1.000000000000000000, 0.000000000000000000, 0.000000000000000000 ) ) ;
#10548=CIRCLE ( 'NONE', #13735, 88.00000000000000000 ) ;
#10550=AXIS2_PLACEMENT_3D ( 'NONE', #15307, #2157, #13867 ) ;
#10551=ORIENTED_EDGE ( 'NONE', *, *, #14057, .T. ) ;
#10553=CIRCLE ( 'NONE', #5612, 88.00000000000000000 ) ;
#10554=CARTESIAN_POINT ( 'NONE',  ( 10.00000000000000000, 0.000000000000000000, 0.000000000000000000 ) ) ;
#10555=ORIENTED_EDGE ( 'NONE', *, *, #4967, .F. ) ;
#10556=DIRECTION ( 'NONE',  ( -1.000000000000000000, 0.000000000000000000, 0.000000000000000000 ) ) ;
#10557=DIRECTION ( 'NONE',  ( 0.000000000000000000, 0.000000000000000000, 1.000000000000000000 ) ) ;
#10559=SURFACE_STYLE_USAGE ( .BOTH. , #12535 ) ;
#10561=VERTEX_POINT ( 'NONE', #10618 ) ;
#10562=EDGE_LOOP ( 'NONE', ( #4683, #2161, #7408, #1291 ) ) ;
#10563=ORIENTED_EDGE ( 'NONE', *, *, #3671, .T. ) ;
#10566=ADVANCED_FACE ( 'NONE', ( #12597 ), #12381, .F. ) ;
#10569=AXIS2_PLACEMENT_3D ( 'NONE', #3452, #8530, #1687 ) ;
#10570=DIRECTION ( 'NONE',  ( -1.000000000000000000, 0.000000000000000000, -0.000000000000000000 ) ) ;
#10571=FACE_OUTER_BOUND ( 'NONE', #1532, .T. ) ;
#10572=DIRECTION ( 'NONE',  ( 0.000000000000000000, 0.5877852522924742473, -0.8090169943749465631 ) ) ;
#10576=CARTESIAN_POINT ( 'NONE',  ( 10.00000000000000000, 84.80486432185190893, 36.94008646920423899 ) ) ;
#10579=DIRECTION ( 'NONE',  ( 0.000000000000000000, 0.9702957262759972501, -0.2419218955996649267 ) ) ;
#10581=DIRECTION ( 'NONE',  ( 0.000000000000000000, 0.8660254037844398178, -0.4999999999999979461 ) ) ;
#10582=DIRECTION ( 'NONE',  ( -1.000000000000000000, 0.000000000000000000, -0.000000000000000000 ) ) ;
#10585=ORIENTED_EDGE ( 'NONE', *, *, #552, .T. ) ;
#10588=ORIENTED_EDGE ( 'NONE', *, *, #13906, .F. ) ;
#10591=EDGE_CURVE ( 'NONE', #5623, #13276, #9702, .T. ) ;
#10592=ORIENTED_EDGE ( 'NONE', *, *, #5811, .T. ) ;
#10594=CARTESIAN_POINT ( 'NONE',  ( 0.000000000000000000, -89.12061559554315693, -24.77803214283632371 ) ) ;
#10595=DIRECTION ( 'NONE',  ( 1.000000000000000000, 0.000000000000000000, 0.000000000000000000 ) ) ;
#10596=DIRECTION ( 'NONE',  ( -1.000000000000000000, -0.000000000000000000, -0.000000000000000000 ) ) ;
#10601=CIRCLE ( 'NONE', #9888, 45.00000000000000711 ) ;
#10602=DIRECTION ( 'NONE',  ( 1.000000000000000000, 0.000000000000000000, 0.000000000000000000 ) ) ;
#10603=CARTESIAN_POINT ( 'NONE',  ( 10.00000000000000000, 0.000000000000000000, 0.000000000000000000 ) ) ;
#10604=VERTEX_POINT ( 'NONE', #2011 ) ;
#10605=DIRECTION ( 'NONE',  ( 0.000000000000000000, 0.000000000000000000, 1.000000000000000000 ) ) ;
#10606=ORIENTED_EDGE ( 'NONE', *, *, #3518, .T. ) ;
#10607=ORIENTED_EDGE ( 'NONE', *, *, #10361, .F. ) ;
#10608=ORIENTED_EDGE ( 'NONE', *, *, #19588, .F. ) ;
#10609=CARTESIAN_POINT ( 'NONE',  ( 5.000000000000000000, 83.48638250753229784, 27.82128566055142826 ) ) ;
#10610=ORIENTED_EDGE ( 'NONE', *, *, #20677, .F. ) ;
#10611=VECTOR ( 'NONE', #10383, 1000.000000000000000 ) ;
#10612=VERTEX_POINT ( 'NONE', #20888 ) ;
#10613=EDGE_CURVE ( 'NONE', #49, #5365, #8666, .T. ) ;
#10614=DIRECTION ( 'NONE',  ( 0.000000000000000000, -0.7880107536067146867, -0.6156614753256676176 ) ) ;
#10615=ORIENTED_EDGE ( 'NONE', *, *, #5147, .T. ) ;
#10617=CARTESIAN_POINT ( 'NONE',  ( 10.00000000000000000, 90.63195040374210976, -18.50093422002330712 ) ) ;
#10618=CARTESIAN_POINT ( 'NONE',  ( 0.000000000000000000, -83.48638250753209888, -27.82128566055197538 ) ) ;
#10619=CARTESIAN_POINT ( 'NONE',  ( 10.00000000000000000, -69.25892805976543798, 49.38005998797819274 ) ) ;
#10620=LINE ( 'NONE', #12599, #590 ) ;
#10621=FACE_OUTER_BOUND ( 'NONE', #19177, .T. ) ;
#10622=LINE ( 'NONE', #13616, #21374 ) ;
#10624=CIRCLE ( 'NONE', #16976, 44.99999999999999289 ) ;
#10625=EDGE_LOOP ( 'NONE', ( #14221, #5347, #4138, #13251 ) ) ;
#10626=DIRECTION ( 'NONE',  ( 1.000000000000000000, 0.000000000000000000, 0.000000000000000000 ) ) ;
#10627=DIRECTION ( 'NONE',  ( 0.000000000000000000, 0.000000000000000000, 1.000000000000000000 ) ) ;
#10631=DIRECTION ( 'NONE',  ( 0.000000000000000000, 0.000000000000000000, 1.000000000000000000 ) ) ;
#10633=EDGE_CURVE ( 'NONE', #1387, #21723, #20320, .T. ) ;
#10637=DIRECTION ( 'NONE',  ( -1.000000000000000000, 0.000000000000000000, 0.000000000000000000 ) ) ;
#10638=LINE ( 'NONE', #15613, #9330 ) ;
#10640=CARTESIAN_POINT ( 'NONE',  ( 0.000000000000000000, 0.000000000000000000, 0.000000000000000000 ) ) ;
#10641=DIRECTION ( 'NONE',  ( 0.000000000000000000, -0.3420201433256757073, 0.9396926207859058744 ) ) ;
#10642=EDGE_CURVE ( 'NONE', #12774, #21645, #3025, .T. ) ;
#10644=DIRECTION ( 'NONE',  ( 0.000000000000000000, 0.000000000000000000, 1.000000000000000000 ) ) ;
#10645=LINE ( 'NONE', #280, #19456 ) ;
#10647=DIRECTION ( 'NONE',  ( 0.000000000000000000, 0.000000000000000000, 1.000000000000000000 ) ) ;
#10648=EDGE_CURVE ( 'NONE', #5893, #10454, #4795, .T. ) ;
#10649=EDGE_LOOP ( 'NONE', ( #9506, #18324, #3069, #21671 ) ) ;
#10650=DIRECTION ( 'NONE',  ( 0.000000000000000000, -0.5299192642332118952, 0.8480480961564216269 ) ) ;
#10651=EDGE_LOOP ( 'NONE', ( #904, #764, #3531, #15526 ) ) ;
#10652=DIRECTION ( 'NONE',  ( 1.000000000000000000, 0.000000000000000000, 0.000000000000000000 ) ) ;
#10653=AXIS2_PLACEMENT_3D ( 'NONE', #678, #5436, #571 ) ;
#10654=CARTESIAN_POINT ( 'NONE',  ( 10.00000000000000000, -57.53593069156319473, -72.42963261301021305 ) ) ;
#10655=ORIENTED_EDGE ( 'NONE', *, *, #14233, .F. ) ;
#10659=ORIENTED_EDGE ( 'NONE', *, *, #9812, .T. ) ;
#10661=ORIENTED_EDGE ( 'NONE', *, *, #7050, .T. ) ;
#10662=ADVANCED_FACE ( 'NONE', ( #14586 ), #21323, .F. ) ;
#10664=VECTOR ( 'NONE', #1523, 1000.000000000000000 ) ;
#10665=ORIENTED_EDGE ( 'NONE', *, *, #4884, .T. ) ;
#10666=ADVANCED_FACE ( 'NONE', ( #14485 ), #11278, .F. ) ;
#10667=CARTESIAN_POINT ( 'NONE',  ( 0.000000000000000000, 0.000000000000000000, 0.000000000000000000 ) ) ;
#10670=DIRECTION ( 'NONE',  ( -1.000000000000000000, -0.000000000000000000, -0.000000000000000000 ) ) ;
#10673=DIRECTION ( 'NONE',  ( 0.000000000000000000, 0.000000000000000000, 1.000000000000000000 ) ) ;
#10675=DIRECTION ( 'NONE',  ( 1.000000000000000000, -0.000000000000000000, -0.000000000000000000 ) ) ;
#10676=EDGE_CURVE ( 'NONE', #9950, #20418, #21016, .T. ) ;
#10679=DIRECTION ( 'NONE',  ( 0.000000000000000000, 0.2079116908177598144, -0.9781476007338055778 ) ) ;
#10680=CIRCLE ( 'NONE', #21633, 44.99999999999999289 ) ;
#10681=EDGE_CURVE ( 'NONE', #21786, #827, #10769, .T. ) ;
#10682=DIRECTION ( 'NONE',  ( 0.000000000000000000, 0.000000000000000000, 1.000000000000000000 ) ) ;
#10684=DIRECTION ( 'NONE',  ( -1.000000000000000000, -0.000000000000000000, -0.000000000000000000 ) ) ;
#10686=CARTESIAN_POINT ( 'NONE',  ( 10.00000000000000000, 86.66425444033919234, 32.33793443156426406 ) ) ;
#10687=ORIENTED_EDGE ( 'NONE', *, *, #14313, .F. ) ;
#10688=AXIS2_PLACEMENT_3D ( 'NONE', #17559, #17775, #12904 ) ;
#10690=VERTEX_POINT ( 'NONE', #12924 ) ;
#10692=ORIENTED_EDGE ( 'NONE', *, *, #2082, .F. ) ;
#10693=DIRECTION ( 'NONE',  ( 0.000000000000000000, 0.000000000000000000, 1.000000000000000000 ) ) ;
#10695=EDGE_CURVE ( 'NONE', #5372, #18178, #19863, .T. ) ;
#10696=DIRECTION ( 'NONE',  ( 1.000000000000000000, 0.000000000000000000, 0.000000000000000000 ) ) ;
#10697=DIRECTION ( 'NONE',  ( 0.000000000000000000, 0.000000000000000000, 1.000000000000000000 ) ) ;
#10698=AXIS2_PLACEMENT_3D ( 'NONE', #13747, #5458, #10631 ) ;
#10701=DIRECTION ( 'NONE',  ( -1.000000000000000000, -0.000000000000000000, -0.000000000000000000 ) ) ;
#10702=DIRECTION ( 'NONE',  ( -1.000000000000000000, -0.000000000000000000, -0.000000000000000000 ) ) ;
#10703=CARTESIAN_POINT ( 'NONE',  ( 0.000000000000000000, -29.47587714451095309, 82.91666097089111531 ) ) ;
#10704=EDGE_CURVE ( 'NONE', #2939, #19686, #1157, .T. ) ;
#10706=ORIENTED_EDGE ( 'NONE', *, *, #3689, .T. ) ;
#10707=EDGE_CURVE ( 'NONE', #1807, #10390, #3630, .T. ) ;
#10710=ORIENTED_EDGE ( 'NONE', *, *, #12564, .F. ) ;
#10712=EDGE_CURVE ( 'NONE', #1586, #7680, #1222, .T. ) ;
#10713=AXIS2_PLACEMENT_3D ( 'NONE', #10996, #17744, #19175 ) ;
#10714=EDGE_CURVE ( 'NONE', #18181, #1305, #13040, .T. ) ;
#10716=LINE ( 'NONE', #17255, #16259 ) ;
#10717=VERTEX_POINT ( 'NONE', #9711 ) ;
#10718=ORIENTED_EDGE ( 'NONE', *, *, #6819, .T. ) ;
#10719=DIRECTION ( 'NONE',  ( -1.000000000000000000, 0.000000000000000000, -0.000000000000000000 ) ) ;
#10721=ORIENTED_EDGE ( 'NONE', *, *, #1774, .T. ) ;
#10723=CYLINDRICAL_SURFACE ( 'NONE', #18451, 92.50100000000000477 ) ;
#10729=CARTESIAN_POINT ( 'NONE',  ( 0.000000000000000000, 61.33825423015778711, -69.23910433415882437 ) ) ;
#10731=DIRECTION ( 'NONE',  ( 1.000000000000000000, 0.000000000000000000, 0.000000000000000000 ) ) ;
#10732=EDGE_LOOP ( 'NONE', ( #6104, #14576, #21292, #11013 ) ) ;
#10734=AXIS2_PLACEMENT_3D ( 'NONE', #17511, #16171, #2248 ) ;
#10736=AXIS2_PLACEMENT_3D ( 'NONE', #5676, #12401, #19150 ) ;
#10738=VERTEX_POINT ( 'NONE', #13142 ) ;
#10739=CARTESIAN_POINT ( 'NONE',  ( 10.00000000000000000, -87.96697768756401103, -2.410567674971490604 ) ) ;
#10740=EDGE_LOOP ( 'NONE', ( #63, #9239, #14031, #8623 ) ) ;
#10741=AXIS2_PLACEMENT_3D ( 'NONE', #4127, #7226, #15729 ) ;
#10742=DIRECTION ( 'NONE',  ( -1.000000000000000000, -0.000000000000000000, -0.000000000000000000 ) ) ;
#10743=EDGE_LOOP ( 'NONE', ( #12776, #17638, #20909, #4529 ) ) ;
#10744=ORIENTED_EDGE ( 'NONE', *, *, #6921, .F. ) ;
#10745=DIRECTION ( 'NONE',  ( -1.000000000000000000, -0.000000000000000000, -0.000000000000000000 ) ) ;
#10747=CARTESIAN_POINT ( 'NONE',  ( 0.000000000000000000, 0.000000000000000000, 0.000000000000000000 ) ) ;
#10748=FACE_OUTER_BOUND ( 'NONE', #5304, .T. ) ;
#10749=CARTESIAN_POINT ( 'NONE',  ( 10.00000000000000000, 60.65655256511316651, -59.63197188857461128 ) ) ;
#10752=DIRECTION ( 'NONE',  ( -1.000000000000000000, 0.000000000000000000, 0.000000000000000000 ) ) ;
#10753=CARTESIAN_POINT ( 'NONE',  ( 10.00000000000000000, -61.71252885873428085, 58.53847642588571887 ) ) ;
#10755=VERTEX_POINT ( 'NONE', #19889 ) ;
#10758=EDGE_CURVE ( 'NONE', #11402, #16302, #8571, .T. ) ;
#10761=ORIENTED_EDGE ( 'NONE', *, *, #16125, .T. ) ;
#10765=AXIS2_PLACEMENT_3D ( 'NONE', #10850, #1022, #14062 ) ;
#10766=VERTEX_POINT ( 'NONE', #21117 ) ;
#10767=ADVANCED_FACE ( 'NONE', ( #8293 ), #3203, .F. ) ;
#10768=AXIS2_PLACEMENT_3D ( 'NONE', #12336, #15433, #10245 ) ;
#10769=CIRCLE ( 'NONE', #1260, 92.50100000000000477 ) ;
#10773=CARTESIAN_POINT ( 'NONE',  ( 10.00000000000000000, -80.18694381077088451, -28.37681241246736974 ) ) ;
#10774=DIRECTION ( 'NONE',  ( -1.000000000000000000, -0.000000000000000000, 0.000000000000000000 ) ) ;
#10776=DIRECTION ( 'NONE',  ( -1.000000000000000000, -0.000000000000000000, 0.000000000000000000 ) ) ;
#10777=DIRECTION ( 'NONE',  ( 1.000000000000000000, 0.000000000000000000, -0.000000000000000000 ) ) ;
#10778=DIRECTION ( 'NONE',  ( 0.000000000000000000, 8.866364432770350877E-15, -1.000000000000000000 ) ) ;
#10779=CARTESIAN_POINT ( 'NONE',  ( 10.00000000000000000, 0.000000000000000000, 0.000000000000000000 ) ) ;
#10780=CARTESIAN_POINT ( 'NONE',  ( 5.000000000000002665, -5.479102470011078196, 87.82926298292112222 ) ) ;
#10784=AXIS2_PLACEMENT_3D ( 'NONE', #2571, #9300, #10863 ) ;
#10785=CARTESIAN_POINT ( 'NONE',  ( 10.00000000000000000, 0.000000000000000000, 0.000000000000000000 ) ) ;
#10786=CIRCLE ( 'NONE', #10444, 44.99999999999999289 ) ;
#10787=DIRECTION ( 'NONE',  ( 1.000000000000000000, 0.000000000000000000, 0.000000000000000000 ) ) ;
#10788=EDGE_CURVE ( 'NONE', #12373, #19614, #8611, .T. ) ;
#10790=DIRECTION ( 'NONE',  ( 0.000000000000000000, 0.8987940462991649282, 0.4383711467890814562 ) ) ;
#10792=DIRECTION ( 'NONE',  ( -1.000000000000000000, 0.000000000000000000, 0.000000000000000000 ) ) ;
#10795=ORIENTED_EDGE ( 'NONE', *, *, #4326, .F. ) ;
#10796=ORIENTED_EDGE ( 'NONE', *, *, #15668, .F. ) ;
#10799=CARTESIAN_POINT ( 'NONE',  ( 10.00000000000000000, -35.34277389771474986, -85.48288328206420772 ) ) ;
#10800=VECTOR ( 'NONE', #1690, 1000.000000000000000 ) ;
#10801=ORIENTED_EDGE ( 'NONE', *, *, #6624, .F. ) ;
#10802=EDGE_CURVE ( 'NONE', #1305, #447, #19148, .T. ) ;
#10803=CARTESIAN_POINT ( 'NONE',  ( -10.00000000000000000, 0.000000000000000000, 0.000000000000000000 ) ) ;
#10805=LINE ( 'NONE', #3749, #5753 ) ;
#10807=EDGE_CURVE ( 'NONE', #16218, #20085, #11035, .T. ) ;
#10808=DIRECTION ( 'NONE',  ( -1.000000000000000000, 0.000000000000000000, 0.000000000000000000 ) ) ;
#10809=DIRECTION ( 'NONE',  ( 1.000000000000000000, 0.000000000000000000, 0.000000000000000000 ) ) ;
#10810=CARTESIAN_POINT ( 'NONE',  ( 10.00000000000000000, 64.66851233300727131, 55.25552418572984692 ) ) ;
#10811=FACE_OUTER_BOUND ( 'NONE', #1617, .T. ) ;
#10813=EDGE_CURVE ( 'NONE', #12455, #19953, #21630, .T. ) ;
#10815=VECTOR ( 'NONE', #10582, 1000.000000000000000 ) ;
#10816=EDGE_CURVE ( 'NONE', #2214, #6618, #6649, .T. ) ;
#10819=ORIENTED_EDGE ( 'NONE', *, *, #2207, .F. ) ;
#10822=ORIENTED_EDGE ( 'NONE', *, *, #13098, .T. ) ;
#10824=VERTEX_POINT ( 'NONE', #9937 ) ;
#10826=DIRECTION ( 'NONE',  ( -1.000000000000000000, 0.000000000000000000, 0.000000000000000000 ) ) ;
#10828=ORIENTED_EDGE ( 'NONE', *, *, #12289, .F. ) ;
#10829=AXIS2_PLACEMENT_3D ( 'NONE', #21286, #7484, #4053 ) ;
#10830=ADVANCED_FACE ( 'NONE', ( #21654 ), #1443, .F. ) ;
#10832=CIRCLE ( 'NONE', #21424, 44.99999999999999289 ) ;
#10834=LINE ( 'NONE', #18918, #11127 ) ;
#10835=DIRECTION ( 'NONE',  ( 0.000000000000000000, 0.000000000000000000, 1.000000000000000000 ) ) ;
#10837=EDGE_CURVE ( 'NONE', #215, #8987, #10329, .T. ) ;
#10838=CARTESIAN_POINT ( 'NONE',  ( 10.00000000000000000, -2.208823992043557283, -85.03123271466938604 ) ) ;
#10839=DIRECTION ( 'NONE',  ( 0.000000000000000000, 0.4694715627858917495, -0.8829475928589264333 ) ) ;
#10840=CARTESIAN_POINT ( 'NONE',  ( 10.00000000000000000, 52.25832601289194201, -70.80301803122729609 ) ) ;
#10844=ADVANCED_FACE ( 'NONE', ( #18359 ), #8407, .F. ) ;
#10846=VECTOR ( 'NONE', #3406, 1000.000000000000000 ) ;
#10847=DIRECTION ( 'NONE',  ( 0.000000000000000000, 0.2079116908177531808, 0.9781476007338069101 ) ) ;
#10848=DIRECTION ( 'NONE',  ( 0.000000000000000000, 0.000000000000000000, 1.000000000000000000 ) ) ;
#10850=CARTESIAN_POINT ( 'NONE',  ( 10.00000000000000000, -51.76708072107932423, 67.49339815138475274 ) ) ;
#10851=EDGE_LOOP ( 'NONE', ( #6224, #12286, #4392, #7412 ) ) ;
#10853=DIRECTION ( 'NONE',  ( 1.000000000000000000, 0.000000000000000000, -0.000000000000000000 ) ) ;
#10854=ORIENTED_EDGE ( 'NONE', *, *, #20959, .T. ) ;
#10855=VERTEX_POINT ( 'NONE', #11712 ) ;
#10856=DIRECTION ( 'NONE',  ( -1.000000000000000000, -0.000000000000000000, -0.000000000000000000 ) ) ;
#10863=DIRECTION ( 'NONE',  ( 0.000000000000000000, -0.4694715627858974671, 0.8829475928589232137 ) ) ;
#10865=CARTESIAN_POINT ( 'NONE',  ( 10.00000000000000000, 36.60317927562682883, -76.78148674856727496 ) ) ;
#10866=AXIS2_PLACEMENT_3D ( 'NONE', #3669, #12281, #19035 ) ;
#10868=DIRECTION ( 'NONE',  ( -1.000000000000000000, -0.000000000000000000, -0.000000000000000000 ) ) ;
#10869=CARTESIAN_POINT ( 'NONE',  ( 10.00000000000000000, -25.56104204395359503, 81.12843256239655432 ) ) ;
#10871=ORIENTED_EDGE ( 'NONE', *, *, #13836, .F. ) ;
#10872=DIRECTION ( 'NONE',  ( -1.000000000000000000, 0.000000000000000000, 0.000000000000000000 ) ) ;
#10875=ORIENTED_EDGE ( 'NONE', *, *, #14704, .T. ) ;
#10876=CIRCLE ( 'NONE', #13709, 44.99999999999999289 ) ;
#10878=AXIS2_PLACEMENT_3D ( 'NONE', #10032, #7862, #8393 ) ;
#10879=AXIS2_PLACEMENT_3D ( 'NONE', #3622, #16669, #10145 ) ;
#10880=DIRECTION ( 'NONE',  ( -1.000000000000000000, 0.000000000000000000, 0.000000000000000000 ) ) ;
#10881=AXIS2_PLACEMENT_3D ( 'NONE', #18032, #19894, #20014 ) ;
#10882=VERTEX_POINT ( 'NONE', #10049 ) ;
#10883=ORIENTED_EDGE ( 'NONE', *, *, #15351, .T. ) ;
#10886=CARTESIAN_POINT ( 'NONE',  ( 10.00000000000000000, 0.000000000000000000, -88.00000000000000000 ) ) ;
#10887=DIRECTION ( 'NONE',  ( 1.000000000000000000, 0.000000000000000000, 0.000000000000000000 ) ) ;
#10889=CARTESIAN_POINT ( 'NONE',  ( 10.00000000000000000, -46.07110168784768689, -74.97635353408431058 ) ) ;
#10890=FACE_OUTER_BOUND ( 'NONE', #1553, .T. ) ;
#10891=CARTESIAN_POINT ( 'NONE',  ( 10.00000000000000000, -45.60224695560514618, -80.47900393021774335 ) ) ;
#10892=VECTOR ( 'NONE', #21279, 1000.000000000000000 ) ;
#10893=DIRECTION ( 'NONE',  ( 0.000000000000000000, 0.2756373558169933902, 0.9612616959383204485 ) ) ;
#10894=CARTESIAN_POINT ( 'NONE',  ( 0.000000000000000000, 87.96697768756401103, -2.410567674970879981 ) ) ;
#10896=AXIS2_PLACEMENT_3D ( 'NONE', #7598, #4388, #15984 ) ;
#10898=ORIENTED_EDGE ( 'NONE', *, *, #19010, .F. ) ;
#10901=DIRECTION ( 'NONE',  ( 0.000000000000000000, 0.000000000000000000, -1.000000000000000000 ) ) ;
#10903=DIRECTION ( 'NONE',  ( 0.000000000000000000, 0.000000000000000000, 1.000000000000000000 ) ) ;
#10904=ORIENTED_EDGE ( 'NONE', *, *, #19673, .T. ) ;
#10905=CARTESIAN_POINT ( 'NONE',  ( 10.00000000000000000, 90.63195040374188238, 18.50093422002450083 ) ) ;
#10906=ORIENTED_EDGE ( 'NONE', *, *, #16150, .T. ) ;
#10907=DIRECTION ( 'NONE',  ( -1.000000000000000000, 0.000000000000000000, 0.000000000000000000 ) ) ;
#10908=EDGE_LOOP ( 'NONE', ( #16596, #17555, #4689, #11416 ) ) ;
#10910=CIRCLE ( 'NONE', #21509, 45.00000000000000000 ) ;
#10911=ORIENTED_EDGE ( 'NONE', *, *, #992, .F. ) ;
#10913=DIRECTION ( 'NONE',  ( -1.000000000000000000, -0.000000000000000000, 0.000000000000000000 ) ) ;
#10914=AXIS2_PLACEMENT_3D ( 'NONE', #14798, #9807, #6416 ) ;
#10915=EDGE_LOOP ( 'NONE', ( #2701, #6315, #10434, #16871 ) ) ;
#10917=LINE ( 'NONE', #3961, #16412 ) ;
#10920=FACE_OUTER_BOUND ( 'NONE', #20079, .T. ) ;
#10922=DIRECTION ( 'NONE',  ( 1.000000000000000000, 0.000000000000000000, 0.000000000000000000 ) ) ;
#10923=LINE ( 'NONE', #18008, #3704 ) ;
#10924=ADVANCED_FACE ( 'NONE', ( #11936 ), #3538, .F. ) ;
#10926=FACE_OUTER_BOUND ( 'NONE', #9541, .T. ) ;
#10928=AXIS2_PLACEMENT_3D ( 'NONE', #17983, #2835, #8142 ) ;
#10929=DIRECTION ( 'NONE',  ( 0.000000000000000000, 0.000000000000000000, 1.000000000000000000 ) ) ;
#10934=ORIENTED_EDGE ( 'NONE', *, *, #17805, .F. ) ;
#10935=ORIENTED_EDGE ( 'NONE', *, *, #3887, .T. ) ;
#10936=CYLINDRICAL_SURFACE ( 'NONE', #6659, 88.00000000000000000 ) ;
#10937=ADVANCED_FACE ( 'NONE', ( #654 ), #10485, .F. ) ;
#10938=VERTEX_POINT ( 'NONE', #18783 ) ;
#10939=EDGE_CURVE ( 'NONE', #6904, #16928, #15465, .T. ) ;
#10940=EDGE_CURVE ( 'NONE', #7162, #9877, #7501, .T. ) ;
#10943=DIRECTION ( 'NONE',  ( 1.000000000000000000, 0.000000000000000000, 0.000000000000000000 ) ) ;
#10945=DIRECTION ( 'NONE',  ( 0.000000000000000000, 0.3420201433256693235, -0.9396926207859080948 ) ) ;
#10946=FACE_OUTER_BOUND ( 'NONE', #21400, .T. ) ;
#10949=CARTESIAN_POINT ( 'NONE',  ( 5.000000000000002665, 35.18804927320642406, -80.65854690202642985 ) ) ;
#10950=DIRECTION ( 'NONE',  ( 1.000000000000000000, 0.000000000000000000, 0.000000000000000000 ) ) ;
#10951=ORIENTED_EDGE ( 'NONE', *, *, #7094, .F. ) ;
#10952=CYLINDRICAL_SURFACE ( 'NONE', #17846, 88.00000000000000000 ) ;
#10953=ADVANCED_FACE ( 'NONE', ( #13907 ), #17561, .F. ) ;
#10955=CYLINDRICAL_SURFACE ( 'NONE', #21449, 88.00000000000000000 ) ;
#10956=ADVANCED_FACE ( 'NONE', ( #17346 ), #5740, .F. ) ;
#10957=DIRECTION ( 'NONE',  ( 0.000000000000000000, -2.698458740408367555E-15, -1.000000000000000000 ) ) ;
#10958=EDGE_LOOP ( 'NONE', ( #2031, #12696, #7794, #4944 ) ) ;
#10959=CYLINDRICAL_SURFACE ( 'NONE', #10765, 44.99999999999998579 ) ;
#10960=ORIENTED_EDGE ( 'NONE', *, *, #19827, .F. ) ;
#10961=ORIENTED_EDGE ( 'NONE', *, *, #9584, .F. ) ;
#10962=EDGE_CURVE ( 'NONE', #18043, #9349, #2567, .T. ) ;
#10964=LINE ( 'NONE', #21143, #3996 ) ;
#10965=VECTOR ( 'NONE', #4817, 1000.000000000000000 ) ;
#10966=ORIENTED_EDGE ( 'NONE', *, *, #16658, .F. ) ;
#10967=EDGE_LOOP ( 'NONE', ( #3825, #15957, #538, #4617 ) ) ;
#10968=CARTESIAN_POINT ( 'NONE',  ( 10.00000000000000000, -75.45728100697627383, 39.26051685139039193 ) ) ;
#10969=DIRECTION ( 'NONE',  ( 0.000000000000000000, 0.000000000000000000, 1.000000000000000000 ) ) ;
#10970=EDGE_CURVE ( 'NONE', #13683, #2527, #15627, .T. ) ;
#10971=DIRECTION ( 'NONE',  ( -1.000000000000000000, -0.000000000000000000, -0.000000000000000000 ) ) ;
#10973=DIRECTION ( 'NONE',  ( 0.000000000000000000, 0.000000000000000000, 1.000000000000000000 ) ) ;
#10975=DIRECTION ( 'NONE',  ( 0.000000000000000000, -0.2756373558169869509, -0.9612616959383223358 ) ) ;
#10976=CYLINDRICAL_SURFACE ( 'NONE', #6837, 44.99999999999999289 ) ;
#10978=LINE ( 'NONE', #17835, #11571 ) ;
#10979=ORIENTED_EDGE ( 'NONE', *, *, #6381, .T. ) ;
#10980=CARTESIAN_POINT ( 'NONE',  ( 10.00000000000000000, 71.72924546249947753, 45.71766382684695884 ) ) ;
#10981=ADVANCED_FACE ( 'NONE', ( #7293 ), #4079, .F. ) ;
#10982=VERTEX_POINT ( 'NONE', #437 ) ;
#10983=ADVANCED_FACE ( 'NONE', ( #8930 ), #20767, .F. ) ;
#10987=AXIS2_PLACEMENT_3D ( 'NONE', #3590, #18736, #15520 ) ;
#10990=CARTESIAN_POINT ( 'NONE',  ( 10.00000000000000000, 0.000000000000000000, 0.000000000000000000 ) ) ;
#10991=EDGE_LOOP ( 'NONE', ( #14783, #5836, #3246, #3240 ) ) ;
#10992=ADVANCED_FACE ( 'NONE', ( #8729 ), #12142, .F. ) ;
#10993=ORIENTED_EDGE ( 'NONE', *, *, #14464, .T. ) ;
#10994=VERTEX_POINT ( 'NONE', #15675 ) ;
#10995=ORIENTED_EDGE ( 'NONE', *, *, #13422, .F. ) ;
#10996=CARTESIAN_POINT ( 'NONE',  ( 0.000000000000000000, 32.56745702629739014, 78.57830605990665163 ) ) ;
#10999=LINE ( 'NONE', #19291, #12853 ) ;
#11002=DIRECTION ( 'NONE',  ( 1.000000000000000000, 0.000000000000000000, 0.000000000000000000 ) ) ;
#11003=DIRECTION ( 'NONE',  ( 1.000000000000000000, 0.000000000000000000, 0.000000000000000000 ) ) ;
#11004=VERTEX_POINT ( 'NONE', #5634 ) ;
#11005=CYLINDRICAL_SURFACE ( 'NONE', #9855, 44.99999999999999289 ) ;
#11008=ORIENTED_EDGE ( 'NONE', *, *, #13366, .F. ) ;
#11009=AXIS2_PLACEMENT_3D ( 'NONE', #18618, #3584, #3362 ) ;
#11010=DIRECTION ( 'NONE',  ( -1.000000000000000000, 0.000000000000000000, 0.000000000000000000 ) ) ;
#11011=ORIENTED_EDGE ( 'NONE', *, *, #6995, .T. ) ;
#11012=CARTESIAN_POINT ( 'NONE',  ( 10.00000000000000000, 88.70892494636771630, -26.21376805916497332 ) ) ;
#11013=ORIENTED_EDGE ( 'NONE', *, *, #12275, .T. ) ;
#11014=ORIENTED_EDGE ( 'NONE', *, *, #14459, .F. ) ;
#11018=DIRECTION ( 'NONE',  ( -1.000000000000000000, -0.000000000000000000, 0.000000000000000000 ) ) ;
#11020=CARTESIAN_POINT ( 'NONE',  ( 5.000000000000000000, -81.34229909304657724, -33.57723005635448743 ) ) ;
#11021=CYLINDRICAL_SURFACE ( 'NONE', #5406, 92.50100000000000477 ) ;
#11022=DIRECTION ( 'NONE',  ( -1.000000000000000000, -0.000000000000000000, -0.000000000000000000 ) ) ;
#11024=DIRECTION ( 'NONE',  ( -1.000000000000000000, 0.000000000000000000, 0.000000000000000000 ) ) ;
#11025=DIRECTION ( 'NONE',  ( 1.000000000000000000, 0.000000000000000000, 0.000000000000000000 ) ) ;
#11026=AXIS2_PLACEMENT_3D ( 'NONE', #13562, #20318, #15214 ) ;
#11027=DIRECTION ( 'NONE',  ( 0.000000000000000000, 0.000000000000000000, 1.000000000000000000 ) ) ;
#11028=DIRECTION ( 'NONE',  ( 0.000000000000000000, 0.000000000000000000, 1.000000000000000000 ) ) ;
#11029=DIRECTION ( 'NONE',  ( 0.000000000000000000, 0.000000000000000000, 1.000000000000000000 ) ) ;
#11030=EDGE_LOOP ( 'NONE', ( #5818, #14772, #11941, #12075 ) ) ;
#11031=AXIS2_PLACEMENT_3D ( 'NONE', #8928, #7173, #17345 ) ;
#11035=CIRCLE ( 'NONE', #18103, 88.00000000000000000 ) ;
#11037=ORIENTED_EDGE ( 'NONE', *, *, #6813, .F. ) ;
#11039=CIRCLE ( 'NONE', #12441, 44.99999999999999289 ) ;
#11040=VERTEX_POINT ( 'NONE', #1398 ) ;
#11042=VERTEX_POINT ( 'NONE', #8236 ) ;
#11043=DIRECTION ( 'NONE',  ( 1.000000000000000000, 0.000000000000000000, 0.000000000000000000 ) ) ;
#11044=DIRECTION ( 'NONE',  ( -1.000000000000000000, -0.000000000000000000, -0.000000000000000000 ) ) ;
#11046=MECHANICAL_DESIGN_GEOMETRIC_PRESENTATION_REPRESENTATION('',(#5421),#7182);
#11047=CARTESIAN_POINT ( 'NONE',  ( 0.000000000000000000, 0.000000000000000000, 0.000000000000000000 ) ) ;
#11048=FACE_OUTER_BOUND ( 'NONE', #2181, .T. ) ;
#11049=DIRECTION ( 'NONE',  ( 0.000000000000000000, 0.9702957262759972501, -0.2419218955996649267 ) ) ;
#11050=LINE ( 'NONE', #9503, #19612 ) ;
#11051=DIRECTION ( 'NONE',  ( 0.000000000000000000, 0.000000000000000000, 1.000000000000000000 ) ) ;
#11053=AXIS2_PLACEMENT_3D ( 'NONE', #19949, #8027, #3157 ) ;
#11054=VERTEX_POINT ( 'NONE', #8348 ) ;
#11057=VECTOR ( 'NONE', #21576, 1000.000000000000000 ) ;
#11058=ADVANCED_FACE ( 'NONE', ( #16413 ), #14763, .F. ) ;
#11060=EDGE_CURVE ( 'NONE', #13186, #21594, #14967, .T. ) ;
#11063=EDGE_CURVE ( 'NONE', #752, #19437, #6488, .T. ) ;
#11064=DIRECTION ( 'NONE',  ( 0.000000000000000000, 0.000000000000000000, 1.000000000000000000 ) ) ;
#11066=VERTEX_POINT ( 'NONE', #21712 ) ;
#11067=FACE_OUTER_BOUND ( 'NONE', #14387, .T. ) ;
#11076=AXIS2_PLACEMENT_3D ( 'NONE', #5600, #17315, #2379 ) ;
#11078=EDGE_CURVE ( 'NONE', #17938, #2662, #8242, .T. ) ;
#11082=DIRECTION ( 'NONE',  ( 0.000000000000000000, -0.4067366430757887175, -0.9135454576426059736 ) ) ;
#11083=DIRECTION ( 'NONE',  ( 0.000000000000000000, 0.000000000000000000, 1.000000000000000000 ) ) ;
#11085=DIRECTION ( 'NONE',  ( 1.000000000000000000, -0.000000000000000000, 0.000000000000000000 ) ) ;
#11087=AXIS2_PLACEMENT_3D ( 'NONE', #10865, #14173, #20920 ) ;
#11088=ORIENTED_EDGE ( 'NONE', *, *, #4847, .T. ) ;
#11089=DIRECTION ( 'NONE',  ( 0.000000000000000000, 0.9945218953682737340, -0.1045284632676505010 ) ) ;
#11090=VECTOR ( 'NONE', #20421, 1000.000000000000000 ) ;
#11094=DIRECTION ( 'NONE',  ( 1.000000000000000000, 0.000000000000000000, 0.000000000000000000 ) ) ;
#11095=ADVANCED_FACE ( 'NONE', ( #16528 ), #19833, .F. ) ;
#11099=AXIS2_PLACEMENT_3D ( 'NONE', #14513, #21253, #19055 ) ;
#11100=VERTEX_POINT ( 'NONE', #14868 ) ;
#11101=ORIENTED_EDGE ( 'NONE', *, *, #13658, .T. ) ;
#11107=VECTOR ( 'NONE', #4395, 1000.000000000000000 ) ;
#11108=EDGE_CURVE ( 'NONE', #5155, #20330, #1287, .T. ) ;
#11110=DIRECTION ( 'NONE',  ( 1.000000000000000000, 0.000000000000000000, 0.000000000000000000 ) ) ;
#11111=CARTESIAN_POINT ( 'NONE',  ( 10.00000000000000000, 67.05625154133539922, -63.71729851637743280 ) ) ;
#11112=CARTESIAN_POINT ( 'NONE',  ( 10.00000000000000000, -84.79630770241078608, -6.691460262316255125 ) ) ;
#11113=EDGE_CURVE ( 'NONE', #12476, #18185, #17772, .T. ) ;
#11114=DIRECTION ( 'NONE',  ( 0.000000000000000000, 0.06975647374411841906, 0.9975640502598247528 ) ) ;
#11116=DIRECTION ( 'NONE',  ( 0.000000000000000000, -9.251858538542973800E-16, -1.000000000000000000 ) ) ;
#11119=EDGE_CURVE ( 'NONE', #17876, #20049, #1535, .T. ) ;
#11120=CARTESIAN_POINT ( 'NONE',  ( 10.00000000000000000, 6.797690662955227836, 87.73705831432218361 ) ) ;
#11127=VECTOR ( 'NONE', #3775, 1000.000000000000000 ) ;
#11128=ORIENTED_EDGE ( 'NONE', *, *, #3390, .T. ) ;
#11129=EDGE_CURVE ( 'NONE', #19437, #7036, #13314, .T. ) ;
#11135=EDGE_LOOP ( 'NONE', ( #18828, #1278, #6560, #14028 ) ) ;
#11136=ORIENTED_EDGE ( 'NONE', *, *, #1249, .T. ) ;
#11138=LINE ( 'NONE', #21731, #13583 ) ;
#11139=ORIENTED_EDGE ( 'NONE', *, *, #9437, .F. ) ;
#11140=DIRECTION ( 'NONE',  ( -1.000000000000000000, -0.000000000000000000, 0.000000000000000000 ) ) ;
#11141=FACE_OUTER_BOUND ( 'NONE', #2912, .T. ) ;
#11143=AXIS2_PLACEMENT_3D ( 'NONE', #9721, #14379, #21133 ) ;
#11145=AXIS2_PLACEMENT_3D ( 'NONE', #3587, #20496, #6916 ) ;
#11146=CARTESIAN_POINT ( 'NONE',  ( 10.00000000000000000, -36.60317927562628881, 76.78148674856751654 ) ) ;
#11148=DIRECTION ( 'NONE',  ( 0.000000000000000000, 0.5877852522924742473, -0.8090169943749465631 ) ) ;
#11151=ORIENTED_EDGE ( 'NONE', *, *, #19607, .F. ) ;
#11152=ORIENTED_EDGE ( 'NONE', *, *, #6089, .T. ) ;
#11153=AXIS2_PLACEMENT_3D ( 'NONE', #16169, #21792, #6683 ) ;
#11154=EDGE_LOOP ( 'NONE', ( #3087, #19682, #12836, #3948 ) ) ;
#11155=AXIS2_PLACEMENT_3D ( 'NONE', #1743, #11044, #17795 ) ;
#11157=ORIENTED_EDGE ( 'NONE', *, *, #18689, .F. ) ;
#11158=DIRECTION ( 'NONE',  ( 1.000000000000000000, 0.000000000000000000, 0.000000000000000000 ) ) ;
#11159=VERTEX_POINT ( 'NONE', #9775 ) ;
#11161=CARTESIAN_POINT ( 'NONE',  ( 0.000000000000000000, 0.000000000000000000, 0.000000000000000000 ) ) ;
#11162=EDGE_CURVE ( 'NONE', #10498, #10717, #10347, .T. ) ;
#11163=CARTESIAN_POINT ( 'NONE',  ( 0.000000000000000000, -84.12297548659712731, -12.59025161327086906 ) ) ;
#11167=CARTESIAN_POINT ( 'NONE',  ( 0.000000000000000000, 80.18694381077148137, -28.37681241246572483 ) ) ;
#11169=DIRECTION ( 'NONE',  ( -1.000000000000000000, -0.000000000000000000, -0.000000000000000000 ) ) ;
#11171=DIRECTION ( 'NONE',  ( -1.000000000000000000, -0.000000000000000000, -0.000000000000000000 ) ) ;
#11172=ORIENTED_EDGE ( 'NONE', *, *, #15303, .F. ) ;
#11174=CARTESIAN_POINT ( 'NONE',  ( -10.00000000000000000, 0.000000000000000000, 0.000000000000000000 ) ) ;
#11177=VECTOR ( 'NONE', #3640, 1000.000000000000000 ) ;
#11180=AXIS2_PLACEMENT_3D ( 'NONE', #19091, #20749, #6958 ) ;
#11182=VERTEX_POINT ( 'NONE', #11559 ) ;
#11183=VERTEX_POINT ( 'NONE', #1493 ) ;
#11185=LINE ( 'NONE', #17935, #3648 ) ;
#11186=EDGE_LOOP ( 'NONE', ( #6722, #17502, #10961, #7440 ) ) ;
#11187=ORIENTED_EDGE ( 'NONE', *, *, #4363, .T. ) ;
#11190=DIRECTION ( 'NONE',  ( 0.000000000000000000, 0.000000000000000000, 1.000000000000000000 ) ) ;
#11192=EDGE_CURVE ( 'NONE', #5435, #7874, #12203, .T. ) ;
#11194=CARTESIAN_POINT ( 'NONE',  ( 0.000000000000000000, 0.000000000000000000, 0.000000000000000000 ) ) ;
#11199=CIRCLE ( 'NONE', #20732, 44.99999999999999289 ) ;
#11204=ORIENTED_EDGE ( 'NONE', *, *, #15040, .T. ) ;
#11206=ADVANCED_FACE ( 'NONE', ( #11877 ), #20600, .F. ) ;
#11210=CIRCLE ( 'NONE', #1694, 92.50100000000000477 ) ;
#11211=VERTEX_POINT ( 'NONE', #15189 ) ;
#11212=ORIENTED_EDGE ( 'NONE', *, *, #14581, .T. ) ;
#11213=CIRCLE ( 'NONE', #19337, 88.00000000000000000 ) ;
#11214=ORIENTED_EDGE ( 'NONE', *, *, #2553, .F. ) ;
#11218=VECTOR ( 'NONE', #16502, 1000.000000000000000 ) ;
#11221=DIRECTION ( 'NONE',  ( 1.000000000000000000, 0.000000000000000000, 0.000000000000000000 ) ) ;
#11222=CARTESIAN_POINT ( 'NONE',  ( 10.00000000000000000, 79.66702613806774025, -29.80527447819464371 ) ) ;
#11223=ADVANCED_FACE ( 'NONE', ( #13427 ), #15291, .F. ) ;
#11224=DIRECTION ( 'NONE',  ( -1.000000000000000000, 0.000000000000000000, 0.000000000000000000 ) ) ;
#11227=DIRECTION ( 'NONE',  ( 1.000000000000000000, 0.000000000000000000, 0.000000000000000000 ) ) ;
#11228=EDGE_CURVE ( 'NONE', #18352, #1974, #20499, .T. ) ;
#11229=ORIENTED_EDGE ( 'NONE', *, *, #18439, .T. ) ;
#11230=DIRECTION ( 'NONE',  ( 0.000000000000000000, 0.000000000000000000, 1.000000000000000000 ) ) ;
#11231=DIRECTION ( 'NONE',  ( -1.000000000000000000, -0.000000000000000000, -0.000000000000000000 ) ) ;
#11234=AXIS2_PLACEMENT_3D ( 'NONE', #19562, #7527, #4219 ) ;
#11238=FACE_OUTER_BOUND ( 'NONE', #615, .T. ) ;
#11240=ORIENTED_EDGE ( 'NONE', *, *, #5305, .F. ) ;
#11241=CARTESIAN_POINT ( 'NONE',  ( 10.00000000000000000, 76.53853822673980289, 43.42639941457142072 ) ) ;
#11243=ORIENTED_EDGE ( 'NONE', *, *, #14459, .T. ) ;
#11244=ORIENTED_EDGE ( 'NONE', *, *, #19774, .T. ) ;
#11245=DIRECTION ( 'NONE',  ( 0.000000000000000000, -0.9993908270190954291, -0.03489949670251119018 ) ) ;
#11246=EDGE_CURVE ( 'NONE', #2625, #971, #16967, .T. ) ;
#11247=ORIENTED_EDGE ( 'NONE', *, *, #4325, .T. ) ;
#11248=DIRECTION ( 'NONE',  ( -1.000000000000000000, 0.000000000000000000, -0.000000000000000000 ) ) ;
#11250=CARTESIAN_POINT ( 'NONE',  ( 10.00000000000000000, -89.12061559554348378, 24.77803214283513356 ) ) ;
#11255=EDGE_CURVE ( 'NONE', #16595, #18563, #6119, .T. ) ;
#11257=CARTESIAN_POINT ( 'NONE',  ( 10.00000000000000000, -85.54350296776095774, -20.64725405482940346 ) ) ;
#11258=DIRECTION ( 'NONE',  ( -1.000000000000000000, 0.000000000000000000, 0.000000000000000000 ) ) ;
#11259=EDGE_CURVE ( 'NONE', #5395, #1178, #13642, .T. ) ;
#11261=CARTESIAN_POINT ( 'NONE',  ( 0.000000000000000000, 32.56745702629844175, -78.57830605990621109 ) ) ;
#11262=CIRCLE ( 'NONE', #20090, 44.99999999999998579 ) ;
#11264=AXIS2_PLACEMENT_3D ( 'NONE', #13769, #3707, #15530 ) ;
#11267=EDGE_CURVE ( 'NONE', #21645, #3268, #17070, .T. ) ;
#11269=ORIENTED_EDGE ( 'NONE', *, *, #9480, .F. ) ;
#11270=ORIENTED_EDGE ( 'NONE', *, *, #12312, .F. ) ;
#11271=EDGE_CURVE ( 'NONE', #19516, #21566, #14938, .T. ) ;
#11272=VERTEX_POINT ( 'NONE', #279 ) ;
#11273=DIRECTION ( 'NONE',  ( 0.000000000000000000, 0.000000000000000000, 1.000000000000000000 ) ) ;
#11275=LINE ( 'NONE', #14580, #7842 ) ;
#11276=DIRECTION ( 'NONE',  ( -1.000000000000000000, 0.000000000000000000, 0.000000000000000000 ) ) ;
#11277=AXIS2_PLACEMENT_3D ( 'NONE', #16939, #4783, #8317 ) ;
#11278=CYLINDRICAL_SURFACE ( 'NONE', #19249, 92.50100000000000477 ) ;
#11279=CARTESIAN_POINT ( 'NONE',  ( 10.00000000000000000, 85.54350296776139828, -20.64725405482768750 ) ) ;
#11280=DIRECTION ( 'NONE',  ( -1.000000000000000000, -0.000000000000000000, -0.000000000000000000 ) ) ;
#11284=CYLINDRICAL_SURFACE ( 'NONE', #10881, 92.50100000000000477 ) ;
#11285=ORIENTED_EDGE ( 'NONE', *, *, #14894, .F. ) ;
#11286=LINE ( 'NONE', #9391, #3379 ) ;
#11287=ORIENTED_EDGE ( 'NONE', *, *, #20175, .F. ) ;
#11289=DIRECTION ( 'NONE',  ( 0.000000000000000000, -0.9702957262759988044, 0.2419218955996582376 ) ) ;
#11290=ORIENTED_EDGE ( 'NONE', *, *, #5316, .F. ) ;
#11301=CYLINDRICAL_SURFACE ( 'NONE', #20635, 44.99999999999999289 ) ;
#11303=CARTESIAN_POINT ( 'NONE',  ( 10.00000000000000000, 23.10190250628834718, 89.56973317806607326 ) ) ;
#11304=CARTESIAN_POINT ( 'NONE',  ( 10.00000000000000000, 43.18649929580291058, -73.28107340219372645 ) ) ;
#11305=DIRECTION ( 'NONE',  ( 0.000000000000000000, 0.000000000000000000, 1.000000000000000000 ) ) ;
#11306=CARTESIAN_POINT ( 'NONE',  ( 0.000000000000000000, -79.38136668499764426, 37.98155635597287016 ) ) ;
#11307=FACE_OUTER_BOUND ( 'NONE', #4397, .T. ) ;
#11308=VECTOR ( 'NONE', #16430, 1000.000000000000000 ) ;
#11309=ORIENTED_EDGE ( 'NONE', *, *, #56, .T. ) ;
#11310=ORIENTED_EDGE ( 'NONE', *, *, #10008, .F. ) ;
#11311=CARTESIAN_POINT ( 'NONE',  ( 0.000000000000000000, 85.54350296776139828, -20.64725405482768750 ) ) ;
#11312=EDGE_CURVE ( 'NONE', #4606, #13627, #20171, .T. ) ;
#11314=VERTEX_POINT ( 'NONE', #2043 ) ;
#11315=ORIENTED_EDGE ( 'NONE', *, *, #17703, .F. ) ;
#11316=ORIENTED_EDGE ( 'NONE', *, *, #8527, .F. ) ;
#11319=DIRECTION ( 'NONE',  ( 1.000000000000000000, 0.000000000000000000, 0.000000000000000000 ) ) ;
#11320=CARTESIAN_POINT ( 'NONE',  ( 10.00000000000000000, 62.44821182181090791, 68.23969402963524544 ) ) ;
#11321=ADVANCED_FACE ( 'NONE', ( #5030 ), #11767, .F. ) ;
#11322=ORIENTED_EDGE ( 'NONE', *, *, #6379, .T. ) ;
#11324=LINE ( 'NONE', #1488, #20408 ) ;
#11326=CYLINDRICAL_SURFACE ( 'NONE', #16713, 44.99999999999998579 ) ;
#11330=CARTESIAN_POINT ( 'NONE',  ( 5.000000000000000000, 36.39558101400138668, 80.12091913260394449 ) ) ;
#11331=CARTESIAN_POINT ( 'NONE',  ( 0.000000000000000000, 15.32665449652044565, -91.22241316115403720 ) ) ;
#11332=ORIENTED_EDGE ( 'NONE', *, *, #16943, .T. ) ;
#11334=CARTESIAN_POINT ( 'NONE',  ( 10.00000000000000000, 82.02147376274727719, -42.76579056660780509 ) ) ;
#11335=ORIENTED_EDGE ( 'NONE', *, *, #3102, .T. ) ;
#11337=ADVANCED_FACE ( 'NONE', ( #17512 ), #9302, .F. ) ;
#11339=DIRECTION ( 'NONE',  ( 1.000000000000000000, 0.000000000000000000, 0.000000000000000000 ) ) ;
#11340=ORIENTED_EDGE ( 'NONE', *, *, #5560, .F. ) ;
#11341=LINE ( 'NONE', #12893, #11308 ) ;
#11344=ORIENTED_EDGE ( 'NONE', *, *, #13953, .T. ) ;
#11346=ORIENTED_EDGE ( 'NONE', *, *, #17320, .F. ) ;
#11348=CARTESIAN_POINT ( 'NONE',  ( 10.00000000000000000, -27.00677879429080974, 80.65868421664423238 ) ) ;
#11351=DIRECTION ( 'NONE',  ( -1.000000000000000000, 0.000000000000000000, 0.000000000000000000 ) ) ;
#11352=ADVANCED_FACE ( 'NONE', ( #805 ), #10976, .F. ) ;
#11353=CYLINDRICAL_SURFACE ( 'NONE', #21079, 100.0000000000000000 ) ;
#11354=DIRECTION ( 'NONE',  ( 0.000000000000000000, -0.8290375725550467312, 0.5591929034707392443 ) ) ;
#11355=DIRECTION ( 'NONE',  ( 0.000000000000000000, 3.546545773108139720E-14, -1.000000000000000000 ) ) ;
#11360=DIRECTION ( 'NONE',  ( 0.000000000000000000, 0.000000000000000000, 1.000000000000000000 ) ) ;
#11364=ORIENTED_EDGE ( 'NONE', *, *, #6913, .T. ) ;
#11366=ADVANCED_FACE ( 'NONE', ( #4344 ), #20714, .F. ) ;
#11367=CIRCLE ( 'NONE', #4315, 44.99999999999999289 ) ;
#11368=ORIENTED_EDGE ( 'NONE', *, *, #16484, .T. ) ;
#11370=DIRECTION ( 'NONE',  ( 0.000000000000000000, 0.000000000000000000, 1.000000000000000000 ) ) ;
#11371=CIRCLE ( 'NONE', #18087, 45.00000000000000000 ) ;
#11373=CARTESIAN_POINT ( 'NONE',  ( -10.00000000000000000, 0.000000000000000000, 0.000000000000000000 ) ) ;
#11376=EDGE_CURVE ( 'NONE', #9424, #14363, #19156, .T. ) ;
#11381=DIRECTION ( 'NONE',  ( -1.000000000000000000, 0.000000000000000000, 0.000000000000000000 ) ) ;
#11382=CARTESIAN_POINT ( 'NONE',  ( 0.000000000000000000, -81.34229909304701778, 33.57723005635337898 ) ) ;
#11383=CIRCLE ( 'NONE', #11748, 92.50100000000000477 ) ;
#11388=VECTOR ( 'NONE', #2539, 1000.000000000000000 ) ;
#11389=VECTOR ( 'NONE', #2413, 1000.000000000000000 ) ;
#11390=ORIENTED_EDGE ( 'NONE', *, *, #15131, .F. ) ;
#11392=ORIENTED_EDGE ( 'NONE', *, *, #6956, .F. ) ;
#11394=FACE_OUTER_BOUND ( 'NONE', #13243, .T. ) ;
#11396=ORIENTED_EDGE ( 'NONE', *, *, #7416, .T. ) ;
#11397=LINE ( 'NONE', #18148, #8416 ) ;
#11398=VERTEX_POINT ( 'NONE', #17623 ) ;
#11399=ORIENTED_EDGE ( 'NONE', *, *, #5938, .T. ) ;
#11402=VERTEX_POINT ( 'NONE', #920 ) ;
#11404=DIRECTION ( 'NONE',  ( 0.000000000000000000, 0.9848077530122074652, 0.1736481776669340227 ) ) ;
#11405=AXIS2_PLACEMENT_3D ( 'NONE', #12684, #4289, #9656 ) ;
#11406=CIRCLE ( 'NONE', #14573, 100.0000000000000000 ) ;
#11409=CARTESIAN_POINT ( 'NONE',  ( 10.00000000000000000, 87.17509410653667601, -30.93441398372498341 ) ) ;
#11411=AXIS2_PLACEMENT_3D ( 'NONE', #16040, #9401, #9518 ) ;
#11412=CARTESIAN_POINT ( 'NONE',  ( 10.00000000000000000, -89.12061559554314272, -24.77803214283632727 ) ) ;
#11413=DIRECTION ( 'NONE',  ( 1.000000000000000000, 0.000000000000000000, 0.000000000000000000 ) ) ;
#11414=CARTESIAN_POINT ( 'NONE',  ( 10.00000000000000000, 72.53479564998782791, 44.42851404693380601 ) ) ;
#11415=AXIS2_PLACEMENT_3D ( 'NONE', #1898, #10509, #15593 ) ;
#11416=ORIENTED_EDGE ( 'NONE', *, *, #14531, .T. ) ;
#11418=VERTEX_POINT ( 'NONE', #14402 ) ;
#11421=ORIENTED_EDGE ( 'NONE', *, *, #410, .F. ) ;
#11425=AXIS2_PLACEMENT_3D ( 'NONE', #17641, #7370, #15871 ) ;
#11427=ORIENTED_EDGE ( 'NONE', *, *, #298, .T. ) ;
#11430=CARTESIAN_POINT ( 'NONE',  ( 10.00000000000000000, 61.33825423015778711, -69.23910433415882437 ) ) ;
#11431=VERTEX_POINT ( 'NONE', #2475 ) ;
#11432=CIRCLE ( 'NONE', #7921, 88.00000000000000000 ) ;
#11433=DIRECTION ( 'NONE',  ( -1.000000000000000000, -0.000000000000000000, -0.000000000000000000 ) ) ;
#11434=DIRECTION ( 'NONE',  ( 1.000000000000000000, -0.000000000000000000, -0.000000000000000000 ) ) ;
#11435=DIRECTION ( 'NONE',  ( 0.000000000000000000, 0.9271838545667857590, 0.3746065934159159561 ) ) ;
#11437=CARTESIAN_POINT ( 'NONE',  ( 10.00000000000000000, -60.65655256511196569, -59.63197188857583342 ) ) ;
#11442=ORIENTED_EDGE ( 'NONE', *, *, #21127, .F. ) ;
#11444=LINE ( 'NONE', #12764, #15523 ) ;
#11445=DIRECTION ( 'NONE',  ( 0.000000000000000000, -0.9702957262759988044, 0.2419218955996582376 ) ) ;
#11447=EDGE_CURVE ( 'NONE', #13770, #6615, #14078, .T. ) ;
#11448=CYLINDRICAL_SURFACE ( 'NONE', #14713, 88.00000000000000000 ) ;
#11449=ORIENTED_EDGE ( 'NONE', *, *, #16541, .T. ) ;
#11451=DIRECTION ( 'NONE',  ( 0.000000000000000000, 0.000000000000000000, -1.000000000000000000 ) ) ;
#11453=CARTESIAN_POINT ( 'NONE',  ( -10.00000000000000000, 0.000000000000000000, 0.000000000000000000 ) ) ;
#11454=ORIENTED_EDGE ( 'NONE', *, *, #143, .F. ) ;
#11455=DIRECTION ( 'NONE',  ( 1.000000000000000000, -0.000000000000000000, -0.000000000000000000 ) ) ;
#11458=ORIENTED_EDGE ( 'NONE', *, *, #14624, .F. ) ;
#11462=DIRECTION ( 'NONE',  ( -1.000000000000000000, -0.000000000000000000, -0.000000000000000000 ) ) ;
#11463=CARTESIAN_POINT ( 'NONE',  ( 10.00000000000000000, -2.481790431839894673, 92.46770094066590673 ) ) ;
#11464=DIRECTION ( 'NONE',  ( -1.000000000000000000, 0.000000000000000000, 0.000000000000000000 ) ) ;
#11467=AXIS2_PLACEMENT_3D ( 'NONE', #17779, #19653, #7728 ) ;
#11468=EDGE_CURVE ( 'NONE', #536, #155, #11773, .T. ) ;
#11469=DIRECTION ( 'NONE',  ( -1.000000000000000000, -0.000000000000000000, -0.000000000000000000 ) ) ;
#11470=EDGE_CURVE ( 'NONE', #2155, #5782, #16356, .T. ) ;
#11471=DIRECTION ( 'NONE',  ( 0.000000000000000000, 0.000000000000000000, 1.000000000000000000 ) ) ;
#11472=CIRCLE ( 'NONE', #14655, 88.00000000000000000 ) ;
#11473=DIRECTION ( 'NONE',  ( 1.000000000000000000, 0.000000000000000000, 0.000000000000000000 ) ) ;
#11474=ADVANCED_BREP_SHAPE_REPRESENTATION ( '', ( #6279, #15567 ), #19793 ) ;
#11475=CARTESIAN_POINT ( 'NONE',  ( 10.00000000000000000, 87.92084725184953697, -3.731570516142035387 ) ) ;
#11477=VECTOR ( 'NONE', #3071, 1000.000000000000000 ) ;
#11478=DIRECTION ( 'NONE',  ( 0.000000000000000000, 0.000000000000000000, 1.000000000000000000 ) ) ;
#11480=ORIENTED_EDGE ( 'NONE', *, *, #10648, .T. ) ;
#11481=AXIS2_PLACEMENT_3D ( 'NONE', #9544, #21596, #21388 ) ;
#11482=EDGE_LOOP ( 'NONE', ( #6900, #9974, #13104, #13971 ) ) ;
#11483=EDGE_CURVE ( 'NONE', #4745, #10738, #18136, .T. ) ;
#11485=AXIS2_PLACEMENT_3D ( 'NONE', #10753, #17951, #15852 ) ;
#11486=VECTOR ( 'NONE', #20530, 1000.000000000000000 ) ;
#11487=CIRCLE ( 'NONE', #1966, 44.99999999999998579 ) ;
#11488=CIRCLE ( 'NONE', #10784, 92.50100000000000477 ) ;
#11489=ORIENTED_EDGE ( 'NONE', *, *, #17859, .T. ) ;
#11490=EDGE_CURVE ( 'NONE', #3061, #18563, #16004, .T. ) ;
#11492=DIRECTION ( 'NONE',  ( 0.000000000000000000, 0.6946583704589934793, 0.7193398003386547446 ) ) ;
#11494=CARTESIAN_POINT ( 'NONE',  ( 10.00000000000000000, -77.39385041987125646, -35.28996114464684553 ) ) ;
#11495=CARTESIAN_POINT ( 'NONE',  ( 10.00000000000000000, -83.89484365856928605, 26.56417150042919673 ) ) ;
#11497=DIRECTION ( 'NONE',  ( 0.000000000000000000, 0.000000000000000000, 1.000000000000000000 ) ) ;
#11499=CARTESIAN_POINT ( 'NONE',  ( 0.000000000000000000, 0.000000000000000000, 0.000000000000000000 ) ) ;
#11501=DIRECTION ( 'NONE',  ( 0.000000000000000000, 0.000000000000000000, 1.000000000000000000 ) ) ;
#11502=CARTESIAN_POINT ( 'NONE',  ( 10.00000000000000000, 45.60224695560681596, -80.47900393021679122 ) ) ;
#11504=CIRCLE ( 'NONE', #11848, 44.99999999999999289 ) ;
#11507=CARTESIAN_POINT ( 'NONE',  ( 10.00000000000000000, 8.925965667928872804, 92.06933331948788179 ) ) ;
#11508=AXIS2_PLACEMENT_3D ( 'NONE', #12453, #9240, #17444 ) ;
#11509=VERTEX_POINT ( 'NONE', #9527 ) ;
#11510=ORIENTED_EDGE ( 'NONE', *, *, #3710, .F. ) ;
#11511=EDGE_CURVE ( 'NONE', #14361, #17102, #14729, .T. ) ;
#11512=CARTESIAN_POINT ( 'NONE',  ( 0.000000000000000000, 0.000000000000000000, 0.000000000000000000 ) ) ;
#11514=CYLINDRICAL_SURFACE ( 'NONE', #17946, 45.00000000000000000 ) ;
#11515=ORIENTED_EDGE ( 'NONE', *, *, #782, .T. ) ;
#11516=ADVANCED_FACE ( 'NONE', ( #1143 ), #7885, .F. ) ;
#11518=CARTESIAN_POINT ( 'NONE',  ( 10.00000000000000000, -84.79630770241089976, 6.691460262315113816 ) ) ;
#11519=ORIENTED_EDGE ( 'NONE', *, *, #1792, .F. ) ;
#11520=AXIS2_PLACEMENT_3D ( 'NONE', #19221, #4088, #4294 ) ;
#11521=DIRECTION ( 'NONE',  ( 1.000000000000000000, 0.000000000000000000, 0.000000000000000000 ) ) ;
#11524=EDGE_CURVE ( 'NONE', #16840, #16161, #8602, .T. ) ;
#11525=VECTOR ( 'NONE', #8811, 1000.000000000000000 ) ;
#11526=FACE_OUTER_BOUND ( 'NONE', #10908, .T. ) ;
#11527=CYLINDRICAL_SURFACE ( 'NONE', #20405, 45.00000000000000000 ) ;
#11528=DIRECTION ( 'NONE',  ( -1.000000000000000000, 0.000000000000000000, -0.000000000000000000 ) ) ;
#11529=CARTESIAN_POINT ( 'NONE',  ( 0.000000000000000000, 0.000000000000000000, 0.000000000000000000 ) ) ;
#11530=CYLINDRICAL_SURFACE ( 'NONE', #12530, 88.00000000000000000 ) ;
#11531=DIRECTION ( 'NONE',  ( 0.000000000000000000, -0.7880107536067275653, 0.6156614753256510753 ) ) ;
#11532=ADVANCED_FACE ( 'NONE', ( #3129 ), #21477, .F. ) ;
#11535=AXIS2_PLACEMENT_3D ( 'NONE', #20495, #7230, #6805 ) ;
#11536=AXIS2_PLACEMENT_3D ( 'NONE', #4964, #18343, #3192 ) ;
#11538=DIRECTION ( 'NONE',  ( -1.000000000000000000, -0.000000000000000000, -0.000000000000000000 ) ) ;
#11539=DIRECTION ( 'NONE',  ( 0.000000000000000000, 0.000000000000000000, 1.000000000000000000 ) ) ;
#11540=VERTEX_POINT ( 'NONE', #14515 ) ;
#11545=CARTESIAN_POINT ( 'NONE',  ( 10.00000000000000000, -78.80192417387952730, 39.16958956249271040 ) ) ;
#11551=EDGE_CURVE ( 'NONE', #5152, #3214, #15662, .T. ) ;
#11552=VECTOR ( 'NONE', #21306, 1000.000000000000000 ) ;
#11553=CYLINDRICAL_SURFACE ( 'NONE', #20619, 88.00000000000000000 ) ;
#11554=DIRECTION ( 'NONE',  ( 0.000000000000000000, -0.8987940462991710344, 0.4383711467890689106 ) ) ;
#11555=AXIS2_PLACEMENT_3D ( 'NONE', #4170, #16207, #10903 ) ;
#11557=DIRECTION ( 'NONE',  ( 0.000000000000000000, 0.000000000000000000, 1.000000000000000000 ) ) ;
#11559=CARTESIAN_POINT ( 'NONE',  ( 0.000000000000000000, 47.19205848891868271, -74.27590198428072199 ) ) ;
#11563=DIRECTION ( 'NONE',  ( 1.000000000000000000, 0.000000000000000000, 0.000000000000000000 ) ) ;
#11564=ORIENTED_EDGE ( 'NONE', *, *, #7905, .F. ) ;
#11565=DIRECTION ( 'NONE',  ( -1.000000000000000000, -0.000000000000000000, 0.000000000000000000 ) ) ;
#11566=ORIENTED_EDGE ( 'NONE', *, *, #12580, .F. ) ;
#11567=AXIS2_PLACEMENT_3D ( 'NONE', #13825, #8850, #14039 ) ;
#11571=VECTOR ( 'NONE', #17725, 1000.000000000000000 ) ;
#11572=EDGE_CURVE ( 'NONE', #20049, #9164, #1257, .T. ) ;
#11573=EDGE_LOOP ( 'NONE', ( #21209, #14828, #14338, #10350, #11892, #10501, #8689, #1681, #16477, #16647, #450, #4451, #18672, #20860, #20643, #21426, #15609, #7819, #748, #21433, #5038, #3252, #14856, #10035, #11214, #5726, #18846, #8767, #21612, #18718, #15228, #8454, #2025, #3577, #9587, #17882, #9085, #12261, #2811, #11489, #2318, #5667, #5890, #905, #17283, #4905, #19963, #13763, #9540, #10795, #5246, #16844, #10381, #7811, #2893, #18526, #2490, #2185, #12096, #6460, #2891, #7927, #15474, #16906, #11316, #9398, #17910, #10706, #4466, #8518, #152, #6791, #1059, #19173, #17442, #8394, #3310, #20401, #16292, #19074, #18070, #19997, #13604, #17144, #19186, #11346, #17404, #5210, #8280, #16818, #4854, #4774, #13572, #7659, #4883, #14931, #14273, #4280, #17630, #12157, #20628, #16552, #16568, #16454, #20705, #10911, #8740, #13733, #9313, #15796, #482, #7983, #19457, #3903, #13418, #7949, #1015, #9033, #1302, #3108, #17823, #21108, #3389, #5272, #7415, #18208, #3902, #13270, #3974, #7673, #9000, #18775, #17409, #8477, #21781, #14780, #1732, #18769, #19420, #14011, #17922, #506, #19908, #20236, #2798, #16452, #11037, #7791, #4173, #15115, #5869, #2739, #2085, #11421, #13061, #20856, #16935, #7488, #2868, #21451, #1590, #8037, #3601, #12262, #18791, #9235, #3627, #9161, #12118, #1512, #6812, #7256, #8948, #7587, #4835, #4028, #21213, #12970, #8894, #19856, #6313, #10451, #4744, #6173, #17584, #2007, #2400, #6213, #21056, #16969, #6439, #5052, #5979, #10378, #5540, #21558, #17853, #3038, #15408, #18593, #11701, #400, #9539, #3927, #11229, #6830, #19011, #16399, #19494, #1827, #3853, #16745, #11128, #5669, #13737, #14142, #15022, #5082, #6828, #4718, #8145, #20265, #8178, #19794, #1557, #7304, #16241, #17023, #6964, #12963, #1984, #16129, #8719, #19823, #2053, #15386, #20945, #3384, #9666, #13519, #11322, #16243, #21801, #21021, #3762, #9764, #9139, #7257, #10659, #11872, #16190, #15739, #9328, #1501, #14652, #8127, #5488, #9184, #4175, #5119, #11776, #8552, #10687, #2435, #12722, #10871, #6163, #21314, #13413, #9028, #15452, #19464, #13138, #20155, #18269, #2593, #2051, #6112, #18149, #4296, #11139, #17768, #4126, #20672, #5532, #8525, #9811, #20834, #335, #10082, #11392, #19805, #7458, #15012, #4991, #8626, #8193, #3174, #10216, #16256, #19487, #5197, #5552, #20108, #11953, #10530, #10060, #14504, #21041, #17785, #11014, #16101, #15422, #12397, #12244, #10236, #3447, #7245, #8973, #19750, #8845, #5611, #9278, #10744, #5596, #10606, #20272, #7868, #17029, #18589, #12794, #7303, #3959, #8756, #20189, #18428, #2887, #18797, #6939, #18036, #19342, #3323, #17989, #9928, #6082, #17073, #21805, #6850, #6079, #9058, #1164, #18722, #728, #6467, #9346, #3679, #13987, #2649, #17331, #10085, #21545, #2721, #618 ) ) ;
#11574=DIRECTION ( 'NONE',  ( 0.000000000000000000, -1.079383496163347022E-14, -1.000000000000000000 ) ) ;
#11577=CARTESIAN_POINT ( 'NONE',  ( 10.00000000000000000, -37.96946988134122591, -76.11510229470897571 ) ) ;
#11578=VERTEX_POINT ( 'NONE', #3022 ) ;
#11579=CIRCLE ( 'NONE', #17934, 92.50099999999999056 ) ;
#11580=DIRECTION ( 'NONE',  ( 0.000000000000000000, 0.000000000000000000, 1.000000000000000000 ) ) ;
#11584=CIRCLE ( 'NONE', #13694, 44.99999999999999289 ) ;
#11586=AXIS2_PLACEMENT_3D ( 'NONE', #18817, #5343, #369 ) ;
#11587=CARTESIAN_POINT ( 'NONE',  ( 0.000000000000000000, 52.34334029047876413, 76.26670130689501548 ) ) ;
#11589=AXIS2_PLACEMENT_3D ( 'NONE', #21685, #21797, #14944 ) ;
#11591=DIRECTION ( 'NONE',  ( -1.000000000000000000, -0.000000000000000000, 0.000000000000000000 ) ) ;
#11592=CARTESIAN_POINT ( 'NONE',  ( 0.000000000000000000, 81.32027326007866463, 44.08455690949082850 ) ) ;
#11593=ORIENTED_EDGE ( 'NONE', *, *, #15301, .F. ) ;
#11595=ORIENTED_EDGE ( 'NONE', *, *, #3689, .F. ) ;
#11596=CIRCLE ( 'NONE', #17593, 44.99999999999998579 ) ;
#11597=ORIENTED_EDGE ( 'NONE', *, *, #20918, .F. ) ;
#11599=VECTOR ( 'NONE', #2456, 1000.000000000000000 ) ;
#11600=CIRCLE ( 'NONE', #2077, 88.00000000000000000 ) ;
#11601=CIRCLE ( 'NONE', #16887, 44.99999999999999289 ) ;
#11608=DIRECTION ( 'NONE',  ( 0.000000000000000000, 0.000000000000000000, 1.000000000000000000 ) ) ;
#11612=LINE ( 'NONE', #8080, #5538 ) ;
#11614=DIRECTION ( 'NONE',  ( 0.000000000000000000, 0.2079116908177599254, -0.9781476007338055778 ) ) ;
#11616=AXIS2_PLACEMENT_3D ( 'NONE', #4829, #19965, #70 ) ;
#11617=AXIS2_PLACEMENT_3D ( 'NONE', #9784, #16311, #961 ) ;
#11618=ORIENTED_EDGE ( 'NONE', *, *, #1375, .F. ) ;
#11620=CARTESIAN_POINT ( 'NONE',  ( 10.00000000000000000, -84.12297548659729785, 12.59025161326973397 ) ) ;
#11622=ORIENTED_EDGE ( 'NONE', *, *, #17705, .F. ) ;
#11626=ADVANCED_FACE ( 'NONE', ( #5114 ), #18809, .F. ) ;
#11627=EDGE_CURVE ( 'NONE', #21052, #15273, #13832, .T. ) ;
#11628=DIRECTION ( 'NONE',  ( 0.000000000000000000, 2.621359919253842577E-15, -1.000000000000000000 ) ) ;
#11633=EDGE_CURVE ( 'NONE', #610, #16361, #14592, .T. ) ;
#11634=ORIENTED_EDGE ( 'NONE', *, *, #20464, .T. ) ;
#11635=AXIS2_PLACEMENT_3D ( 'NONE', #21378, #7677, #6140 ) ;
#11636=DIRECTION ( 'NONE',  ( -1.000000000000000000, 0.000000000000000000, 0.000000000000000000 ) ) ;
#11637=AXIS2_PLACEMENT_3D ( 'NONE', #20319, #8492, #5181 ) ;
#11639=DIRECTION ( 'NONE',  ( -1.000000000000000000, -0.000000000000000000, 0.000000000000000000 ) ) ;
#11641=CARTESIAN_POINT ( 'NONE',  ( 10.00000000000000000, 0.000000000000000000, 0.000000000000000000 ) ) ;
#11642=DIRECTION ( 'NONE',  ( -1.000000000000000000, -0.000000000000000000, -0.000000000000000000 ) ) ;
#11643=CARTESIAN_POINT ( 'NONE',  ( 10.00000000000000000, -72.53479564998815476, 44.42851404693331574 ) ) ;
#11645=LINE ( 'NONE', #18389, #13700 ) ;
#11646=ORIENTED_EDGE ( 'NONE', *, *, #5987, .T. ) ;
#11658=VERTEX_POINT ( 'NONE', #16825 ) ;
#11659=ORIENTED_EDGE ( 'NONE', *, *, #20008, .T. ) ;
#11664=DIRECTION ( 'NONE',  ( 0.000000000000000000, 0.000000000000000000, 1.000000000000000000 ) ) ;
#11665=DIRECTION ( 'NONE',  ( 0.000000000000000000, -0.7431448254774000173, 0.6691306063588517983 ) ) ;
#11666=CIRCLE ( 'NONE', #12366, 88.00000000000000000 ) ;
#11667=LINE ( 'NONE', #18413, #13191 ) ;
#11668=CARTESIAN_POINT ( 'NONE',  ( 10.00000000000000000, 0.000000000000000000, 0.000000000000000000 ) ) ;
#11669=CARTESIAN_POINT ( 'NONE',  ( 0.000000000000000000, -3.974475837765555575, 92.41557521768190497 ) ) ;
#11672=EDGE_LOOP ( 'NONE', ( #18344, #14501, #194, #3308 ) ) ;
#11674=CARTESIAN_POINT ( 'NONE',  ( 0.000000000000000000, -6.797690662954623875, -87.73705831432221203 ) ) ;
#11675=DIRECTION ( 'NONE',  ( 0.000000000000000000, 0.000000000000000000, 1.000000000000000000 ) ) ;
#11679=CARTESIAN_POINT ( 'NONE',  ( 10.00000000000000000, 84.19736439813857487, -38.30455363800848545 ) ) ;
#11680=ORIENTED_EDGE ( 'NONE', *, *, #12966, .T. ) ;
#11682=FACE_OUTER_BOUND ( 'NONE', #12730, .T. ) ;
#11683=ORIENTED_EDGE ( 'NONE', *, *, #14627, .T. ) ;
#11685=ORIENTED_EDGE ( 'NONE', *, *, #3681, .T. ) ;
#11686=EDGE_LOOP ( 'NONE', ( #12974, #21320, #11828, #21511 ) ) ;
#11688=ORIENTED_EDGE ( 'NONE', *, *, #19713, .T. ) ;
#11693=DIRECTION ( 'NONE',  ( 1.000000000000000000, -0.000000000000000000, -0.000000000000000000 ) ) ;
#11695=LINE ( 'NONE', #1640, #18627 ) ;
#11696=DIRECTION ( 'NONE',  ( 0.000000000000000000, 0.000000000000000000, 1.000000000000000000 ) ) ;
#11697=STYLED_ITEM ( 'NONE', ( #12420 ), #11474 ) ;
#11698=CARTESIAN_POINT ( 'NONE',  ( -10.00000000000000000, 0.000000000000000000, 0.000000000000000000 ) ) ;
#11699=DIRECTION ( 'NONE',  ( 0.000000000000000000, 0.000000000000000000, 1.000000000000000000 ) ) ;
#11700=CARTESIAN_POINT ( 'NONE',  ( 0.000000000000000000, -80.18694381077088451, -28.37681241246736974 ) ) ;
#11701=ORIENTED_EDGE ( 'NONE', *, *, #10268, .T. ) ;
#11708=FACE_OUTER_BOUND ( 'NONE', #3684, .T. ) ;
#11709=ORIENTED_EDGE ( 'NONE', *, *, #7529, .F. ) ;
#11712=CARTESIAN_POINT ( 'NONE',  ( 0.000000000000000000, 56.35896156214949571, 73.34918167666329225 ) ) ;
#11714=DIRECTION ( 'NONE',  ( -1.000000000000000000, 0.000000000000000000, -0.000000000000000000 ) ) ;
#11715=FACE_OUTER_BOUND ( 'NONE', #19391, .T. ) ;
#11716=EDGE_CURVE ( 'NONE', #21723, #15150, #17042, .T. ) ;
#11718=CARTESIAN_POINT ( 'NONE',  ( 10.00000000000000000, 78.01214607583752070, 33.90124636420136994 ) ) ;
#11719=VECTOR ( 'NONE', #16016, 1000.000000000000000 ) ;
#11721=EDGE_CURVE ( 'NONE', #18379, #19278, #17423, .T. ) ;
#11723=DIRECTION ( 'NONE',  ( 0.000000000000000000, 0.000000000000000000, -1.000000000000000000 ) ) ;
#11725=ORIENTED_EDGE ( 'NONE', *, *, #21637, .T. ) ;
#11726=CARTESIAN_POINT ( 'NONE',  ( 10.00000000000000000, 40.72878876293257377, -78.00747250042405767 ) ) ;
#11727=VERTEX_POINT ( 'NONE', #8638 ) ;
#11728=ORIENTED_EDGE ( 'NONE', *, *, #8914, .T. ) ;
#11729=CARTESIAN_POINT ( 'NONE',  ( 10.00000000000000000, -75.27139873020847460, -53.76477968147890607 ) ) ;
#11732=CIRCLE ( 'NONE', #13476, 92.50100000000001899 ) ;
#11733=LINE ( 'NONE', #13724, #15006 ) ;
#11735=LINE ( 'NONE', #10510, #12916 ) ;
#11737=CYLINDRICAL_SURFACE ( 'NONE', #18199, 44.99999999999999289 ) ;
#11738=LINE ( 'NONE', #6688, #11218 ) ;
#11742=EDGE_CURVE ( 'NONE', #16874, #18196, #17157, .T. ) ;
#11743=ORIENTED_EDGE ( 'NONE', *, *, #10387, .T. ) ;
#11745=ADVANCED_FACE ( 'NONE', ( #9273 ), #20892, .F. ) ;
#11748=AXIS2_PLACEMENT_3D ( 'NONE', #11161, #2773, #9496 ) ;
#11749=ORIENTED_EDGE ( 'NONE', *, *, #13896, .T. ) ;
#11752=EDGE_CURVE ( 'NONE', #13981, #6087, #7323, .T. ) ;
#11753=ORIENTED_EDGE ( 'NONE', *, *, #17606, .T. ) ;
#11754=AXIS2_PLACEMENT_3D ( 'NONE', #6713, #387, #20281 ) ;
#11755=DIRECTION ( 'NONE',  ( 1.000000000000000000, 0.000000000000000000, 0.000000000000000000 ) ) ;
#11756=ORIENTED_EDGE ( 'NONE', *, *, #8371, .F. ) ;
#11758=CARTESIAN_POINT ( 'NONE',  ( 10.00000000000000000, 36.60317927562682883, -76.78148674856727496 ) ) ;
#11761=ORIENTED_EDGE ( 'NONE', *, *, #6132, .T. ) ;
#11762=ADVANCED_FACE ( 'NONE', ( #10621 ), #19129, .F. ) ;
#11763=CARTESIAN_POINT ( 'NONE',  ( 10.00000000000000000, 57.53593069156372053, 72.42963261300981515 ) ) ;
#11764=CARTESIAN_POINT ( 'NONE',  ( 0.000000000000000000, 5.479102470010468018, 87.82926298292115064 ) ) ;
#11765=CYLINDRICAL_SURFACE ( 'NONE', #18905, 92.50100000000000477 ) ;
#11767=CYLINDRICAL_SURFACE ( 'NONE', #12815, 44.99999999999999289 ) ;
#11768=CARTESIAN_POINT ( 'NONE',  ( 10.00000000000000000, -8.925965667929485647, 92.06933331948778232 ) ) ;
#11769=AXIS2_PLACEMENT_3D ( 'NONE', #2417, #12783, #4187 ) ;
#11770=EDGE_CURVE ( 'NONE', #14184, #1184, #5160, .T. ) ;
#11773=CIRCLE ( 'NONE', #17075, 92.50100000000000477 ) ;
#11774=ADVANCED_FACE ( 'NONE', ( #20796 ), #2542, .F. ) ;
#11776=ORIENTED_EDGE ( 'NONE', *, *, #8665, .T. ) ;
#11777=AXIS2_PLACEMENT_3D ( 'NONE', #10886, #15962, #2493 ) ;
#11780=CARTESIAN_POINT ( 'NONE',  ( 0.000000000000000000, 0.000000000000000000, 0.000000000000000000 ) ) ;
#11781=CARTESIAN_POINT ( 'NONE',  ( 10.00000000000000000, -15.32665449651985590, 91.22241316115413667 ) ) ;
#11782=ORIENTED_EDGE ( 'NONE', *, *, #13082, .T. ) ;
#11785=CIRCLE ( 'NONE', #15294, 44.99999999999999289 ) ;
#11786=ORIENTED_EDGE ( 'NONE', *, *, #11898, .T. ) ;
#11790=EDGE_CURVE ( 'NONE', #16638, #5777, #17507, .T. ) ;
#11792=LINE ( 'NONE', #14168, #13371 ) ;
#11793=AXIS2_PLACEMENT_3D ( 'NONE', #13875, #5491, #18974 ) ;
#11796=LINE ( 'NONE', #4957, #5121 ) ;
#11798=DIRECTION ( 'NONE',  ( 1.000000000000000000, 0.000000000000000000, 0.000000000000000000 ) ) ;
#11801=DIRECTION ( 'NONE',  ( 0.000000000000000000, -0.2756373558170063798, 0.9612616959383167847 ) ) ;
#11802=DIRECTION ( 'NONE',  ( -1.000000000000000000, -0.000000000000000000, -0.000000000000000000 ) ) ;
#11803=FACE_OUTER_BOUND ( 'NONE', #17687, .T. ) ;
#11805=EDGE_CURVE ( 'NONE', #966, #17521, #4804, .T. ) ;
#11806=CARTESIAN_POINT ( 'NONE',  ( 10.00000000000000000, 80.18694381077148137, -28.37681241246572483 ) ) ;
#11809=ORIENTED_EDGE ( 'NONE', *, *, #18912, .T. ) ;
#11812=ORIENTED_EDGE ( 'NONE', *, *, #18685, .T. ) ;
#11813=ORIENTED_EDGE ( 'NONE', *, *, #6361, .T. ) ;
#11814=VERTEX_POINT ( 'NONE', #10729 ) ;
#11815=CARTESIAN_POINT ( 'NONE',  ( 10.00000000000000000, -56.34908017029516714, -63.71789861856507997 ) ) ;
#11816=ORIENTED_EDGE ( 'NONE', *, *, #16774, .T. ) ;
#11818=VECTOR ( 'NONE', #5654, 1000.000000000000000 ) ;
#11820=AXIS2_PLACEMENT_3D ( 'NONE', #1511, #16221, #1079 ) ;
#11821=EDGE_CURVE ( 'NONE', #6764, #4687, #10786, .T. ) ;
#11822=DIRECTION ( 'NONE',  ( 1.000000000000000000, 0.000000000000000000, 0.000000000000000000 ) ) ;
#11824=DIRECTION ( 'NONE',  ( 0.000000000000000000, 0.000000000000000000, 1.000000000000000000 ) ) ;
#11826=FACE_OUTER_BOUND ( 'NONE', #11672, .T. ) ;
#11827=CARTESIAN_POINT ( 'NONE',  ( 0.000000000000000000, 0.000000000000000000, 0.000000000000000000 ) ) ;
#11828=ORIENTED_EDGE ( 'NONE', *, *, #10387, .F. ) ;
#11829=DIRECTION ( 'NONE',  ( 1.000000000000000000, 0.000000000000000000, 0.000000000000000000 ) ) ;
#11830=CIRCLE ( 'NONE', #7953, 92.50100000000000477 ) ;
#11837=DIRECTION ( 'NONE',  ( 1.000000000000000000, 0.000000000000000000, 0.000000000000000000 ) ) ;
#11838=VERTEX_POINT ( 'NONE', #12279 ) ;
#11839=EDGE_LOOP ( 'NONE', ( #20000, #8244, #15776, #1105 ) ) ;
#11841=ORIENTED_EDGE ( 'NONE', *, *, #9339, .F. ) ;
#11844=LINE ( 'NONE', #1895, #5018 ) ;
#11846=DIRECTION ( 'NONE',  ( 0.000000000000000000, 0.000000000000000000, 1.000000000000000000 ) ) ;
#11848=AXIS2_PLACEMENT_3D ( 'NONE', #7917, #4706, #11445 ) ;
#11849=DIRECTION ( 'NONE',  ( 0.000000000000000000, 0.7431448254773910245, 0.6691306063588617903 ) ) ;
#11850=AXIS2_PLACEMENT_3D ( 'NONE', #20826, #20604, #7353 ) ;
#11853=DIRECTION ( 'NONE',  ( -1.000000000000000000, -0.000000000000000000, -0.000000000000000000 ) ) ;
#11859=CARTESIAN_POINT ( 'NONE',  ( 10.00000000000000000, 0.000000000000000000, 0.000000000000000000 ) ) ;
#11861=CIRCLE ( 'NONE', #16088, 44.99999999999999289 ) ;
#11862=DIRECTION ( 'NONE',  ( -1.000000000000000000, -0.000000000000000000, 0.000000000000000000 ) ) ;
#11863=ORIENTED_EDGE ( 'NONE', *, *, #15293, .F. ) ;
#11864=AXIS2_PLACEMENT_3D ( 'NONE', #18275, #12953, #1363 ) ;
#11866=DIRECTION ( 'NONE',  ( -1.000000000000000000, 0.000000000000000000, 0.000000000000000000 ) ) ;
#11867=VERTEX_POINT ( 'NONE', #15921 ) ;
#11868=ADVANCED_FACE ( 'NONE', ( #21009 ), #4109, .F. ) ;
#11872=ORIENTED_EDGE ( 'NONE', *, *, #15035, .F. ) ;
#11873=CARTESIAN_POINT ( 'NONE',  ( 10.00000000000000000, -21.65267340503189430, -89.93106657554454841 ) ) ;
#11874=CARTESIAN_POINT ( 'NONE',  ( 0.000000000000000000, -29.47587714450981622, -82.91666097089152743 ) ) ;
#11875=CARTESIAN_POINT ( 'NONE',  ( -10.00000000000000000, 0.000000000000000000, 0.000000000000000000 ) ) ;
#11876=DIRECTION ( 'NONE',  ( 0.000000000000000000, 0.000000000000000000, 1.000000000000000000 ) ) ;
#11877=FACE_OUTER_BOUND ( 'NONE', #14689, .T. ) ;
#11881=ORIENTED_EDGE ( 'NONE', *, *, #6, .F. ) ;
#11882=DIRECTION ( 'NONE',  ( -1.000000000000000000, -0.000000000000000000, 0.000000000000000000 ) ) ;
#11884=CARTESIAN_POINT ( 'NONE',  ( 0.000000000000000000, -84.12297548659712731, -12.59025161327086906 ) ) ;
#11886=DIRECTION ( 'NONE',  ( 0.000000000000000000, 0.000000000000000000, 1.000000000000000000 ) ) ;
#11887=ORIENTED_EDGE ( 'NONE', *, *, #18758, .T. ) ;
#11889=CARTESIAN_POINT ( 'NONE',  ( 10.00000000000000000, 0.000000000000000000, 0.000000000000000000 ) ) ;
#11890=ORIENTED_EDGE ( 'NONE', *, *, #17712, .T. ) ;
#11891=VECTOR ( 'NONE', #6653, 1000.000000000000000 ) ;
#11892=ORIENTED_EDGE ( 'NONE', *, *, #20845, .F. ) ;
#11893=EDGE_CURVE ( 'NONE', #15626, #15275, #20669, .T. ) ;
#11894=VERTEX_POINT ( 'NONE', #17919 ) ;
#11897=ORIENTED_EDGE ( 'NONE', *, *, #12529, .T. ) ;
#11898=EDGE_CURVE ( 'NONE', #11418, #3881, #12554, .T. ) ;
#11900=VECTOR ( 'NONE', #17015, 1000.000000000000000 ) ;
#11903=EDGE_CURVE ( 'NONE', #10412, #12425, #6209, .T. ) ;
#11906=CARTESIAN_POINT ( 'NONE',  ( 10.00000000000000000, -65.64563793391792501, -54.09103124042881916 ) ) ;
#11911=DIRECTION ( 'NONE',  ( -1.000000000000000000, -0.000000000000000000, 0.000000000000000000 ) ) ;
#11912=EDGE_CURVE ( 'NONE', #21782, #13331, #11050, .T. ) ;
#11913=AXIS2_PLACEMENT_3D ( 'NONE', #14797, #16231, #4629 ) ;
#11915=AXIS2_PLACEMENT_3D ( 'NONE', #21742, #6625, #18339 ) ;
#11916=EDGE_CURVE ( 'NONE', #12371, #14961, #2658, .T. ) ;
#11917=CARTESIAN_POINT ( 'NONE',  ( 0.000000000000000000, 60.65655256511316651, -59.63197188857461128 ) ) ;
#11918=EDGE_LOOP ( 'NONE', ( #1783, #1679, #20667, #7760 ) ) ;
#11920=ORIENTED_EDGE ( 'NONE', *, *, #15420, .F. ) ;
#11922=ADVANCED_FACE ( 'NONE', ( #19560 ), #4431, .F. ) ;
#11924=ORIENTED_EDGE ( 'NONE', *, *, #4317, .F. ) ;
#11926=CARTESIAN_POINT ( 'NONE',  ( 10.00000000000000000, 72.53479564998846740, -44.42851404693280415 ) ) ;
#11928=CIRCLE ( 'NONE', #2747, 44.99999999999999289 ) ;
#11934=AXIS2_PLACEMENT_3D ( 'NONE', #17159, #7212, #2129 ) ;
#11936=FACE_OUTER_BOUND ( 'NONE', #14470, .T. ) ;
#11939=LINE ( 'NONE', #8513, #9768 ) ;
#11940=CARTESIAN_POINT ( 'NONE',  ( 10.00000000000000000, -43.18649929580243452, 73.28107340219401067 ) ) ;
#11941=ORIENTED_EDGE ( 'NONE', *, *, #11312, .F. ) ;
#11942=EDGE_CURVE ( 'NONE', #10332, #16155, #9143, .T. ) ;
#11943=DIRECTION ( 'NONE',  ( 1.000000000000000000, 0.000000000000000000, 0.000000000000000000 ) ) ;
#11944=AXIS2_PLACEMENT_3D ( 'NONE', #1328, #14808, #19999 ) ;
#11945=CIRCLE ( 'NONE', #9470, 45.00000000000000711 ) ;
#11946=ORIENTED_EDGE ( 'NONE', *, *, #3044, .F. ) ;
#11948=EDGE_CURVE ( 'NONE', #8942, #2674, #20335, .T. ) ;
#11949=AXIS2_PLACEMENT_3D ( 'NONE', #15249, #11837, #13602 ) ;
#11951=EDGE_LOOP ( 'NONE', ( #9404, #15496 ) ) ;
#11952=DIRECTION ( 'NONE',  ( -1.000000000000000000, 0.000000000000000000, 0.000000000000000000 ) ) ;
#11953=ORIENTED_EDGE ( 'NONE', *, *, #19892, .F. ) ;
#11956=ORIENTED_EDGE ( 'NONE', *, *, #15407, .F. ) ;
#11958=CARTESIAN_POINT ( 'NONE',  ( 10.00000000000000000, 0.000000000000000000, 0.000000000000000000 ) ) ;
#11960=CYLINDRICAL_SURFACE ( 'NONE', #9957, 92.50100000000000477 ) ;
#11962=DIRECTION ( 'NONE',  ( 1.000000000000000000, 0.000000000000000000, 0.000000000000000000 ) ) ;
#11963=AXIS2_PLACEMENT_3D ( 'NONE', #9904, #16545, #8250 ) ;
#11964=DIRECTION ( 'NONE',  ( -1.000000000000000000, 0.000000000000000000, 0.000000000000000000 ) ) ;
#11965=CARTESIAN_POINT ( 'NONE',  ( 5.000000000000002665, -81.83745710415297481, 32.35167097270123548 ) ) ;
#11966=CARTESIAN_POINT ( 'NONE',  ( 0.000000000000000000, 88.70892494636771630, -26.21376805916498043 ) ) ;
#11967=DIRECTION ( 'NONE',  ( 0.000000000000000000, 0.000000000000000000, -1.000000000000000000 ) ) ;
#11968=ORIENTED_EDGE ( 'NONE', *, *, #687, .F. ) ;
#11970=AXIS2_PLACEMENT_3D ( 'NONE', #18751, #16877, #20518 ) ;
#11972=ORIENTED_EDGE ( 'NONE', *, *, #2046, .T. ) ;
#11973=DIRECTION ( 'NONE',  ( -1.000000000000000000, 0.000000000000000000, 0.000000000000000000 ) ) ;
#11975=AXIS2_PLACEMENT_3D ( 'NONE', #15112, #18665, #10352 ) ;
#11976=ORIENTED_EDGE ( 'NONE', *, *, #13363, .F. ) ;
#11982=CARTESIAN_POINT ( 'NONE',  ( 0.000000000000000000, 0.000000000000000000, 0.000000000000000000 ) ) ;
#11984=FACE_OUTER_BOUND ( 'NONE', #17500, .T. ) ;
#11985=DIRECTION ( 'NONE',  ( -1.000000000000000000, -0.000000000000000000, -0.000000000000000000 ) ) ;
#11988=FACE_OUTER_BOUND ( 'NONE', #5701, .T. ) ;
#11991=AXIS2_PLACEMENT_3D ( 'NONE', #8352, #15082, #8566 ) ;
#11992=DIRECTION ( 'NONE',  ( 0.000000000000000000, 0.000000000000000000, 1.000000000000000000 ) ) ;
#11994=ADVANCED_FACE ( 'NONE', ( #20970 ), #2623, .F. ) ;
#11996=CARTESIAN_POINT ( 'NONE',  ( 10.00000000000000000, 92.49798535263882115, 0.7467976319023850174 ) ) ;
#11997=ORIENTED_EDGE ( 'NONE', *, *, #3213, .F. ) ;
#11998=CYLINDRICAL_SURFACE ( 'NONE', #13394, 44.99999999999999289 ) ;
#12001=EDGE_CURVE ( 'NONE', #5809, #15140, #10081, .T. ) ;
#12005=ORIENTED_EDGE ( 'NONE', *, *, #11912, .T. ) ;
#12008=VERTEX_POINT ( 'NONE', #10799 ) ;
#12011=CARTESIAN_POINT ( 'NONE',  ( 0.000000000000000000, -8.925965667928249303, -92.06933331948791022 ) ) ;
#12012=CARTESIAN_POINT ( 'NONE',  ( 10.00000000000000000, 65.64563793391906188, -54.09103124042745492 ) ) ;
#12013=CARTESIAN_POINT ( 'NONE',  ( 0.000000000000000000, 46.07110168784925008, -74.97635353408335845 ) ) ;
#12014=DIRECTION ( 'NONE',  ( -1.000000000000000000, -0.000000000000000000, -0.000000000000000000 ) ) ;
#12016=DIRECTION ( 'NONE',  ( 0.000000000000000000, 0.000000000000000000, 1.000000000000000000 ) ) ;
#12017=VERTEX_POINT ( 'NONE', #5951 ) ;
#12018=DIRECTION ( 'NONE',  ( -1.000000000000000000, 0.000000000000000000, 0.000000000000000000 ) ) ;
#12019=DIRECTION ( 'NONE',  ( 0.000000000000000000, 0.000000000000000000, 1.000000000000000000 ) ) ;
#12021=EDGE_CURVE ( 'NONE', #13109, #1355, #914, .T. ) ;
#12022=EDGE_CURVE ( 'NONE', #20543, #15549, #12357, .T. ) ;
#12024=CYLINDRICAL_SURFACE ( 'NONE', #21423, 92.50100000000000477 ) ;
#12025=ORIENTED_EDGE ( 'NONE', *, *, #12288, .T. ) ;
#12028=ORIENTED_EDGE ( 'NONE', *, *, #11271, .T. ) ;
#12029=CARTESIAN_POINT ( 'NONE',  ( 0.000000000000000000, -41.87002153499162915, 74.04114219178029543 ) ) ;
#12030=ORIENTED_EDGE ( 'NONE', *, *, #2050, .T. ) ;
#12032=VERTEX_POINT ( 'NONE', #17339 ) ;
#12033=EDGE_CURVE ( 'NONE', #12565, #14140, #12568, .T. ) ;
#12034=CARTESIAN_POINT ( 'NONE',  ( 0.000000000000000000, -9.646732466564730046, -84.51112348751858860 ) ) ;
#12040=ADVANCED_FACE ( 'NONE', ( #9031 ), #15778, .F. ) ;
#12041=CARTESIAN_POINT ( 'NONE',  ( 10.00000000000000000, 0.000000000000000000, 0.000000000000000000 ) ) ;
#12042=CARTESIAN_POINT ( 'NONE',  ( 0.000000000000000000, -85.54350296776125617, 20.64725405482824883 ) ) ;
#12043=FACE_OUTER_BOUND ( 'NONE', #219, .T. ) ;
#12044=DIRECTION ( 'NONE',  ( 0.000000000000000000, 0.6427876096865353661, 0.7660444431189814551 ) ) ;
#12046=ORIENTED_EDGE ( 'NONE', *, *, #4468, .F. ) ;
#12047=CARTESIAN_POINT ( 'NONE',  ( 10.00000000000000000, 0.000000000000000000, 0.000000000000000000 ) ) ;
#12048=EDGE_CURVE ( 'NONE', #8158, #16874, #3746, .T. ) ;
#12050=VERTEX_POINT ( 'NONE', #15988 ) ;
#12051=DIRECTION ( 'NONE',  ( 0.000000000000000000, 0.000000000000000000, 1.000000000000000000 ) ) ;
#12056=ORIENTED_EDGE ( 'NONE', *, *, #12465, .T. ) ;
#12059=CARTESIAN_POINT ( 'NONE',  ( 0.000000000000000000, 65.83713140174806711, -58.39068529131128571 ) ) ;
#12061=LINE ( 'NONE', #20573, #1980 ) ;
#12066=DIRECTION ( 'NONE',  ( 0.000000000000000000, -0.06975647374413235235, 0.9975640502598237536 ) ) ;
#12067=VERTEX_POINT ( 'NONE', #9676 ) ;
#12071=DIRECTION ( 'NONE',  ( -1.000000000000000000, -0.000000000000000000, 0.000000000000000000 ) ) ;
#12073=DIRECTION ( 'NONE',  ( 0.000000000000000000, 0.000000000000000000, 1.000000000000000000 ) ) ;
#12074=ORIENTED_EDGE ( 'NONE', *, *, #9628, .F. ) ;
#12075=ORIENTED_EDGE ( 'NONE', *, *, #5519, .F. ) ;
#12076=CARTESIAN_POINT ( 'NONE',  ( 10.00000000000000000, -62.44821182181136976, 68.23969402963483333 ) ) ;
#12078=EDGE_LOOP ( 'NONE', ( #15507, #15924, #8473, #6938 ) ) ;
#12079=ORIENTED_EDGE ( 'NONE', *, *, #20367, .F. ) ;
#12080=FACE_OUTER_BOUND ( 'NONE', #1210, .T. ) ;
#12081=DIRECTION ( 'NONE',  ( -1.000000000000000000, 0.000000000000000000, 0.000000000000000000 ) ) ;
#12083=FACE_OUTER_BOUND ( 'NONE', #8151, .T. ) ;
#12085=CARTESIAN_POINT ( 'NONE',  ( 0.000000000000000000, 21.65267340503369198, -89.93106657554412209 ) ) ;
#12087=AXIS2_PLACEMENT_3D ( 'NONE', #3077, #11802, #21536 ) ;
#12088=DIRECTION ( 'NONE',  ( 1.000000000000000000, 0.000000000000000000, -0.000000000000000000 ) ) ;
#12089=FACE_OUTER_BOUND ( 'NONE', #1386, .T. ) ;
#12090=ORIENTED_EDGE ( 'NONE', *, *, #8241, .F. ) ;
#12091=DIRECTION ( 'NONE',  ( 0.000000000000000000, -0.7431448254773861395, -0.6691306063588672304 ) ) ;
#12093=CARTESIAN_POINT ( 'NONE',  ( 10.00000000000000000, -78.83848282823873888, -48.38314403117582430 ) ) ;
#12095=CYLINDRICAL_SURFACE ( 'NONE', #9416, 92.50100000000000477 ) ;
#12096=ORIENTED_EDGE ( 'NONE', *, *, #4782, .F. ) ;
#12097=CIRCLE ( 'NONE', #4657, 92.50100000000001899 ) ;
#12098=CARTESIAN_POINT ( 'NONE',  ( 10.00000000000000000, 71.33759994382042180, -58.88447872958914786 ) ) ;
#12101=CIRCLE ( 'NONE', #19514, 88.00000000000000000 ) ;
#12102=DIRECTION ( 'NONE',  ( 0.000000000000000000, -0.2079116908177664480, 0.9781476007338041345 ) ) ;
#12103=ORIENTED_EDGE ( 'NONE', *, *, #18393, .F. ) ;
#12104=ORIENTED_EDGE ( 'NONE', *, *, #13953, .F. ) ;
#12105=ORIENTED_EDGE ( 'NONE', *, *, #3418, .F. ) ;
#12107=EDGE_CURVE ( 'NONE', #3061, #3876, #11138, .T. ) ;
#12109=DIRECTION ( 'NONE',  ( 0.000000000000000000, 0.000000000000000000, 1.000000000000000000 ) ) ;
#12110=DIRECTION ( 'NONE',  ( 1.000000000000000000, 0.000000000000000000, 0.000000000000000000 ) ) ;
#12111=CARTESIAN_POINT ( 'NONE',  ( 0.000000000000000000, 47.19205848891765243, 74.27590198428138990 ) ) ;
#12113=CARTESIAN_POINT ( 'NONE',  ( 0.000000000000000000, 0.6609040254611577847, 87.99751818016873983 ) ) ;
#12115=DIRECTION ( 'NONE',  ( -1.000000000000000000, 0.000000000000000000, 0.000000000000000000 ) ) ;
#12116=CARTESIAN_POINT ( 'NONE',  ( -10.00000000000000000, 0.000000000000000000, 0.000000000000000000 ) ) ;
#12117=CARTESIAN_POINT ( 'NONE',  ( 0.000000000000000000, 71.72924546249947753, 45.71766382684695884 ) ) ;
#12118=ORIENTED_EDGE ( 'NONE', *, *, #19569, .F. ) ;
#12119=ADVANCED_FACE ( 'NONE', ( #9792 ), #4511, .F. ) ;
#12120=VECTOR ( 'NONE', #16267, 1000.000000000000000 ) ;
#12121=CYLINDRICAL_SURFACE ( 'NONE', #14804, 44.99999999999999289 ) ;
#12123=DIRECTION ( 'NONE',  ( 1.000000000000000000, 0.000000000000000000, 0.000000000000000000 ) ) ;
#12124=CARTESIAN_POINT ( 'NONE',  ( 0.000000000000000000, 6.797690662955227836, 87.73705831432218361 ) ) ;
#12126=CIRCLE ( 'NONE', #2251, 44.99999999999999289 ) ;
#12129=CARTESIAN_POINT ( 'NONE',  ( 0.000000000000000000, 70.37753541436022431, -60.02863908169561569 ) ) ;
#12130=VERTEX_POINT ( 'NONE', #18095 ) ;
#12134=ORIENTED_EDGE ( 'NONE', *, *, #3671, .F. ) ;
#12135=DIRECTION ( 'NONE',  ( 1.000000000000000000, 0.000000000000000000, 0.000000000000000000 ) ) ;
#12136=CARTESIAN_POINT ( 'NONE',  ( 10.00000000000000000, 0.000000000000000000, 0.000000000000000000 ) ) ;
#12137=CARTESIAN_POINT ( 'NONE',  ( 0.000000000000000000, -10.41137886060045048, -91.91321010181856366 ) ) ;
#12139=ADVANCED_FACE ( 'NONE', ( #14992 ), #8048, .F. ) ;
#12141=CIRCLE ( 'NONE', #1907, 88.00000000000000000 ) ;
#12142=CYLINDRICAL_SURFACE ( 'NONE', #2211, 92.50100000000000477 ) ;
#12147=VECTOR ( 'NONE', #17644, 1000.000000000000000 ) ;
#12151=EDGE_CURVE ( 'NONE', #2087, #17425, #14886, .T. ) ;
#12152=ORIENTED_EDGE ( 'NONE', *, *, #10439, .F. ) ;
#12153=EDGE_LOOP ( 'NONE', ( #18033, #19876, #6980, #13184 ) ) ;
#12154=EDGE_CURVE ( 'NONE', #2139, #17111, #21527, .T. ) ;
#12155=DIRECTION ( 'NONE',  ( -1.000000000000000000, -0.000000000000000000, -0.000000000000000000 ) ) ;
#12156=VECTOR ( 'NONE', #8837, 1000.000000000000000 ) ;
#12157=ORIENTED_EDGE ( 'NONE', *, *, #16389, .T. ) ;
#12163=VERTEX_POINT ( 'NONE', #3067 ) ;
#12164=EDGE_CURVE ( 'NONE', #3424, #12008, #15694, .T. ) ;
#12165=ADVANCED_FACE ( 'NONE', ( #12897 ), #1418, .F. ) ;
#12167=DIRECTION ( 'NONE',  ( -1.000000000000000000, -0.000000000000000000, -0.000000000000000000 ) ) ;
#12168=EDGE_CURVE ( 'NONE', #14884, #12349, #580, .T. ) ;
#12170=CARTESIAN_POINT ( 'NONE',  ( 10.00000000000000000, 0.000000000000000000, 0.000000000000000000 ) ) ;
#12171=DIRECTION ( 'NONE',  ( 0.000000000000000000, 0.000000000000000000, 1.000000000000000000 ) ) ;
#12172=DIRECTION ( 'NONE',  ( -1.000000000000000000, 0.000000000000000000, 0.000000000000000000 ) ) ;
#12174=CARTESIAN_POINT ( 'NONE',  ( 10.00000000000000000, 92.22057093985038989, -7.197311757039552838 ) ) ;
#12176=AXIS2_PLACEMENT_3D ( 'NONE', #15968, #835, #21061 ) ;
#12178=AXIS2_PLACEMENT_3D ( 'NONE', #10072, #18712, #13492 ) ;
#12179=EDGE_CURVE ( 'NONE', #9724, #15532, #1581, .T. ) ;
#12180=AXIS2_PLACEMENT_3D ( 'NONE', #6833, #3831, #12223 ) ;
#12181=DIRECTION ( 'NONE',  ( 1.000000000000000000, 0.000000000000000000, 0.000000000000000000 ) ) ;
#12184=VERTEX_POINT ( 'NONE', #16318 ) ;
#12185=CIRCLE ( 'NONE', #4085, 92.50100000000000477 ) ;
#12186=CARTESIAN_POINT ( 'NONE',  ( 10.00000000000000000, 0.000000000000000000, 0.000000000000000000 ) ) ;
#12192=AXIS2_PLACEMENT_3D ( 'NONE', #2547, #13047, #16258 ) ;
#12193=ORIENTED_EDGE ( 'NONE', *, *, #20575, .T. ) ;
#12194=DIRECTION ( 'NONE',  ( 0.000000000000000000, 0.000000000000000000, 1.000000000000000000 ) ) ;
#12195=CYLINDRICAL_SURFACE ( 'NONE', #1486, 88.00000000000000000 ) ;
#12198=EDGE_CURVE ( 'NONE', #19416, #7568, #6510, .T. ) ;
#12200=CARTESIAN_POINT ( 'NONE',  ( 10.00000000000000000, -89.12061559554348378, 24.77803214283513356 ) ) ;
#12201=CYLINDRICAL_SURFACE ( 'NONE', #18203, 88.00000000000000000 ) ;
#12203=LINE ( 'NONE', #10221, #13880 ) ;
#12205=EDGE_LOOP ( 'NONE', ( #6471, #16486, #721, #9674 ) ) ;
#12206=CARTESIAN_POINT ( 'NONE',  ( 0.000000000000000000, -86.66425444033897918, -32.33793443156484670 ) ) ;
#12208=AXIS2_PLACEMENT_3D ( 'NONE', #12047, #446, #13708 ) ;
#12209=EDGE_CURVE ( 'NONE', #5375, #7808, #13928, .T. ) ;
#12211=CARTESIAN_POINT ( 'NONE',  ( 0.000000000000000000, -40.72878876293093242, -78.00747250042492453 ) ) ;
#12217=EDGE_CURVE ( 'NONE', #21597, #13328, #3347, .T. ) ;
#12218=ORIENTED_EDGE ( 'NONE', *, *, #10712, .F. ) ;
#12220=ORIENTED_EDGE ( 'NONE', *, *, #21733, .T. ) ;
#12222=ORIENTED_EDGE ( 'NONE', *, *, #16251, .F. ) ;
#12223=DIRECTION ( 'NONE',  ( 0.000000000000000000, 0.7880107536067190166, 0.6156614753256620665 ) ) ;
#12224=DIRECTION ( 'NONE',  ( -1.000000000000000000, 0.000000000000000000, 0.000000000000000000 ) ) ;
#12226=DIRECTION ( 'NONE',  ( 0.000000000000000000, 0.000000000000000000, 1.000000000000000000 ) ) ;
#12227=CARTESIAN_POINT ( 'NONE',  ( 5.000000000000002665, -83.89484365856893078, -26.56417150043033359 ) ) ;
#12228=AXIS2_PLACEMENT_3D ( 'NONE', #2223, #20891, #21119 ) ;
#12232=CARTESIAN_POINT ( 'NONE',  ( 5.000000000000000000, 64.95266917914317162, 59.37298010462993858 ) ) ;
#12235=VERTEX_POINT ( 'NONE', #8265 ) ;
#12236=CIRCLE ( 'NONE', #5888, 44.99999999999999289 ) ;
#12238=CIRCLE ( 'NONE', #4488, 44.99999999999999289 ) ;
#12239=ORIENTED_EDGE ( 'NONE', *, *, #12945, .F. ) ;
#12240=DIRECTION ( 'NONE',  ( -1.000000000000000000, -0.000000000000000000, -0.000000000000000000 ) ) ;
#12241=AXIS2_PLACEMENT_3D ( 'NONE', #8612, #18895, #13586 ) ;
#12242=ORIENTED_EDGE ( 'NONE', *, *, #2702, .F. ) ;
#12243=ORIENTED_EDGE ( 'NONE', *, *, #919, .T. ) ;
#12244=ORIENTED_EDGE ( 'NONE', *, *, #11524, .F. ) ;
#12246=LINE ( 'NONE', #7171, #15333 ) ;
#12247=DIRECTION ( 'NONE',  ( -1.000000000000000000, -0.000000000000000000, 0.000000000000000000 ) ) ;
#12249=PRODUCT_DEFINITION_CONTEXT ( 'detailed design', #14469, 'design' ) ;
#12250=DIRECTION ( 'NONE',  ( -1.000000000000000000, -0.000000000000000000, -0.000000000000000000 ) ) ;
#12251=AXIS2_PLACEMENT_3D ( 'NONE', #7244, #6820, #8472 ) ;
#12252=CARTESIAN_POINT ( 'NONE',  ( 10.00000000000000000, 0.000000000000000000, 0.000000000000000000 ) ) ;
#12253=CARTESIAN_POINT ( 'NONE',  ( 5.000000000000002665, 12.90135963484197212, -87.04915231966633371 ) ) ;
#12259=VERTEX_POINT ( 'NONE', #14997 ) ;
#12261=ORIENTED_EDGE ( 'NONE', *, *, #7416, .F. ) ;
#12262=ORIENTED_EDGE ( 'NONE', *, *, #17805, .T. ) ;
#12263=AXIS2_PLACEMENT_3D ( 'NONE', #9953, #18268, #8198 ) ;
#12264=CYLINDRICAL_SURFACE ( 'NONE', #19783, 45.00000000000000000 ) ;
#12265=VERTEX_POINT ( 'NONE', #3185 ) ;
#12268=VERTEX_POINT ( 'NONE', #4425 ) ;
#12269=AXIS2_PLACEMENT_3D ( 'NONE', #20370, #5228, #11967 ) ;
#12272=ORIENTED_EDGE ( 'NONE', *, *, #14067, .F. ) ;
#12273=CARTESIAN_POINT ( 'NONE',  ( 10.00000000000000000, -35.18804927320584142, 80.65854690202667143 ) ) ;
#12274=CARTESIAN_POINT ( 'NONE',  ( 5.000000000000002665, 85.54350296776139828, -20.64725405482769460 ) ) ;
#12275=EDGE_CURVE ( 'NONE', #11314, #18794, #16092, .T. ) ;
#12276=CARTESIAN_POINT ( 'NONE',  ( 10.00000000000000000, -27.00677879429080974, 80.65868421664423238 ) ) ;
#12279=CARTESIAN_POINT ( 'NONE',  ( 10.00000000000000000, 87.96697768756401103, -2.410567674970879981 ) ) ;
#12281=DIRECTION ( 'NONE',  ( -1.000000000000000000, 0.000000000000000000, 0.000000000000000000 ) ) ;
#12284=AXIS2_PLACEMENT_3D ( 'NONE', #12390, #1019, #583 ) ;
#12286=ORIENTED_EDGE ( 'NONE', *, *, #3840, .T. ) ;
#12288=EDGE_CURVE ( 'NONE', #20720, #17060, #20298, .T. ) ;
#12289=EDGE_CURVE ( 'NONE', #20360, #16931, #19571, .T. ) ;
#12291=DIRECTION ( 'NONE',  ( -1.000000000000000000, -0.000000000000000000, -0.000000000000000000 ) ) ;
#12295=DIRECTION ( 'NONE',  ( 0.000000000000000000, 0.000000000000000000, 1.000000000000000000 ) ) ;
#12298=CIRCLE ( 'NONE', #5607, 44.99999999999999289 ) ;
#12299=DIRECTION ( 'NONE',  ( 1.000000000000000000, 0.000000000000000000, 0.000000000000000000 ) ) ;
#12301=ORIENTED_EDGE ( 'NONE', *, *, #1771, .T. ) ;
#12302=CARTESIAN_POINT ( 'NONE',  ( 10.00000000000000000, 88.70892494636771630, -26.21376805916497332 ) ) ;
#12303=AXIS2_PLACEMENT_3D ( 'NONE', #6395, #13105, #19844 ) ;
#12304=CARTESIAN_POINT ( 'NONE',  ( 10.00000000000000000, 57.53593069156372053, 72.42963261300981515 ) ) ;
#12307=FACE_OUTER_BOUND ( 'NONE', #10562, .T. ) ;
#12309=DIRECTION ( 'NONE',  ( 0.000000000000000000, 0.000000000000000000, 1.000000000000000000 ) ) ;
#12310=CARTESIAN_POINT ( 'NONE',  ( 10.00000000000000000, -78.80192417387900150, -39.16958956249377621 ) ) ;
#12311=DIRECTION ( 'NONE',  ( 1.000000000000000000, 0.000000000000000000, 0.000000000000000000 ) ) ;
#12312=EDGE_CURVE ( 'NONE', #5510, #1263, #2285, .T. ) ;
#12313=CYLINDRICAL_SURFACE ( 'NONE', #21129, 88.00000000000000000 ) ;
#12314=ORIENTED_EDGE ( 'NONE', *, *, #1411, .T. ) ;
#12315=DIRECTION ( 'NONE',  ( 0.000000000000000000, 0.000000000000000000, -1.000000000000000000 ) ) ;
#12317=ORIENTED_EDGE ( 'NONE', *, *, #7167, .F. ) ;
#12318=VECTOR ( 'NONE', #10556, 1000.000000000000000 ) ;
#12319=AXIS2_PLACEMENT_3D ( 'NONE', #18010, #8062, #1525 ) ;
#12320=DIRECTION ( 'NONE',  ( -1.000000000000000000, 0.000000000000000000, 0.000000000000000000 ) ) ;
#12321=ORIENTED_EDGE ( 'NONE', *, *, #11524, .T. ) ;
#12322=EDGE_CURVE ( 'NONE', #971, #1655, #16807, .T. ) ;
#12324=CARTESIAN_POINT ( 'NONE',  ( 10.00000000000000000, 8.925965667930086056, -92.06933331948771126 ) ) ;
#12326=FILL_AREA_STYLE ('',( #8998 ) ) ;
#12327=ORIENTED_EDGE ( 'NONE', *, *, #7160, .T. ) ;
#12328=ORIENTED_EDGE ( 'NONE', *, *, #13477, .T. ) ;
#12329=EDGE_LOOP ( 'NONE', ( #19101, #5103, #7430, #18705 ) ) ;
#12330=DIRECTION ( 'NONE',  ( 0.000000000000000000, -0.7431448254774000173, 0.6691306063588519093 ) ) ;
#12331=ORIENTED_EDGE ( 'NONE', *, *, #5432, .F. ) ;
#12332=CIRCLE ( 'NONE', #2215, 44.99999999999998579 ) ;
#12333=EDGE_CURVE ( 'NONE', #14447, #21500, #11796, .T. ) ;
#12334=CYLINDRICAL_SURFACE ( 'NONE', #4021, 92.50100000000000477 ) ;
#12335=CARTESIAN_POINT ( 'NONE',  ( 10.00000000000000000, -51.18896083639217665, -71.57995730992236361 ) ) ;
#12336=CARTESIAN_POINT ( 'NONE',  ( 10.00000000000000000, 0.000000000000000000, 0.000000000000000000 ) ) ;
#12340=DIRECTION ( 'NONE',  ( -1.000000000000000000, -0.000000000000000000, 0.000000000000000000 ) ) ;
#12342=CARTESIAN_POINT ( 'NONE',  ( 10.00000000000000000, 74.74361964203228581, -40.60271866773572214 ) ) ;
#12343=ADVANCED_FACE ( 'NONE', ( #16767 ), #8375, .F. ) ;
#12344=ORIENTED_EDGE ( 'NONE', *, *, #20048, .F. ) ;
#12349=VERTEX_POINT ( 'NONE', #3510 ) ;
#12350=LINE ( 'NONE', #10905, #18336 ) ;
#12351=ORIENTED_EDGE ( 'NONE', *, *, #15837, .T. ) ;
#12355=ORIENTED_EDGE ( 'NONE', *, *, #16759, .F. ) ;
#12356=ORIENTED_EDGE ( 'NONE', *, *, #8004, .T. ) ;
#12357=LINE ( 'NONE', #19099, #3733 ) ;
#12359=CYLINDRICAL_SURFACE ( 'NONE', #18675, 92.50100000000000477 ) ;
#12360=CARTESIAN_POINT ( 'NONE',  ( 10.00000000000000000, -31.15801000616886896, 79.14775961996379294 ) ) ;
#12361=CARTESIAN_POINT ( 'NONE',  ( 10.00000000000000000, 61.71252885873388294, 58.53847642588613809 ) ) ;
#12362=CARTESIAN_POINT ( 'NONE',  ( 10.00000000000000000, 79.38136668499741688, 37.98155635597341728 ) ) ;
#12364=FACE_OUTER_BOUND ( 'NONE', #2969, .T. ) ;
#12365=DIRECTION ( 'NONE',  ( -1.000000000000000000, -0.000000000000000000, -0.000000000000000000 ) ) ;
#12366=AXIS2_PLACEMENT_3D ( 'NONE', #788, #21456, #19576 ) ;
#12368=CARTESIAN_POINT ( 'NONE',  ( 0.000000000000000000, 0.000000000000000000, 0.000000000000000000 ) ) ;
#12369=VERTEX_POINT ( 'NONE', #20738 ) ;
#12370=DIRECTION ( 'NONE',  ( 1.000000000000000000, 0.000000000000000000, 0.000000000000000000 ) ) ;
#12371=VERTEX_POINT ( 'NONE', #3833 ) ;
#12373=VERTEX_POINT ( 'NONE', #5176 ) ;
#12376=ORIENTED_EDGE ( 'NONE', *, *, #10633, .T. ) ;
#12379=DIRECTION ( 'NONE',  ( -1.000000000000000000, -0.000000000000000000, -0.000000000000000000 ) ) ;
#12381=CYLINDRICAL_SURFACE ( 'NONE', #13584, 44.99999999999998579 ) ;
#12382=CARTESIAN_POINT ( 'NONE',  ( 10.00000000000000000, 84.12297548659721258, -12.59025161327029529 ) ) ;
#12383=ADVANCED_FACE ( 'NONE', ( #3722 ), #17319, .F. ) ;
#12384=CARTESIAN_POINT ( 'NONE',  ( 10.00000000000000000, -40.72878876293203376, 78.00747250042435610 ) ) ;
#12390=CARTESIAN_POINT ( 'NONE',  ( 10.00000000000000000, -84.90234713953988432, 5.175025661883520200 ) ) ;
#12393=CARTESIAN_POINT ( 'NONE',  ( 10.00000000000000000, -64.66851233300690183, -55.25552418573029456 ) ) ;
#12396=LINE ( 'NONE', #20589, #7174 ) ;
#12397=ORIENTED_EDGE ( 'NONE', *, *, #20816, .T. ) ;
#12399=ORIENTED_EDGE ( 'NONE', *, *, #13221, .F. ) ;
#12400=CARTESIAN_POINT ( 'NONE',  ( 5.000000000000002665, 5.479102470010468018, 87.82926298292115064 ) ) ;
#12401=DIRECTION ( 'NONE',  ( -1.000000000000000000, -0.000000000000000000, -0.000000000000000000 ) ) ;
#12402=LINE ( 'NONE', #19151, #14746 ) ;
#12403=EDGE_CURVE ( 'NONE', #8003, #1184, #11472, .T. ) ;
#12404=EDGE_CURVE ( 'NONE', #10332, #12482, #20996, .T. ) ;
#12407=CARTESIAN_POINT ( 'NONE',  ( 10.00000000000000000, -16.79755869217588682, -90.96305306542271296 ) ) ;
#12408=DIRECTION ( 'NONE',  ( 1.000000000000000000, 0.000000000000000000, 0.000000000000000000 ) ) ;
#12409=EDGE_CURVE ( 'NONE', #5185, #9562, #13231, .T. ) ;
#12412=ORIENTED_EDGE ( 'NONE', *, *, #3920, .F. ) ;
#12413=DIRECTION ( 'NONE',  ( 0.000000000000000000, 0.000000000000000000, -1.000000000000000000 ) ) ;
#12415=ORIENTED_EDGE ( 'NONE', *, *, #20048, .T. ) ;
#12416=CARTESIAN_POINT ( 'NONE',  ( 10.00000000000000000, 0.000000000000000000, 0.000000000000000000 ) ) ;
#12418=DIRECTION ( 'NONE',  ( 1.000000000000000000, -0.000000000000000000, -0.000000000000000000 ) ) ;
#12420=PRESENTATION_STYLE_ASSIGNMENT (( #10559 ) ) ;
#12421=ADVANCED_FACE ( 'NONE', ( #13781 ), #2071, .F. ) ;
#12424=VERTEX_POINT ( 'NONE', #12113 ) ;
#12425=VERTEX_POINT ( 'NONE', #7263 ) ;
#12426=CARTESIAN_POINT ( 'NONE',  ( 5.000000000000002665, -87.44637528609653998, -9.855528870799531660 ) ) ;
#12428=AXIS2_PLACEMENT_3D ( 'NONE', #4730, #3188, #11471 ) ;
#12429=VERTEX_POINT ( 'NONE', #13877 ) ;
#12430=DIRECTION ( 'NONE',  ( 0.000000000000000000, 0.000000000000000000, 1.000000000000000000 ) ) ;
#12432=CARTESIAN_POINT ( 'NONE',  ( 10.00000000000000000, 0.000000000000000000, 0.000000000000000000 ) ) ;
#12434=CARTESIAN_POINT ( 'NONE',  ( 10.00000000000000000, -9.646732466565913100, 84.51112348751846071 ) ) ;
#12435=CARTESIAN_POINT ( 'NONE',  ( 0.000000000000000000, 0.000000000000000000, 0.000000000000000000 ) ) ;
#12436=ADVANCED_FACE ( 'NONE', ( #19081 ), #18754, .F. ) ;
#12437=AXIS2_PLACEMENT_3D ( 'NONE', #8508, #9935, #8292 ) ;
#12440=CARTESIAN_POINT ( 'NONE',  ( 0.000000000000000000, 0.000000000000000000, 0.000000000000000000 ) ) ;
#12441=AXIS2_PLACEMENT_3D ( 'NONE', #21699, #21590, #3578 ) ;
#12443=EDGE_CURVE ( 'NONE', #12017, #17170, #20651, .T. ) ;
#12444=ORIENTED_EDGE ( 'NONE', *, *, #15946, .F. ) ;
#12446=ORIENTED_EDGE ( 'NONE', *, *, #3920, .T. ) ;
#12448=EDGE_CURVE ( 'NONE', #10147, #8155, #6198, .T. ) ;
#12450=CIRCLE ( 'NONE', #19522, 88.00000000000000000 ) ;
#12451=ORIENTED_EDGE ( 'NONE', *, *, #5464, .F. ) ;
#12452=EDGE_LOOP ( 'NONE', ( #3763, #1894, #16930, #11593 ) ) ;
#12453=CARTESIAN_POINT ( 'NONE',  ( 10.00000000000000000, -84.33453774737664332, 11.08490790852103380 ) ) ;
#12455=VERTEX_POINT ( 'NONE', #13991 ) ;
#12456=CARTESIAN_POINT ( 'NONE',  ( 10.00000000000000000, -47.19205848891816402, 74.27590198428104884 ) ) ;
#12457=VECTOR ( 'NONE', #2521, 1000.000000000000000 ) ;
#12459=DIRECTION ( 'NONE',  ( -1.000000000000000000, -0.000000000000000000, 0.000000000000000000 ) ) ;
#12460=LINE ( 'NONE', #8832, #7152 ) ;
#12461=DIRECTION ( 'NONE',  ( -1.000000000000000000, -0.000000000000000000, -0.000000000000000000 ) ) ;
#12462=CIRCLE ( 'NONE', #19880, 44.99999999999999289 ) ;
#12464=DIRECTION ( 'NONE',  ( -1.000000000000000000, 0.000000000000000000, -0.000000000000000000 ) ) ;
#12465=EDGE_CURVE ( 'NONE', #15522, #9323, #9688, .T. ) ;
#12466=CARTESIAN_POINT ( 'NONE',  ( 10.00000000000000000, 37.96946988134275358, -76.11510229470822253 ) ) ;
#12467=DIRECTION ( 'NONE',  ( 0.000000000000000000, 0.000000000000000000, 1.000000000000000000 ) ) ;
#12468=CARTESIAN_POINT ( 'NONE',  ( 10.00000000000000000, 0.000000000000000000, 0.000000000000000000 ) ) ;
#12470=CIRCLE ( 'NONE', #20602, 44.99999999999999289 ) ;
#12471=ORIENTED_EDGE ( 'NONE', *, *, #18242, .F. ) ;
#12472=CYLINDRICAL_SURFACE ( 'NONE', #11520, 88.00000000000000000 ) ;
#12474=ORIENTED_EDGE ( 'NONE', *, *, #11721, .T. ) ;
#12476=VERTEX_POINT ( 'NONE', #625 ) ;
#12478=ORIENTED_EDGE ( 'NONE', *, *, #11716, .T. ) ;
#12479=EDGE_CURVE ( 'NONE', #18348, #4328, #17492, .T. ) ;
#12480=ORIENTED_EDGE ( 'NONE', *, *, #4715, .T. ) ;
#12481=CARTESIAN_POINT ( 'NONE',  ( 0.000000000000000000, 16.79755869217770936, -90.96305306542237190 ) ) ;
#12482=VERTEX_POINT ( 'NONE', #9548 ) ;
#12483=DIRECTION ( 'NONE',  ( 0.000000000000000000, -0.06975647374413235235, 0.9975640502598237536 ) ) ;
#12484=DIRECTION ( 'NONE',  ( 0.000000000000000000, 0.000000000000000000, 1.000000000000000000 ) ) ;
#12486=LINE ( 'NONE', #14486, #13504 ) ;
#12491=DIRECTION ( 'NONE',  ( 0.000000000000000000, -0.9945218953682722907, -0.1045284632676635739 ) ) ;
#12492=VERTEX_POINT ( 'NONE', #7581 ) ;
#12494=AXIS2_PLACEMENT_3D ( 'NONE', #5088, #18577, #16915 ) ;
#12495=CIRCLE ( 'NONE', #3034, 44.99999999999999289 ) ;
#12496=FACE_OUTER_BOUND ( 'NONE', #498, .T. ) ;
#12497=CIRCLE ( 'NONE', #17460, 88.00000000000000000 ) ;
#12499=ORIENTED_EDGE ( 'NONE', *, *, #8531, .T. ) ;
#12504=DIRECTION ( 'NONE',  ( 0.000000000000000000, 0.000000000000000000, 1.000000000000000000 ) ) ;
#12505=ORIENTED_EDGE ( 'NONE', *, *, #2940, .F. ) ;
#12506=ORIENTED_EDGE ( 'NONE', *, *, #5982, .T. ) ;
#12509=CARTESIAN_POINT ( 'NONE',  ( 10.00000000000000000, 0.6609040254623582689, -87.99751818016873983 ) ) ;
#12511=CARTESIAN_POINT ( 'NONE',  ( 10.00000000000000000, -51.10509369859380513, -77.10190917907254970 ) ) ;
#12513=CIRCLE ( 'NONE', #523, 88.00000000000000000 ) ;
#12514=DIRECTION ( 'NONE',  ( 0.000000000000000000, 0.000000000000000000, 1.000000000000000000 ) ) ;
#12515=FACE_OUTER_BOUND ( 'NONE', #21521, .T. ) ;
#12520=AXIS2_PLACEMENT_3D ( 'NONE', #1360, #17827, #16602 ) ;
#12522=AXIS2_PLACEMENT_3D ( 'NONE', #17235, #2097, #8831 ) ;
#12523=CYLINDRICAL_SURFACE ( 'NONE', #15372, 92.50100000000000477 ) ;
#12525=VECTOR ( 'NONE', #1596, 1000.000000000000000 ) ;
#12526=CYLINDRICAL_SURFACE ( 'NONE', #21093, 44.99999999999999289 ) ;
#12529=EDGE_CURVE ( 'NONE', #3876, #21664, #19247, .T. ) ;
#12530=AXIS2_PLACEMENT_3D ( 'NONE', #8000, #8441, #21581 ) ;
#12531=AXIS2_PLACEMENT_3D ( 'NONE', #21608, #15083, #14651 ) ;
#12532=DIRECTION ( 'NONE',  ( 1.000000000000000000, 0.000000000000000000, 0.000000000000000000 ) ) ;
#12534=VECTOR ( 'NONE', #19478, 1000.000000000000000 ) ;
#12535=SURFACE_SIDE_STYLE ('',( #4029 ) ) ;
#12536=AXIS2_PLACEMENT_3D ( 'NONE', #4755, #12808, #2654 ) ;
#12538=VERTEX_POINT ( 'NONE', #14203 ) ;
#12541=CARTESIAN_POINT ( 'NONE',  ( 10.00000000000000000, -88.70892494636754577, 26.21376805916555242 ) ) ;
#12542=ADVANCED_FACE ( 'NONE', ( #6046 ), #1062, .F. ) ;
#12543=ORIENTED_EDGE ( 'NONE', *, *, #2878, .F. ) ;
#12546=DIRECTION ( 'NONE',  ( 0.000000000000000000, 0.000000000000000000, -1.000000000000000000 ) ) ;
#12547=DIRECTION ( 'NONE',  ( 1.000000000000000000, 0.000000000000000000, 0.000000000000000000 ) ) ;
#12550=AXIS2_PLACEMENT_3D ( 'NONE', #14493, #6101, #2992 ) ;
#12552=AXIS2_PLACEMENT_3D ( 'NONE', #19946, #18306, #16634 ) ;
#12553=CARTESIAN_POINT ( 'NONE',  ( -10.00000000000000000, 0.000000000000000000, 0.000000000000000000 ) ) ;
#12554=CIRCLE ( 'NONE', #21382, 92.50100000000000477 ) ;
#12555=DIRECTION ( 'NONE',  ( -1.000000000000000000, -0.000000000000000000, -0.000000000000000000 ) ) ;
#12557=EDGE_CURVE ( 'NONE', #12259, #966, #2829, .T. ) ;
#12558=DIRECTION ( 'NONE',  ( 0.000000000000000000, 0.000000000000000000, 1.000000000000000000 ) ) ;
#12559=EDGE_CURVE ( 'NONE', #7099, #4539, #7592, .T. ) ;
#12561=ORIENTED_EDGE ( 'NONE', *, *, #2736, .F. ) ;
#12562=DIRECTION ( 'NONE',  ( 0.000000000000000000, 0.7880107536067231244, -0.6156614753256566264 ) ) ;
#12563=EDGE_LOOP ( 'NONE', ( #7413, #3737, #3871, #3196 ) ) ;
#12564=EDGE_CURVE ( 'NONE', #6526, #5435, #19943, .T. ) ;
#12565=VERTEX_POINT ( 'NONE', #10891 ) ;
#12566=CIRCLE ( 'NONE', #1994, 88.00000000000000000 ) ;
#12567=ORIENTED_EDGE ( 'NONE', *, *, #3505, .F. ) ;
#12568=LINE ( 'NONE', #4067, #13265 ) ;
#12569=AXIS2_PLACEMENT_3D ( 'NONE', #3126, #19919, #21473 ) ;
#12570=ORIENTED_EDGE ( 'NONE', *, *, #19051, .T. ) ;
#12572=DIRECTION ( 'NONE',  ( 1.000000000000000000, 0.000000000000000000, 0.000000000000000000 ) ) ;
#12575=CARTESIAN_POINT ( 'NONE',  ( 0.000000000000000000, -52.25832601289145884, 70.80301803122767978 ) ) ;
#12577=DIRECTION ( 'NONE',  ( 0.000000000000000000, -0.1391731009600725433, 0.9902680687415692518 ) ) ;
#12579=CARTESIAN_POINT ( 'NONE',  ( 10.00000000000000000, 0.000000000000000000, 0.000000000000000000 ) ) ;
#12580=EDGE_CURVE ( 'NONE', #5874, #9950, #12885, .T. ) ;
#12581=DIRECTION ( 'NONE',  ( 0.000000000000000000, 0.000000000000000000, 1.000000000000000000 ) ) ;
#12590=VERTEX_POINT ( 'NONE', #5708 ) ;
#12592=DIRECTION ( 'NONE',  ( 0.000000000000000000, 0.9945218953682729568, 0.1045284632676569958 ) ) ;
#12593=ORIENTED_EDGE ( 'NONE', *, *, #13462, .T. ) ;
#12594=CIRCLE ( 'NONE', #11555, 88.00000000000000000 ) ;
#12595=CARTESIAN_POINT ( 'NONE',  ( 5.000000000000002665, -87.92084725184950855, 3.731570516142653116 ) ) ;
#12597=FACE_OUTER_BOUND ( 'NONE', #3793, .T. ) ;
#12599=CARTESIAN_POINT ( 'NONE',  ( 10.00000000000000000, 27.87320266523671819, -88.20158487341731757 ) ) ;
#12601=DIRECTION ( 'NONE',  ( -1.000000000000000000, 0.000000000000000000, -0.000000000000000000 ) ) ;
#12602=CARTESIAN_POINT ( 'NONE',  ( 10.00000000000000000, 85.05652083079336023, -0.7600687895862878740 ) ) ;
#12604=EDGE_CURVE ( 'NONE', #791, #6638, #3365, .T. ) ;
#12605=VERTEX_POINT ( 'NONE', #21277 ) ;
#12606=EDGE_CURVE ( 'NONE', #17077, #8172, #17535, .T. ) ;
#12607=DIRECTION ( 'NONE',  ( -1.000000000000000000, 0.000000000000000000, 0.000000000000000000 ) ) ;
#12608=VECTOR ( 'NONE', #553, 1000.000000000000000 ) ;
#12609=CIRCLE ( 'NONE', #617, 44.99999999999999289 ) ;
#12610=AXIS2_PLACEMENT_3D ( 'NONE', #6301, #11469, #979 ) ;
#12611=CARTESIAN_POINT ( 'NONE',  ( 0.000000000000000000, 0.000000000000000000, 0.000000000000000000 ) ) ;
#12612=DIRECTION ( 'NONE',  ( -1.000000000000000000, 0.000000000000000000, 0.000000000000000000 ) ) ;
#12613=VECTOR ( 'NONE', #17803, 1000.000000000000000 ) ;
#12614=ORIENTED_EDGE ( 'NONE', *, *, #17184, .F. ) ;
#12615=DIRECTION ( 'NONE',  ( 0.000000000000000000, 0.000000000000000000, 1.000000000000000000 ) ) ;
#12616=ORIENTED_EDGE ( 'NONE', *, *, #12033, .F. ) ;
#12617=CARTESIAN_POINT ( 'NONE',  ( 0.000000000000000000, -90.63195040374175449, -18.50093422002511900 ) ) ;
#12620=DIRECTION ( 'NONE',  ( -1.000000000000000000, -0.000000000000000000, -0.000000000000000000 ) ) ;
#12622=AXIS2_PLACEMENT_3D ( 'NONE', #7685, #15872, #2380 ) ;
#12625=CARTESIAN_POINT ( 'NONE',  ( 10.00000000000000000, -46.89573839703331259, 79.73220629831473616 ) ) ;
#12627=CYLINDRICAL_SURFACE ( 'NONE', #9720, 44.99999999999999289 ) ;
#12628=CIRCLE ( 'NONE', #19681, 45.00000000000000000 ) ;
#12629=DIRECTION ( 'NONE',  ( -1.000000000000000000, 0.000000000000000000, 0.000000000000000000 ) ) ;
#12630=AXIS2_PLACEMENT_3D ( 'NONE', #16387, #1577, #11531 ) ;
#12633=DIRECTION ( 'NONE',  ( -1.000000000000000000, 0.000000000000000000, 0.000000000000000000 ) ) ;
#12634=VERTEX_POINT ( 'NONE', #14759 ) ;
#12635=CARTESIAN_POINT ( 'NONE',  ( 10.00000000000000000, 92.22057093985038989, -7.197311757039552838 ) ) ;
#12637=CARTESIAN_POINT ( 'NONE',  ( 10.00000000000000000, -74.39348546125087580, 54.97312363261389834 ) ) ;
#12639=AXIS2_PLACEMENT_3D ( 'NONE', #4748, #1438, #11492 ) ;
#12641=VECTOR ( 'NONE', #16351, 1000.000000000000000 ) ;
#12642=AXIS2_PLACEMENT_3D ( 'NONE', #13158, #6340, #19907 ) ;
#12643=DIRECTION ( 'NONE',  ( -1.000000000000000000, -0.000000000000000000, -0.000000000000000000 ) ) ;
#12645=ORIENTED_EDGE ( 'NONE', *, *, #12021, .T. ) ;
#12649=CYLINDRICAL_SURFACE ( 'NONE', #19898, 44.99999999999999289 ) ;
#12650=CARTESIAN_POINT ( 'NONE',  ( 0.000000000000000000, 0.000000000000000000, 0.000000000000000000 ) ) ;
#12651=ORIENTED_EDGE ( 'NONE', *, *, #2050, .F. ) ;
#12654=DIRECTION ( 'NONE',  ( -1.000000000000000000, -0.000000000000000000, -0.000000000000000000 ) ) ;
#12655=AXIS2_PLACEMENT_3D ( 'NONE', #19407, #20953, #11116 ) ;
#12659=AXIS2_PLACEMENT_3D ( 'NONE', #11889, #3274, #13437 ) ;
#12661=ORIENTED_EDGE ( 'NONE', *, *, #7481, .F. ) ;
#12663=CARTESIAN_POINT ( 'NONE',  ( 0.000000000000000000, -88.70892494636720471, -26.21376805916674613 ) ) ;
#12665=EDGE_CURVE ( 'NONE', #13330, #15096, #7252, .T. ) ;
#12667=AXIS2_PLACEMENT_3D ( 'NONE', #15494, #578, #20687 ) ;
#12668=VERTEX_POINT ( 'NONE', #2929 ) ;
#12670=ORIENTED_EDGE ( 'NONE', *, *, #13503, .F. ) ;
#12672=ORIENTED_EDGE ( 'NONE', *, *, #3282, .T. ) ;
#12674=AXIS2_PLACEMENT_3D ( 'NONE', #820, #15865, #14299 ) ;
#12675=ORIENTED_EDGE ( 'NONE', *, *, #6217, .T. ) ;
#12677=DIRECTION ( 'NONE',  ( -1.000000000000000000, -0.000000000000000000, -0.000000000000000000 ) ) ;
#12678=AXIS2_PLACEMENT_3D ( 'NONE', #19869, #16564, #1430 ) ;
#12680=LINE ( 'NONE', #19421, #4547 ) ;
#12684=CARTESIAN_POINT ( 'NONE',  ( 10.00000000000000000, 0.000000000000000000, 0.000000000000000000 ) ) ;
#12685=EDGE_CURVE ( 'NONE', #15558, #15756, #10059, .T. ) ;
#12686=CARTESIAN_POINT ( 'NONE',  ( 10.00000000000000000, 0.000000000000000000, 0.000000000000000000 ) ) ;
#12689=ADVANCED_FACE ( 'NONE', ( #9887 ), #20169, .F. ) ;
#12692=EDGE_CURVE ( 'NONE', #10982, #12032, #18074, .T. ) ;
#12696=ORIENTED_EDGE ( 'NONE', *, *, #4573, .T. ) ;
#12700=ORIENTED_EDGE ( 'NONE', *, *, #8783, .F. ) ;
#12702=EDGE_CURVE ( 'NONE', #16808, #2427, #19261, .T. ) ;
#12705=DIRECTION ( 'NONE',  ( 0.000000000000000000, 0.000000000000000000, 1.000000000000000000 ) ) ;
#12708=DIRECTION ( 'NONE',  ( -1.000000000000000000, -0.000000000000000000, -0.000000000000000000 ) ) ;
#12709=CARTESIAN_POINT ( 'NONE',  ( 10.00000000000000000, -2.208823992044743445, 85.03123271466935762 ) ) ;
#12712=DIRECTION ( 'NONE',  ( -1.000000000000000000, -0.000000000000000000, 0.000000000000000000 ) ) ;
#12713=DIRECTION ( 'NONE',  ( -1.000000000000000000, 0.000000000000000000, -0.000000000000000000 ) ) ;
#12714=DIRECTION ( 'NONE',  ( -1.000000000000000000, 0.000000000000000000, 0.000000000000000000 ) ) ;
#12716=EDGE_LOOP ( 'NONE', ( #7240, #20941, #12272, #8123 ) ) ;
#12717=CYLINDRICAL_SURFACE ( 'NONE', #15727, 88.00000000000000000 ) ;
#12718=CIRCLE ( 'NONE', #3201, 44.99999999999998579 ) ;
#12719=DIRECTION ( 'NONE',  ( -1.000000000000000000, -0.000000000000000000, 0.000000000000000000 ) ) ;
#12720=ADVANCED_FACE ( 'NONE', ( #13194 ), #9772, .F. ) ;
#12722=ORIENTED_EDGE ( 'NONE', *, *, #4350, .T. ) ;
#12723=DIRECTION ( 'NONE',  ( 0.000000000000000000, 0.000000000000000000, 1.000000000000000000 ) ) ;
#12725=ADVANCED_FACE ( 'NONE', ( #4931 ), #19731, .F. ) ;
#12730=EDGE_LOOP ( 'NONE', ( #17465, #3360, #6802, #6786 ) ) ;
#12731=ORIENTED_EDGE ( 'NONE', *, *, #9840, .T. ) ;
#12733=CARTESIAN_POINT ( 'NONE',  ( 10.00000000000000000, 82.02147376274727719, -42.76579056660780509 ) ) ;
#12734=CARTESIAN_POINT ( 'NONE',  ( 10.00000000000000000, 0.000000000000000000, 0.000000000000000000 ) ) ;
#12736=CYLINDRICAL_SURFACE ( 'NONE', #13233, 92.50100000000000477 ) ;
#12739=DIRECTION ( 'NONE',  ( 1.000000000000000000, 0.000000000000000000, 0.000000000000000000 ) ) ;
#12740=CARTESIAN_POINT ( 'NONE',  ( 10.00000000000000000, 81.55207211302045778, 24.17537951050201883 ) ) ;
#12741=DIRECTION ( 'NONE',  ( 0.000000000000000000, -0.2079116908177468248, -0.9781476007338083534 ) ) ;
#12742=CARTESIAN_POINT ( 'NONE',  ( -10.00000000000000000, 0.000000000000000000, 0.000000000000000000 ) ) ;
#12745=CYLINDRICAL_SURFACE ( 'NONE', #4802, 45.00000000000000000 ) ;
#12750=ORIENTED_EDGE ( 'NONE', *, *, #11490, .T. ) ;
#12753=EDGE_LOOP ( 'NONE', ( #15779, #10309, #10384, #20973 ) ) ;
#12754=ORIENTED_EDGE ( 'NONE', *, *, #1533, .T. ) ;
#12756=CARTESIAN_POINT ( 'NONE',  ( 10.00000000000000000, -14.02138820414853448, -83.89630571862299746 ) ) ;
#12757=ORIENTED_EDGE ( 'NONE', *, *, #10613, .T. ) ;
#12764=CARTESIAN_POINT ( 'NONE',  ( 5.000000000000002665, -24.89070495400792637, 84.40647372620493627 ) ) ;
#12765=DIRECTION ( 'NONE',  ( -1.000000000000000000, 0.000000000000000000, 0.000000000000000000 ) ) ;
#12767=ORIENTED_EDGE ( 'NONE', *, *, #372, .T. ) ;
#12770=ORIENTED_EDGE ( 'NONE', *, *, #18037, .T. ) ;
#12772=VERTEX_POINT ( 'NONE', #15074 ) ;
#12773=DIRECTION ( 'NONE',  ( 0.000000000000000000, 0.000000000000000000, -1.000000000000000000 ) ) ;
#12774=VERTEX_POINT ( 'NONE', #16733 ) ;
#12775=ADVANCED_FACE ( 'NONE', ( #1604 ), #11765, .F. ) ;
#12776=ORIENTED_EDGE ( 'NONE', *, *, #14096, .F. ) ;
#12778=VERTEX_POINT ( 'NONE', #4697 ) ;
#12779=DIRECTION ( 'NONE',  ( -1.000000000000000000, -0.000000000000000000, -0.000000000000000000 ) ) ;
#12781=CARTESIAN_POINT ( 'NONE',  ( 5.000000000000000000, 75.87763420127893710, -44.57111876559645225 ) ) ;
#12783=DIRECTION ( 'NONE',  ( -1.000000000000000000, 0.000000000000000000, 0.000000000000000000 ) ) ;
#12784=ADVANCED_FACE ( 'NONE', ( #384 ), #12201, .F. ) ;
#12790=CIRCLE ( 'NONE', #1165, 88.00000000000000000 ) ;
#12794=ORIENTED_EDGE ( 'NONE', *, *, #3290, .F. ) ;
#12798=ORIENTED_EDGE ( 'NONE', *, *, #8665, .F. ) ;
#12799=EDGE_CURVE ( 'NONE', #16358, #12017, #6572, .T. ) ;
#12801=ORIENTED_EDGE ( 'NONE', *, *, #2437, .T. ) ;
#12804=FACE_OUTER_BOUND ( 'NONE', #8539, .T. ) ;
#12805=CARTESIAN_POINT ( 'NONE',  ( 0.000000000000000000, 0.000000000000000000, 0.000000000000000000 ) ) ;
#12808=DIRECTION ( 'NONE',  ( -1.000000000000000000, -0.000000000000000000, -0.000000000000000000 ) ) ;
#12809=CYLINDRICAL_SURFACE ( 'NONE', #7865, 44.99999999999999289 ) ;
#12811=CARTESIAN_POINT ( 'NONE',  ( 10.00000000000000000, 67.05625154133453236, 63.71729851637834940 ) ) ;
#12815=AXIS2_PLACEMENT_3D ( 'NONE', #7125, #6809, #3371 ) ;
#12820=AXIS2_PLACEMENT_3D ( 'NONE', #18482, #14940, #19918 ) ;
#12823=CARTESIAN_POINT ( 'NONE',  ( 10.00000000000000000, 0.000000000000000000, 0.000000000000000000 ) ) ;
#12825=EDGE_CURVE ( 'NONE', #12425, #17806, #15018, .T. ) ;
#12827=EDGE_CURVE ( 'NONE', #11727, #659, #8669, .T. ) ;
#12828=EDGE_CURVE ( 'NONE', #12830, #12032, #6215, .T. ) ;
#12829=LINE ( 'NONE', #7335, #15357 ) ;
#12830=VERTEX_POINT ( 'NONE', #12085 ) ;
#12831=ORIENTED_EDGE ( 'NONE', *, *, #2179, .T. ) ;
#12833=DIRECTION ( 'NONE',  ( 1.000000000000000000, 0.000000000000000000, 0.000000000000000000 ) ) ;
#12834=EDGE_CURVE ( 'NONE', #2240, #16026, #14673, .T. ) ;
#12835=ORIENTED_EDGE ( 'NONE', *, *, #2470, .F. ) ;
#12836=ORIENTED_EDGE ( 'NONE', *, *, #16538, .T. ) ;
#12839=LINE ( 'NONE', #14508, #4560 ) ;
#12843=CARTESIAN_POINT ( 'NONE',  ( 0.000000000000000000, 66.01871308925549897, -64.79170103522952218 ) ) ;
#12845=DIRECTION ( 'NONE',  ( -1.000000000000000000, -0.000000000000000000, -0.000000000000000000 ) ) ;
#12846=EDGE_CURVE ( 'NONE', #2607, #18262, #4790, .T. ) ;
#12848=CIRCLE ( 'NONE', #9651, 45.00000000000000711 ) ;
#12851=EDGE_CURVE ( 'NONE', #1865, #17490, #19960, .T. ) ;
#12852=CARTESIAN_POINT ( 'NONE',  ( 0.000000000000000000, -86.66425444033941972, 32.33793443156368141 ) ) ;
#12853=VECTOR ( 'NONE', #21058, 1000.000000000000000 ) ;
#12854=ORIENTED_EDGE ( 'NONE', *, *, #19492, .T. ) ;
#12856=EDGE_CURVE ( 'NONE', #15286, #12492, #17181, .T. ) ;
#12857=CARTESIAN_POINT ( 'NONE',  ( 0.000000000000000000, 8.134922360106093819, 84.67002113262482510 ) ) ;
#12858=LINE ( 'NONE', #8446, #10224 ) ;
#12860=ORIENTED_EDGE ( 'NONE', *, *, #18514, .F. ) ;
#12863=EDGE_CURVE ( 'NONE', #21566, #18952, #8778, .T. ) ;
#12864=VERTEX_POINT ( 'NONE', #13967 ) ;
#12867=CYLINDRICAL_SURFACE ( 'NONE', #5786, 44.99999999999998579 ) ;
#12869=ORIENTED_EDGE ( 'NONE', *, *, #8090, .T. ) ;
#12872=DIRECTION ( 'NONE',  ( 0.000000000000000000, 0.000000000000000000, 1.000000000000000000 ) ) ;
#12876=AXIS2_PLACEMENT_3D ( 'NONE', #4955, #6620, #21299 ) ;
#12877=DIRECTION ( 'NONE',  ( 0.000000000000000000, 0.000000000000000000, 1.000000000000000000 ) ) ;
#12879=EDGE_CURVE ( 'NONE', #19613, #13415, #6931, .T. ) ;
#12880=DIRECTION ( 'NONE',  ( 1.000000000000000000, -0.000000000000000000, -0.000000000000000000 ) ) ;
#12882=ORIENTED_EDGE ( 'NONE', *, *, #12217, .T. ) ;
#12884=AXIS2_PLACEMENT_3D ( 'NONE', #151, #16953, #1808 ) ;
#12885=CIRCLE ( 'NONE', #12176, 44.99999999999999289 ) ;
#12886=EDGE_CURVE ( 'NONE', #1075, #15764, #898, .T. ) ;
#12887=DIRECTION ( 'NONE',  ( 1.000000000000000000, 0.000000000000000000, 0.000000000000000000 ) ) ;
#12889=ORIENTED_EDGE ( 'NONE', *, *, #5006, .T. ) ;
#12891=CARTESIAN_POINT ( 'NONE',  ( 0.000000000000000000, 71.33759994382042180, -58.88447872958914786 ) ) ;
#12892=ORIENTED_EDGE ( 'NONE', *, *, #12022, .T. ) ;
#12893=CARTESIAN_POINT ( 'NONE',  ( 5.000000000000002665, -87.92084725184945171, -3.731570516143874361 ) ) ;
#12895=ORIENTED_EDGE ( 'NONE', *, *, #14488, .F. ) ;
#12897=FACE_OUTER_BOUND ( 'NONE', #4480, .T. ) ;
#12898=ORIENTED_EDGE ( 'NONE', *, *, #19488, .T. ) ;
#12900=CARTESIAN_POINT ( 'NONE',  ( 10.00000000000000000, -16.79755869217588682, -90.96305306542271296 ) ) ;
#12901=CARTESIAN_POINT ( 'NONE',  ( 0.000000000000000000, 0.000000000000000000, 0.000000000000000000 ) ) ;
#12902=VECTOR ( 'NONE', #18698, 1000.000000000000000 ) ;
#12903=VECTOR ( 'NONE', #15740, 1000.000000000000000 ) ;
#12904=DIRECTION ( 'NONE',  ( 0.000000000000000000, -0.9848077530122096857, 0.1736481776669207000 ) ) ;
#12907=DIRECTION ( 'NONE',  ( 0.000000000000000000, -0.9510565162951565288, 0.3090169943749382919 ) ) ;
#12908=DIRECTION ( 'NONE',  ( 0.000000000000000000, 0.7431448254773910245, 0.6691306063588617903 ) ) ;
#12909=DIRECTION ( 'NONE',  ( 1.000000000000000000, 0.000000000000000000, 0.000000000000000000 ) ) ;
#12910=DIRECTION ( 'NONE',  ( 0.000000000000000000, 0.000000000000000000, 1.000000000000000000 ) ) ;
#12912=CIRCLE ( 'NONE', #7986, 88.00000000000000000 ) ;
#12913=ORIENTED_EDGE ( 'NONE', *, *, #11942, .F. ) ;
#12914=AXIS2_PLACEMENT_3D ( 'NONE', #6658, #17020, #18792 ) ;
#12915=ORIENTED_EDGE ( 'NONE', *, *, #6971, .F. ) ;
#12916=VECTOR ( 'NONE', #3564, 1000.000000000000000 ) ;
#12917=ORIENTED_EDGE ( 'NONE', *, *, #20119, .T. ) ;
#12918=ORIENTED_EDGE ( 'NONE', *, *, #15653, .T. ) ;
#12920=CARTESIAN_POINT ( 'NONE',  ( 0.000000000000000000, -90.32141448704695108, 19.96189084378192291 ) ) ;
#12921=EDGE_LOOP ( 'NONE', ( #4708, #533, #8231, #19384 ) ) ;
#12924=CARTESIAN_POINT ( 'NONE',  ( 0.000000000000000000, -75.87763420127802760, -44.57111876559801544 ) ) ;
#12925=CARTESIAN_POINT ( 'NONE',  ( 10.00000000000000000, 2.481790431840499966, -92.46770094066590673 ) ) ;
#12927=AXIS2_PLACEMENT_3D ( 'NONE', #9068, #15819, #4106 ) ;
#12928=DIRECTION ( 'NONE',  ( -1.000000000000000000, -0.000000000000000000, 0.000000000000000000 ) ) ;
#12929=CYLINDRICAL_SURFACE ( 'NONE', #2005, 92.50100000000000477 ) ;
#12931=ADVANCED_FACE ( 'NONE', ( #15615 ), #7232, .F. ) ;
#12932=VERTEX_POINT ( 'NONE', #19054 ) ;
#12933=CARTESIAN_POINT ( 'NONE',  ( 10.00000000000000000, -84.90234713953981327, -5.175025661884713912 ) ) ;
#12934=ORIENTED_EDGE ( 'NONE', *, *, #7988, .T. ) ;
#12935=EDGE_CURVE ( 'NONE', #4602, #6281, #7271, .T. ) ;
#12936=LINE ( 'NONE', #4658, #1710 ) ;
#12937=AXIS2_PLACEMENT_3D ( 'NONE', #21555, #14700, #3101 ) ;
#12939=ORIENTED_EDGE ( 'NONE', *, *, #7050, .F. ) ;
#12940=AXIS2_PLACEMENT_3D ( 'NONE', #19515, #12555, #743 ) ;
#12945=EDGE_CURVE ( 'NONE', #21410, #21168, #19611, .T. ) ;
#12946=CARTESIAN_POINT ( 'NONE',  ( 10.00000000000000000, 25.56104204395304080, 81.12843256239672485 ) ) ;
#12947=ORIENTED_EDGE ( 'NONE', *, *, #17184, .T. ) ;
#12948=ORIENTED_EDGE ( 'NONE', *, *, #16182, .T. ) ;
#12949=CARTESIAN_POINT ( 'NONE',  ( 10.00000000000000000, 86.54587337002898551, -15.93147207946920396 ) ) ;
#12950=CARTESIAN_POINT ( 'NONE',  ( 10.00000000000000000, -92.22057093985026199, -7.197311757041478408 ) ) ;
#12951=CARTESIAN_POINT ( 'NONE',  ( 10.00000000000000000, -15.51843147776295950, -83.63233659819665888 ) ) ;
#12952=DIRECTION ( 'NONE',  ( 1.000000000000000000, 0.000000000000000000, 0.000000000000000000 ) ) ;
#12953=DIRECTION ( 'NONE',  ( 1.000000000000000000, 0.000000000000000000, 0.000000000000000000 ) ) ;
#12954=DIRECTION ( 'NONE',  ( 0.000000000000000000, 0.000000000000000000, 1.000000000000000000 ) ) ;
#12956=FACE_OUTER_BOUND ( 'NONE', #15413, .T. ) ;
#12957=DIRECTION ( 'NONE',  ( 0.000000000000000000, 1.773272886554069860E-14, -1.000000000000000000 ) ) ;
#12958=AXIS2_PLACEMENT_3D ( 'NONE', #1315, #8061, #19655 ) ;
#12959=ADVANCED_FACE ( 'NONE', ( #7550 ), #20919, .F. ) ;
#12960=ADVANCED_FACE ( 'NONE', ( #1036 ), #12627, .F. ) ;
#12962=ADVANCED_FACE ( 'NONE', ( #4242 ), #8980, .F. ) ;
#12963=ORIENTED_EDGE ( 'NONE', *, *, #9509, .F. ) ;
#12965=AXIS2_PLACEMENT_3D ( 'NONE', #19297, #11227, #16414 ) ;
#12966=EDGE_CURVE ( 'NONE', #12565, #4587, #17506, .T. ) ;
#12967=VERTEX_POINT ( 'NONE', #5902 ) ;
#12969=LINE ( 'NONE', #14850, #5993 ) ;
#12970=ORIENTED_EDGE ( 'NONE', *, *, #1784, .F. ) ;
#12972=EDGE_CURVE ( 'NONE', #52, #12455, #19266, .T. ) ;
#12973=CIRCLE ( 'NONE', #18982, 88.00000000000000000 ) ;
#12974=ORIENTED_EDGE ( 'NONE', *, *, #1587, .F. ) ;
#12975=ORIENTED_EDGE ( 'NONE', *, *, #15248, .F. ) ;
#12978=AXIS2_PLACEMENT_3D ( 'NONE', #11222, #6266, #15967 ) ;
#12980=DIRECTION ( 'NONE',  ( 1.000000000000000000, -0.000000000000000000, 0.000000000000000000 ) ) ;
#12982=ORIENTED_EDGE ( 'NONE', *, *, #15695, .T. ) ;
#12984=CARTESIAN_POINT ( 'NONE',  ( 10.00000000000000000, -83.03980459022467642, -18.42770452393328995 ) ) ;
#12987=CARTESIAN_POINT ( 'NONE',  ( 10.00000000000000000, 23.10190250628834718, 89.56973317806607326 ) ) ;
#12991=ORIENTED_EDGE ( 'NONE', *, *, #9687, .F. ) ;
#12993=CIRCLE ( 'NONE', #15823, 44.99999999999999289 ) ;
#12994=EDGE_CURVE ( 'NONE', #11658, #21836, #11488, .T. ) ;
#12995=FACE_OUTER_BOUND ( 'NONE', #9978, .T. ) ;
#12996=ORIENTED_EDGE ( 'NONE', *, *, #14507, .T. ) ;
#12999=FACE_OUTER_BOUND ( 'NONE', #8721, .T. ) ;
#13001=CARTESIAN_POINT ( 'NONE',  ( 0.000000000000000000, 9.646732466565339337, 84.51112348751853176 ) ) ;
#13002=DIRECTION ( 'NONE',  ( 1.000000000000000000, 0.000000000000000000, 0.000000000000000000 ) ) ;
#13003=ORIENTED_EDGE ( 'NONE', *, *, #14067, .T. ) ;
#13005=ADVANCED_FACE ( 'NONE', ( #7664 ), #2473, .F. ) ;
#13006=VERTEX_POINT ( 'NONE', #4131 ) ;
#13011=DIRECTION ( 'NONE',  ( -1.000000000000000000, -0.000000000000000000, -0.000000000000000000 ) ) ;
#13012=VECTOR ( 'NONE', #11248, 1000.000000000000000 ) ;
#13015=CIRCLE ( 'NONE', #9484, 92.50100000000000477 ) ;
#13019=DIRECTION ( 'NONE',  ( -1.000000000000000000, 0.000000000000000000, -0.000000000000000000 ) ) ;
#13020=EDGE_CURVE ( 'NONE', #6719, #20752, #17156, .T. ) ;
#13021=CARTESIAN_POINT ( 'NONE',  ( 10.00000000000000000, 81.32027326007924728, -44.08455690948972716 ) ) ;
#13022=DIRECTION ( 'NONE',  ( -1.000000000000000000, -0.000000000000000000, 0.000000000000000000 ) ) ;
#13023=CARTESIAN_POINT ( 'NONE',  ( 0.000000000000000000, -46.07110168784872428, 74.97635353408365688 ) ) ;
#13024=DIRECTION ( 'NONE',  ( 0.000000000000000000, 0.9848077530122085754, -0.1736481776669273613 ) ) ;
#13027=AXIS2_PLACEMENT_3D ( 'NONE', #19857, #13011, #21734 ) ;
#13028=ORIENTED_EDGE ( 'NONE', *, *, #12886, .F. ) ;
#13034=ORIENTED_EDGE ( 'NONE', *, *, #20412, .F. ) ;
#13035=EDGE_LOOP ( 'NONE', ( #11618, #20348, #2501, #14905 ) ) ;
#13036=DIRECTION ( 'NONE',  ( 0.000000000000000000, -0.3420201433256756518, 0.9396926207859059854 ) ) ;
#13038=DIRECTION ( 'NONE',  ( -1.000000000000000000, 0.000000000000000000, -0.000000000000000000 ) ) ;
#13040=LINE ( 'NONE', #2983, #11388 ) ;
#13041=CARTESIAN_POINT ( 'NONE',  ( 10.00000000000000000, -87.58454185039444440, 8.540961822681374827 ) ) ;
#13042=FACE_OUTER_BOUND ( 'NONE', #10465, .T. ) ;
#13044=CARTESIAN_POINT ( 'NONE',  ( 0.000000000000000000, 14.02138820415029663, -83.89630571862271324 ) ) ;
#13045=CARTESIAN_POINT ( 'NONE',  ( 0.000000000000000000, -6.797690662955810481, 87.73705831432212676 ) ) ;
#13046=ORIENTED_EDGE ( 'NONE', *, *, #8818, .T. ) ;
#13047=DIRECTION ( 'NONE',  ( 1.000000000000000000, 0.000000000000000000, 0.000000000000000000 ) ) ;
#13050=CARTESIAN_POINT ( 'NONE',  ( 5.000000000000002665, 23.62010150527222052, 84.77081340225913664 ) ) ;
#13051=DIRECTION ( 'NONE',  ( 1.000000000000000000, 0.000000000000000000, 0.000000000000000000 ) ) ;
#13052=VERTEX_POINT ( 'NONE', #14076 ) ;
#13053=CIRCLE ( 'NONE', #714, 44.99999999999999289 ) ;
#13054=CARTESIAN_POINT ( 'NONE',  ( 0.000000000000000000, 69.25892805976580746, -49.38005998797770246 ) ) ;
#13056=ORIENTED_EDGE ( 'NONE', *, *, #20504, .F. ) ;
#13059=ORIENTED_EDGE ( 'NONE', *, *, #18023, .T. ) ;
#13061=ORIENTED_EDGE ( 'NONE', *, *, #3958, .F. ) ;
#13062=DIRECTION ( 'NONE',  ( 1.000000000000000000, 0.000000000000000000, 0.000000000000000000 ) ) ;
#13064=DIRECTION ( 'NONE',  ( 0.000000000000000000, 0.000000000000000000, 1.000000000000000000 ) ) ;
#13065=CARTESIAN_POINT ( 'NONE',  ( 5.000000000000002665, 0.6609040254611577847, 87.99751818016873983 ) ) ;
#13066=CARTESIAN_POINT ( 'NONE',  ( 10.00000000000000000, -69.74988376404053270, 53.65588238863315240 ) ) ;
#13069=CARTESIAN_POINT ( 'NONE',  ( 10.00000000000000000, 0.000000000000000000, 0.000000000000000000 ) ) ;
#13070=DIRECTION ( 'NONE',  ( 0.000000000000000000, 0.000000000000000000, 1.000000000000000000 ) ) ;
#13071=CARTESIAN_POINT ( 'NONE',  ( 5.000000000000000000, 52.25832601289098278, 70.80301803122803506 ) ) ;
#13072=CIRCLE ( 'NONE', #13791, 92.50099999999999056 ) ;
#13074=EDGE_LOOP ( 'NONE', ( #15335, #953, #8190, #20836 ) ) ;
#13075=CARTESIAN_POINT ( 'NONE',  ( 10.00000000000000000, -56.05743251323904985, 67.83483072893783117 ) ) ;
#13076=DIRECTION ( 'NONE',  ( 0.000000000000000000, 0.6427876096865403621, -0.7660444431189772363 ) ) ;
#13077=DIRECTION ( 'NONE',  ( 0.000000000000000000, 0.4694715627858855322, 0.8829475928589297640 ) ) ;
#13078=ORIENTED_EDGE ( 'NONE', *, *, #9760, .T. ) ;
#13081=VERTEX_POINT ( 'NONE', #20819 ) ;
#13082=EDGE_CURVE ( 'NONE', #239, #1840, #6583, .T. ) ;
#13084=ORIENTED_EDGE ( 'NONE', *, *, #17037, .F. ) ;
#13085=( GEOMETRIC_REPRESENTATION_CONTEXT ( 3 ) GLOBAL_UNCERTAINTY_ASSIGNED_CONTEXT ( ( #8140 ) ) GLOBAL_UNIT_ASSIGNED_CONTEXT ( ( #15750, #3711, #19283 ) ) REPRESENTATION_CONTEXT ( 'NONE', 'WORKASPACE' ) );
#13094=DIRECTION ( 'NONE',  ( -1.000000000000000000, 0.000000000000000000, -0.000000000000000000 ) ) ;
#13096=ORIENTED_EDGE ( 'NONE', *, *, #13345, .F. ) ;
#13097=DIRECTION ( 'NONE',  ( 0.000000000000000000, 0.1391731009600591373, 0.9902680687415712502 ) ) ;
#13098=EDGE_CURVE ( 'NONE', #19754, #3874, #3744, .T. ) ;
#13099=DIRECTION ( 'NONE',  ( 1.000000000000000000, 0.000000000000000000, 0.000000000000000000 ) ) ;
#13102=ADVANCED_FACE ( 'NONE', ( #21682 ), #13284, .F. ) ;
#13103=DIRECTION ( 'NONE',  ( 0.000000000000000000, 0.000000000000000000, 1.000000000000000000 ) ) ;
#13104=ORIENTED_EDGE ( 'NONE', *, *, #5464, .T. ) ;
#13105=DIRECTION ( 'NONE',  ( 1.000000000000000000, 0.000000000000000000, 0.000000000000000000 ) ) ;
#13106=CYLINDRICAL_SURFACE ( 'NONE', #17267, 100.0000000000000000 ) ;
#13108=CARTESIAN_POINT ( 'NONE',  ( 10.00000000000000000, -19.83954325428602061, -82.71385593638713374 ) ) ;
#13109=VERTEX_POINT ( 'NONE', #13066 ) ;
#13110=EDGE_CURVE ( 'NONE', #14138, #3479, #9737, .T. ) ;
#13111=EDGE_LOOP ( 'NONE', ( #16037, #13248, #13501, #6199 ) ) ;
#13112=ADVANCED_FACE ( 'NONE', ( #6240 ), #13400, .F. ) ;
#13115=DIRECTION ( 'NONE',  ( 1.000000000000000000, 0.000000000000000000, 0.000000000000000000 ) ) ;
#13116=EDGE_CURVE ( 'NONE', #923, #14609, #7883, .T. ) ;
#13119=AXIS2_PLACEMENT_3D ( 'NONE', #12435, #309, #20626 ) ;
#13120=DIRECTION ( 'NONE',  ( -1.000000000000000000, -0.000000000000000000, -0.000000000000000000 ) ) ;
#13121=CARTESIAN_POINT ( 'NONE',  ( 0.000000000000000000, -2.481790431838652111, -92.46770094066596357 ) ) ;
#13123=CYLINDRICAL_SURFACE ( 'NONE', #16905, 44.99999999999999289 ) ;
#13124=EDGE_CURVE ( 'NONE', #378, #14927, #20349, .T. ) ;
#13125=FACE_OUTER_BOUND ( 'NONE', #13547, .T. ) ;
#13126=EDGE_CURVE ( 'NONE', #17521, #1324, #5867, .T. ) ;
#13128=EDGE_LOOP ( 'NONE', ( #4856, #9204, #14009, #5920 ) ) ;
#13130=EDGE_CURVE ( 'NONE', #6690, #6258, #4571, .T. ) ;
#13131=ORIENTED_EDGE ( 'NONE', *, *, #19445, .F. ) ;
#13133=ORIENTED_EDGE ( 'NONE', *, *, #11770, .F. ) ;
#13134=ORIENTED_EDGE ( 'NONE', *, *, #5564, .T. ) ;
#13135=CARTESIAN_POINT ( 'NONE',  ( 10.00000000000000000, -60.65279801375299229, -63.75921967137679047 ) ) ;
#13136=CIRCLE ( 'NONE', #3272, 45.00000000000000000 ) ;
#13137=EDGE_CURVE ( 'NONE', #18255, #1046, #18222, .T. ) ;
#13138=ORIENTED_EDGE ( 'NONE', *, *, #12799, .F. ) ;
#13139=DIRECTION ( 'NONE',  ( 0.000000000000000000, 0.000000000000000000, 1.000000000000000000 ) ) ;
#13140=LINE ( 'NONE', #15130, #7509 ) ;
#13142=CARTESIAN_POINT ( 'NONE',  ( 0.000000000000000000, 68.93609746931163329, 54.69748134696484954 ) ) ;
#13145=CARTESIAN_POINT ( 'NONE',  ( 10.00000000000000000, 75.27139873020959726, -53.76477968147737840 ) ) ;
#13146=CARTESIAN_POINT ( 'NONE',  ( 10.00000000000000000, 15.51843147776463638, -83.63233659819634624 ) ) ;
#13147=VECTOR ( 'NONE', #14811, 1000.000000000000000 ) ;
#13148=VERTEX_POINT ( 'NONE', #9627 ) ;
#13149=DIRECTION ( 'NONE',  ( 0.000000000000000000, -7.093091546216279124E-15, 1.000000000000000000 ) ) ;
#13150=VECTOR ( 'NONE', #2418, 1000.000000000000000 ) ;
#13151=AXIS2_PLACEMENT_3D ( 'NONE', #7172, #20547, #20646 ) ;
#13154=EDGE_CURVE ( 'NONE', #6764, #5377, #19629, .T. ) ;
#13155=EDGE_LOOP ( 'NONE', ( #14597, #2495, #13410, #7299 ) ) ;
#13157=EDGE_LOOP ( 'NONE', ( #14068, #5331, #7991, #14095 ) ) ;
#13158=CARTESIAN_POINT ( 'NONE',  ( 0.000000000000000000, 0.000000000000000000, 0.000000000000000000 ) ) ;
#13159=VERTEX_POINT ( 'NONE', #9860 ) ;
#13160=ORIENTED_EDGE ( 'NONE', *, *, #41, .T. ) ;
#13161=FACE_OUTER_BOUND ( 'NONE', #13035, .T. ) ;
#13162=AXIS2_PLACEMENT_3D ( 'NONE', #1425, #11351, #21629 ) ;
#13163=ORIENTED_EDGE ( 'NONE', *, *, #21593, .F. ) ;
#13164=CARTESIAN_POINT ( 'NONE',  ( 5.000000000000002665, 5.479102470011647519, -87.82926298292107958 ) ) ;
#13165=CARTESIAN_POINT ( 'NONE',  ( 10.00000000000000000, 77.39385041987151226, -35.28996114464630551 ) ) ;
#13166=CARTESIAN_POINT ( 'NONE',  ( 10.00000000000000000, 90.32141448704707898, -19.96189084378132961 ) ) ;
#13169=DIRECTION ( 'NONE',  ( 0.000000000000000000, -0.9993908270190954291, -0.03489949670251119018 ) ) ;
#13171=CARTESIAN_POINT ( 'NONE',  ( 0.000000000000000000, 0.000000000000000000, 0.000000000000000000 ) ) ;
#13173=AXIS2_PLACEMENT_3D ( 'NONE', #2903, #6353, #3124 ) ;
#13174=VERTEX_POINT ( 'NONE', #4898 ) ;
#13175=AXIS2_PLACEMENT_3D ( 'NONE', #15546, #3513, #408 ) ;
#13178=DIRECTION ( 'NONE',  ( -1.000000000000000000, -0.000000000000000000, 0.000000000000000000 ) ) ;
#13179=ORIENTED_EDGE ( 'NONE', *, *, #1270, .F. ) ;
#13181=VERTEX_POINT ( 'NONE', #9961 ) ;
#13182=CIRCLE ( 'NONE', #2608, 44.99999999999999289 ) ;
#13184=ORIENTED_EDGE ( 'NONE', *, *, #11633, .T. ) ;
#13185=FACE_OUTER_BOUND ( 'NONE', #19723, .T. ) ;
#13186=VERTEX_POINT ( 'NONE', #11409 ) ;
#13189=CARTESIAN_POINT ( 'NONE',  ( 5.000000000000002665, 87.58454185039451545, -8.540961822680756654 ) ) ;
#13191=VECTOR ( 'NONE', #9990, 1000.000000000000000 ) ;
#13192=CARTESIAN_POINT ( 'NONE',  ( 10.00000000000000000, 90.32141448704683739, 19.96189084378252332 ) ) ;
#13194=FACE_OUTER_BOUND ( 'NONE', #14301, .T. ) ;
#13195=CARTESIAN_POINT ( 'NONE',  ( 0.000000000000000000, 81.97107881582195432, 22.71412948308594437 ) ) ;
#13200=VERTEX_POINT ( 'NONE', #3018 ) ;
#13201=VECTOR ( 'NONE', #596, 1000.000000000000000 ) ;
#13202=CYLINDRICAL_SURFACE ( 'NONE', #10226, 44.99999999999999289 ) ;
#13203=DIRECTION ( 'NONE',  ( -1.000000000000000000, -0.000000000000000000, -0.000000000000000000 ) ) ;
#13204=EDGE_CURVE ( 'NONE', #2153, #20998, #16497, .T. ) ;
#13206=DIRECTION ( 'NONE',  ( 0.000000000000000000, 0.000000000000000000, 1.000000000000000000 ) ) ;
#13208=AXIS2_PLACEMENT_3D ( 'NONE', #20656, #2103, #7179 ) ;
#13209=DIRECTION ( 'NONE',  ( 0.000000000000000000, -0.9702957262759988044, 0.2419218955996583209 ) ) ;
#13210=AXIS2_PLACEMENT_3D ( 'NONE', #7316, #11591, #11360 ) ;
#13213=EDGE_CURVE ( 'NONE', #16808, #19662, #13263, .T. ) ;
#13215=AXIS2_PLACEMENT_3D ( 'NONE', #17179, #15397, #10101 ) ;
#13216=ORIENTED_EDGE ( 'NONE', *, *, #13525, .F. ) ;
#13217=ORIENTED_EDGE ( 'NONE', *, *, #11228, .F. ) ;
#13218=CARTESIAN_POINT ( 'NONE',  ( 10.00000000000000000, 0.000000000000000000, 0.000000000000000000 ) ) ;
#13221=EDGE_CURVE ( 'NONE', #5691, #12772, #11735, .T. ) ;
#13222=DIRECTION ( 'NONE',  ( -1.000000000000000000, 0.000000000000000000, 0.000000000000000000 ) ) ;
#13223=DIRECTION ( 'NONE',  ( 0.000000000000000000, -0.9702957262759988044, 0.2419218955996583209 ) ) ;
#13225=DIRECTION ( 'NONE',  ( -1.000000000000000000, 0.000000000000000000, 0.000000000000000000 ) ) ;
#13226=DIRECTION ( 'NONE',  ( 1.000000000000000000, 0.000000000000000000, 0.000000000000000000 ) ) ;
#13228=CARTESIAN_POINT ( 'NONE',  ( 0.000000000000000000, 0.000000000000000000, 0.000000000000000000 ) ) ;
#13231=CIRCLE ( 'NONE', #10768, 88.00000000000000000 ) ;
#13232=DIRECTION ( 'NONE',  ( -1.000000000000000000, -0.000000000000000000, 0.000000000000000000 ) ) ;
#13233=AXIS2_PLACEMENT_3D ( 'NONE', #21470, #21250, #6352 ) ;
#13234=EDGE_CURVE ( 'NONE', #17607, #4602, #12061, .T. ) ;
#13235=CYLINDRICAL_SURFACE ( 'NONE', #184, 44.99999999999999289 ) ;
#13237=EDGE_CURVE ( 'NONE', #7101, #19710, #9032, .T. ) ;
#13241=EDGE_CURVE ( 'NONE', #12017, #17526, #8856, .T. ) ;
#13243=EDGE_LOOP ( 'NONE', ( #16543, #12614, #4509, #20968 ) ) ;
#13245=VECTOR ( 'NONE', #11085, 1000.000000000000000 ) ;
#13246=VECTOR ( 'NONE', #4653, 1000.000000000000000 ) ;
#13247=AXIS2_PLACEMENT_3D ( 'NONE', #6481, #20063, #4814 ) ;
#13248=ORIENTED_EDGE ( 'NONE', *, *, #13687, .T. ) ;
#13250=CARTESIAN_POINT ( 'NONE',  ( 10.00000000000000000, 21.65267340503369198, -89.93106657554412209 ) ) ;
#13251=ORIENTED_EDGE ( 'NONE', *, *, #4369, .T. ) ;
#13252=CARTESIAN_POINT ( 'NONE',  ( 10.00000000000000000, 15.51843147776463638, -83.63233659819634624 ) ) ;
#13256=DIRECTION ( 'NONE',  ( 0.000000000000000000, 0.000000000000000000, 1.000000000000000000 ) ) ;
#13257=DIRECTION ( 'NONE',  ( 0.000000000000000000, 0.000000000000000000, -1.000000000000000000 ) ) ;
#13260=CIRCLE ( 'NONE', #12914, 45.00000000000000711 ) ;
#13261=EDGE_LOOP ( 'NONE', ( #18668, #18326, #11399, #12892 ) ) ;
#13262=AXIS2_PLACEMENT_3D ( 'NONE', #19235, #4209, #14251 ) ;
#13263=CIRCLE ( 'NONE', #576, 92.50100000000001899 ) ;
#13264=CARTESIAN_POINT ( 'NONE',  ( 10.00000000000000000, -81.83745710415254848, -32.35167097270233683 ) ) ;
#13265=VECTOR ( 'NONE', #5844, 1000.000000000000000 ) ;
#13266=ADVANCED_FACE ( 'NONE', ( #16942 ), #1899, .F. ) ;
#13270=ORIENTED_EDGE ( 'NONE', *, *, #7167, .T. ) ;
#13271=DIRECTION ( 'NONE',  ( -1.000000000000000000, -0.000000000000000000, -0.000000000000000000 ) ) ;
#13272=ORIENTED_EDGE ( 'NONE', *, *, #6903, .F. ) ;
#13276=VERTEX_POINT ( 'NONE', #464 ) ;
#13277=AXIS2_PLACEMENT_3D ( 'NONE', #11261, #20989, #4528 ) ;
#13278=DIRECTION ( 'NONE',  ( 0.000000000000000000, 0.9848077530122073542, 0.1736481776669339949 ) ) ;
#13279=EDGE_CURVE ( 'NONE', #14957, #16786, #18598, .T. ) ;
#13281=DIRECTION ( 'NONE',  ( -1.000000000000000000, 0.000000000000000000, -0.000000000000000000 ) ) ;
#13282=LINE ( 'NONE', #13398, #6200 ) ;
#13284=CYLINDRICAL_SURFACE ( 'NONE', #16805, 44.99999999999998579 ) ;
#13285=EDGE_CURVE ( 'NONE', #18956, #13661, #7206, .T. ) ;
#13289=FACE_OUTER_BOUND ( 'NONE', #5023, .T. ) ;
#13290=ORIENTED_EDGE ( 'NONE', *, *, #6863, .F. ) ;
#13292=AXIS2_PLACEMENT_3D ( 'NONE', #5144, #271, #2037 ) ;
#13294=VECTOR ( 'NONE', #2522, 1000.000000000000000 ) ;
#13297=VERTEX_POINT ( 'NONE', #3455 ) ;
#13299=ORIENTED_EDGE ( 'NONE', *, *, #16048, .F. ) ;
#13305=DIRECTION ( 'NONE',  ( -1.000000000000000000, 0.000000000000000000, 0.000000000000000000 ) ) ;
#13307=AXIS2_PLACEMENT_3D ( 'NONE', #3433, #1776, #14462 ) ;
#13308=FACE_OUTER_BOUND ( 'NONE', #20415, .T. ) ;
#13311=DIRECTION ( 'NONE',  ( -1.000000000000000000, -0.000000000000000000, -0.000000000000000000 ) ) ;
#13314=LINE ( 'NONE', #18193, #12457 ) ;
#13315=DIRECTION ( 'NONE',  ( 1.000000000000000000, 0.000000000000000000, 0.000000000000000000 ) ) ;
#13318=CARTESIAN_POINT ( 'NONE',  ( 10.00000000000000000, 0.000000000000000000, 0.000000000000000000 ) ) ;
#13321=VERTEX_POINT ( 'NONE', #249 ) ;
#13322=VECTOR ( 'NONE', #5651, 1000.000000000000000 ) ;
#13326=CARTESIAN_POINT ( 'NONE',  ( 10.00000000000000000, 0.000000000000000000, 0.000000000000000000 ) ) ;
#13327=VECTOR ( 'NONE', #18925, 1000.000000000000000 ) ;
#13328=VERTEX_POINT ( 'NONE', #18714 ) ;
#13330=VERTEX_POINT ( 'NONE', #7105 ) ;
#13331=VERTEX_POINT ( 'NONE', #6994 ) ;
#13332=DIRECTION ( 'NONE',  ( 1.000000000000000000, 0.000000000000000000, 0.000000000000000000 ) ) ;
#13337=CARTESIAN_POINT ( 'NONE',  ( 10.00000000000000000, -3.974475837764312569, -92.41557521768193340 ) ) ;
#13338=EDGE_CURVE ( 'NONE', #5362, #8003, #16455, .T. ) ;
#13340=VECTOR ( 'NONE', #7547, 1000.000000000000000 ) ;
#13343=CIRCLE ( 'NONE', #11949, 44.99999999999999289 ) ;
#13344=CIRCLE ( 'NONE', #21818, 44.99999999999999289 ) ;
#13345=EDGE_CURVE ( 'NONE', #610, #13331, #244, .T. ) ;
#13346=DIRECTION ( 'NONE',  ( 1.000000000000000000, 0.000000000000000000, -0.000000000000000000 ) ) ;
#13348=CARTESIAN_POINT ( 'NONE',  ( 0.000000000000000000, 0.000000000000000000, 0.000000000000000000 ) ) ;
#13349=ORIENTED_EDGE ( 'NONE', *, *, #5031, .F. ) ;
#13350=DIRECTION ( 'NONE',  ( -1.000000000000000000, 0.000000000000000000, 0.000000000000000000 ) ) ;
#13351=ORIENTED_EDGE ( 'NONE', *, *, #14980, .F. ) ;
#13354=VERTEX_POINT ( 'NONE', #6886 ) ;
#13355=AXIS2_PLACEMENT_3D ( 'NONE', #15118, #16899, #21338 ) ;
#13356=CIRCLE ( 'NONE', #6684, 44.99999999999998579 ) ;
#13357=AXIS2_PLACEMENT_3D ( 'NONE', #21099, #14352, #21206 ) ;
#13359=CARTESIAN_POINT ( 'NONE',  ( 0.000000000000000000, 0.000000000000000000, 0.000000000000000000 ) ) ;
#13361=DIRECTION ( 'NONE',  ( 0.000000000000000000, 0.7880107536067231244, -0.6156614753256566264 ) ) ;
#13362=ADVANCED_FACE ( 'NONE', ( #5225 ), #18808, .F. ) ;
#13363=EDGE_CURVE ( 'NONE', #3486, #14906, #17154, .T. ) ;
#13364=ADVANCED_FACE ( 'NONE', ( #5547 ), #9272, .F. ) ;
#13365=DIRECTION ( 'NONE',  ( -1.000000000000000000, -0.000000000000000000, -0.000000000000000000 ) ) ;
#13366=EDGE_CURVE ( 'NONE', #6258, #4702, #20362, .T. ) ;
#13367=CARTESIAN_POINT ( 'NONE',  ( -10.00000000000000000, 0.000000000000000000, 0.000000000000000000 ) ) ;
#13368=DIRECTION ( 'NONE',  ( -1.000000000000000000, -0.000000000000000000, -0.000000000000000000 ) ) ;
#13369=CARTESIAN_POINT ( 'NONE',  ( 10.00000000000000000, -35.18804927320473297, -80.65854690202716881 ) ) ;
#13370=DIRECTION ( 'NONE',  ( -1.000000000000000000, 0.000000000000000000, -0.000000000000000000 ) ) ;
#13371=VECTOR ( 'NONE', #3397, 1000.000000000000000 ) ;
#13372=CIRCLE ( 'NONE', #15488, 88.00000000000000000 ) ;
#13376=CIRCLE ( 'NONE', #18350, 92.50099999999999056 ) ;
#13377=DIRECTION ( 'NONE',  ( -1.000000000000000000, 0.000000000000000000, 0.000000000000000000 ) ) ;
#13378=ADVANCED_FACE ( 'NONE', ( #2541 ), #2448, .F. ) ;
#13379=EDGE_LOOP ( 'NONE', ( #13717, #19170, #16268, #189 ) ) ;
#13383=VERTEX_POINT ( 'NONE', #7638 ) ;
#13384=DIRECTION ( 'NONE',  ( -1.000000000000000000, -0.000000000000000000, -0.000000000000000000 ) ) ;
#13385=VERTEX_POINT ( 'NONE', #21007 ) ;
#13389=CARTESIAN_POINT ( 'NONE',  ( -10.00000000000000000, 0.000000000000000000, 0.000000000000000000 ) ) ;
#13390=ORIENTED_EDGE ( 'NONE', *, *, #145, .T. ) ;
#13391=AXIS2_PLACEMENT_3D ( 'NONE', #5593, #294, #10557 ) ;
#13393=DIRECTION ( 'NONE',  ( -1.000000000000000000, 0.000000000000000000, -0.000000000000000000 ) ) ;
#13394=AXIS2_PLACEMENT_3D ( 'NONE', #3597, #19964, #4828 ) ;
#13395=AXIS2_PLACEMENT_3D ( 'NONE', #8379, #2081, #13789 ) ;
#13398=CARTESIAN_POINT ( 'NONE',  ( 5.000000000000002665, -40.72878876293203376, 78.00747250042435610 ) ) ;
#13399=DIRECTION ( 'NONE',  ( -1.000000000000000000, 0.000000000000000000, 0.000000000000000000 ) ) ;
#13400=CYLINDRICAL_SURFACE ( 'NONE', #10090, 44.99999999999999289 ) ;
#13401=DIRECTION ( 'NONE',  ( 0.000000000000000000, -8.943463253924872306E-15, -1.000000000000000000 ) ) ;
#13403=DIRECTION ( 'NONE',  ( -1.000000000000000000, -0.000000000000000000, -0.000000000000000000 ) ) ;
#13404=ORIENTED_EDGE ( 'NONE', *, *, #11060, .T. ) ;
#13407=EDGE_CURVE ( 'NONE', #19953, #589, #5881, .T. ) ;
#13410=ORIENTED_EDGE ( 'NONE', *, *, #831, .F. ) ;
#13413=ORIENTED_EDGE ( 'NONE', *, *, #16458, .T. ) ;
#13414=EDGE_CURVE ( 'NONE', #15191, #21786, #10620, .T. ) ;
#13415=VERTEX_POINT ( 'NONE', #12384 ) ;
#13418=ORIENTED_EDGE ( 'NONE', *, *, #10802, .F. ) ;
#13419=CARTESIAN_POINT ( 'NONE',  ( 0.000000000000000000, 62.44821182181184582, -68.23969402963440700 ) ) ;
#13420=DIRECTION ( 'NONE',  ( 1.000000000000000000, 0.000000000000000000, 0.000000000000000000 ) ) ;
#13422=EDGE_CURVE ( 'NONE', #10755, #20618, #2696, .T. ) ;
#13424=CARTESIAN_POINT ( 'NONE',  ( 0.000000000000000000, 0.000000000000000000, 0.000000000000000000 ) ) ;
#13426=DIRECTION ( 'NONE',  ( -1.000000000000000000, -0.000000000000000000, 0.000000000000000000 ) ) ;
#13427=FACE_OUTER_BOUND ( 'NONE', #19146, .T. ) ;
#13429=EDGE_LOOP ( 'NONE', ( #8093, #21385, #8803, #8415 ) ) ;
#13432=ORIENTED_EDGE ( 'NONE', *, *, #20532, .T. ) ;
#13433=DIRECTION ( 'NONE',  ( -1.000000000000000000, 0.000000000000000000, -0.000000000000000000 ) ) ;
#13435=DIRECTION ( 'NONE',  ( 1.000000000000000000, 0.000000000000000000, 0.000000000000000000 ) ) ;
#13436=VECTOR ( 'NONE', #2115, 1000.000000000000000 ) ;
#13437=DIRECTION ( 'NONE',  ( 0.000000000000000000, -0.06975647374413236623, 0.9975640502598237536 ) ) ;
#13442=ORIENTED_EDGE ( 'NONE', *, *, #6819, .F. ) ;
#13444=ORIENTED_EDGE ( 'NONE', *, *, #4405, .T. ) ;
#13445=CARTESIAN_POINT ( 'NONE',  ( -10.00000000000000000, 0.000000000000000000, 0.000000000000000000 ) ) ;
#13446=DIRECTION ( 'NONE',  ( 0.000000000000000000, -7.093091546216279124E-15, 1.000000000000000000 ) ) ;
#13447=DIRECTION ( 'NONE',  ( 1.000000000000000000, 0.000000000000000000, 0.000000000000000000 ) ) ;
#13449=CYLINDRICAL_SURFACE ( 'NONE', #13162, 92.50100000000000477 ) ;
#13452=DIRECTION ( 'NONE',  ( 0.000000000000000000, 0.3420201433256694901, -0.9396926207859080948 ) ) ;
#13453=DIRECTION ( 'NONE',  ( -1.000000000000000000, -0.000000000000000000, -0.000000000000000000 ) ) ;
#13454=CYLINDRICAL_SURFACE ( 'NONE', #11536, 92.50100000000000477 ) ;
#13455=ORIENTED_EDGE ( 'NONE', *, *, #17872, .F. ) ;
#13456=CYLINDRICAL_SURFACE ( 'NONE', #10879, 44.99999999999999289 ) ;
#13457=EDGE_CURVE ( 'NONE', #3544, #4447, #777, .T. ) ;
#13458=ORIENTED_EDGE ( 'NONE', *, *, #12312, .T. ) ;
#13459=CYLINDRICAL_SURFACE ( 'NONE', #13355, 44.99999999999999289 ) ;
#13461=ORIENTED_EDGE ( 'NONE', *, *, #20788, .T. ) ;
#13462=EDGE_CURVE ( 'NONE', #9164, #15549, #19296, .T. ) ;
#13464=CARTESIAN_POINT ( 'NONE',  ( 10.00000000000000000, 57.47876254627143311, 62.70072803846409215 ) ) ;
#13465=VERTEX_POINT ( 'NONE', #4215 ) ;
#13466=CARTESIAN_POINT ( 'NONE',  ( 0.000000000000000000, -27.87320266523617107, 88.20158487341750231 ) ) ;
#13468=VECTOR ( 'NONE', #11464, 1000.000000000000000 ) ;
#13469=DIRECTION ( 'NONE',  ( -1.000000000000000000, -0.000000000000000000, -0.000000000000000000 ) ) ;
#13470=FACE_OUTER_BOUND ( 'NONE', #2787, .T. ) ;
#13471=DIRECTION ( 'NONE',  ( -1.000000000000000000, 0.000000000000000000, 0.000000000000000000 ) ) ;
#13472=DIRECTION ( 'NONE',  ( 0.000000000000000000, 0.000000000000000000, 1.000000000000000000 ) ) ;
#13473=CARTESIAN_POINT ( 'NONE',  ( 10.00000000000000000, -92.32475887865429343, 5.707354816230212791 ) ) ;
#13475=DIRECTION ( 'NONE',  ( 0.000000000000000000, 0.000000000000000000, 1.000000000000000000 ) ) ;
#13476=AXIS2_PLACEMENT_3D ( 'NONE', #17262, #20569, #3773 ) ;
#13477=EDGE_CURVE ( 'NONE', #13893, #18255, #927, .T. ) ;
#13478=VERTEX_POINT ( 'NONE', #7426 ) ;
#13479=ORIENTED_EDGE ( 'NONE', *, *, #6354, .F. ) ;
#13480=DIRECTION ( 'NONE',  ( -1.000000000000000000, 0.000000000000000000, 0.000000000000000000 ) ) ;
#13482=EDGE_LOOP ( 'NONE', ( #21775, #17256, #6145, #13598 ) ) ;
#13487=CARTESIAN_POINT ( 'NONE',  ( 10.00000000000000000, -39.87723064937176076, 83.46401306393555330 ) ) ;
#13489=CARTESIAN_POINT ( 'NONE',  ( 0.000000000000000000, -5.479102470009884485, -87.82926298292120748 ) ) ;
#13492=DIRECTION ( 'NONE',  ( 0.000000000000000000, -0.9510565162951503115, -0.3090169943749573322 ) ) ;
#13494=CARTESIAN_POINT ( 'NONE',  ( 0.000000000000000000, 0.000000000000000000, 0.000000000000000000 ) ) ;
#13498=DIRECTION ( 'NONE',  ( 1.000000000000000000, 0.000000000000000000, 0.000000000000000000 ) ) ;
#13500=AXIS2_PLACEMENT_3D ( 'NONE', #12361, #5310, #17450 ) ;
#13501=ORIENTED_EDGE ( 'NONE', *, *, #11752, .F. ) ;
#13502=CIRCLE ( 'NONE', #4693, 92.50100000000000477 ) ;
#13503=EDGE_CURVE ( 'NONE', #17231, #12265, #18030, .T. ) ;
#13504=VECTOR ( 'NONE', #21223, 1000.000000000000000 ) ;
#13505=ADVANCED_FACE ( 'NONE', ( #13042 ), #7849, .F. ) ;
#13506=ADVANCED_FACE ( 'NONE', ( #9500 ), #2985, .F. ) ;
#13507=DIRECTION ( 'NONE',  ( 0.000000000000000000, -0.9993908270190959842, 0.03489949670249112984 ) ) ;
#13509=DIRECTION ( 'NONE',  ( 1.000000000000000000, 0.000000000000000000, 0.000000000000000000 ) ) ;
#13510=VECTOR ( 'NONE', #18544, 1000.000000000000000 ) ;
#13512=DIRECTION ( 'NONE',  ( -1.000000000000000000, -0.000000000000000000, -0.000000000000000000 ) ) ;
#13517=DIRECTION ( 'NONE',  ( 0.000000000000000000, 0.000000000000000000, 1.000000000000000000 ) ) ;
#13518=EDGE_CURVE ( 'NONE', #17357, #4335, #13647, .T. ) ;
#13519=ORIENTED_EDGE ( 'NONE', *, *, #3004, .F. ) ;
#13520=ORIENTED_EDGE ( 'NONE', *, *, #6197, .T. ) ;
#13522=FACE_OUTER_BOUND ( 'NONE', #4636, .T. ) ;
#13525=EDGE_CURVE ( 'NONE', #11814, #12538, #18234, .T. ) ;
#13526=CIRCLE ( 'NONE', #7693, 88.00000000000000000 ) ;
#13528=DIRECTION ( 'NONE',  ( 0.000000000000000000, 0.000000000000000000, 1.000000000000000000 ) ) ;
#13530=CYLINDRICAL_SURFACE ( 'NONE', #17086, 44.99999999999999289 ) ;
#13531=DIRECTION ( 'NONE',  ( 1.000000000000000000, 0.000000000000000000, -0.000000000000000000 ) ) ;
#13534=CIRCLE ( 'NONE', #14601, 44.99999999999999289 ) ;
#13535=ORIENTED_EDGE ( 'NONE', *, *, #4203, .F. ) ;
#13540=VERTEX_POINT ( 'NONE', #19787 ) ;
#13541=CIRCLE ( 'NONE', #9630, 92.50100000000000477 ) ;
#13542=DIRECTION ( 'NONE',  ( 0.000000000000000000, 0.000000000000000000, 1.000000000000000000 ) ) ;
#13543=VERTEX_POINT ( 'NONE', #9713 ) ;
#13544=EDGE_CURVE ( 'NONE', #18504, #13297, #14340, .T. ) ;
#13546=CYLINDRICAL_SURFACE ( 'NONE', #6696, 44.99999999999999289 ) ;
#13547=EDGE_LOOP ( 'NONE', ( #4423, #3972, #12074, #1102 ) ) ;
#13548=LINE ( 'NONE', #18532, #21214 ) ;
#13550=ORIENTED_EDGE ( 'NONE', *, *, #9178, .T. ) ;
#13551=ORIENTED_EDGE ( 'NONE', *, *, #9884, .T. ) ;
#13552=ORIENTED_EDGE ( 'NONE', *, *, #3376, .F. ) ;
#13554=ORIENTED_EDGE ( 'NONE', *, *, #19605, .T. ) ;
#13556=VECTOR ( 'NONE', #20620, 1000.000000000000000 ) ;
#13557=CARTESIAN_POINT ( 'NONE',  ( 0.000000000000000000, -87.17509410653603652, -30.93441398372672069 ) ) ;
#13558=LINE ( 'NONE', #21736, #13468 ) ;
#13559=DIRECTION ( 'NONE',  ( 0.000000000000000000, -0.8290375725550467312, 0.5591929034707392443 ) ) ;
#13562=CARTESIAN_POINT ( 'NONE',  ( 0.000000000000000000, 83.03980459022480431, -18.42770452393272862 ) ) ;
#13565=DIRECTION ( 'NONE',  ( 0.000000000000000000, 0.000000000000000000, 1.000000000000000000 ) ) ;
#13568=FACE_OUTER_BOUND ( 'NONE', #14322, .T. ) ;
#13570=ORIENTED_EDGE ( 'NONE', *, *, #10695, .T. ) ;
#13572=ORIENTED_EDGE ( 'NONE', *, *, #21793, .F. ) ;
#13574=AXIS2_PLACEMENT_3D ( 'NONE', #11758, #1920, #8661 ) ;
#13576=ORIENTED_EDGE ( 'NONE', *, *, #6548, .F. ) ;
#13577=VERTEX_POINT ( 'NONE', #16352 ) ;
#13578=DIRECTION ( 'NONE',  ( 0.000000000000000000, 0.000000000000000000, 1.000000000000000000 ) ) ;
#13579=ORIENTED_EDGE ( 'NONE', *, *, #7, .T. ) ;
#13580=CARTESIAN_POINT ( 'NONE',  ( 10.00000000000000000, -84.12297548659712731, 32.40974838672912028 ) ) ;
#13582=DIRECTION ( 'NONE',  ( 1.000000000000000000, 0.000000000000000000, -0.000000000000000000 ) ) ;
#13583=VECTOR ( 'NONE', #2851, 1000.000000000000000 ) ;
#13584=AXIS2_PLACEMENT_3D ( 'NONE', #12276, #17366, #19126 ) ;
#13585=CARTESIAN_POINT ( 'NONE',  ( 5.000000000000000000, -36.39558101400191958, 80.12091913260368869 ) ) ;
#13586=DIRECTION ( 'NONE',  ( 0.000000000000000000, 0.000000000000000000, 1.000000000000000000 ) ) ;
#13587=CYLINDRICAL_SURFACE ( 'NONE', #2630, 44.99999999999999289 ) ;
#13588=AXIS2_PLACEMENT_3D ( 'NONE', #19316, #21087, #9468 ) ;
#13589=DIRECTION ( 'NONE',  ( -1.000000000000000000, -0.000000000000000000, -0.000000000000000000 ) ) ;
#13590=FACE_OUTER_BOUND ( 'NONE', #718, .T. ) ;
#13592=DIRECTION ( 'NONE',  ( 1.000000000000000000, 0.000000000000000000, 0.000000000000000000 ) ) ;
#13593=CIRCLE ( 'NONE', #10056, 92.50100000000000477 ) ;
#13595=VERTEX_POINT ( 'NONE', #8078 ) ;
#13598=ORIENTED_EDGE ( 'NONE', *, *, #10712, .T. ) ;
#13600=CARTESIAN_POINT ( 'NONE',  ( 0.000000000000000000, 56.05743251323859511, 67.83483072893820065 ) ) ;
#13601=VERTEX_POINT ( 'NONE', #3638 ) ;
#13602=DIRECTION ( 'NONE',  ( 0.000000000000000000, 0.7880107536067231244, -0.6156614753256568484 ) ) ;
#13603=VERTEX_POINT ( 'NONE', #6975 ) ;
#13604=ORIENTED_EDGE ( 'NONE', *, *, #11063, .F. ) ;
#13606=ORIENTED_EDGE ( 'NONE', *, *, #13682, .T. ) ;
#13608=LINE ( 'NONE', #20364, #17836 ) ;
#13609=FACE_OUTER_BOUND ( 'NONE', #8256, .T. ) ;
#13612=CARTESIAN_POINT ( 'NONE',  ( 10.00000000000000000, -64.66851233300764079, 55.25552418572942059 ) ) ;
#13613=AXIS2_PLACEMENT_3D ( 'NONE', #19485, #4351, #11089 ) ;
#13616=CARTESIAN_POINT ( 'NONE',  ( 10.00000000000000000, -90.63195040374174027, -18.50093422002511900 ) ) ;
#13617=LINE ( 'NONE', #20479, #21802 ) ;
#13619=ORIENTED_EDGE ( 'NONE', *, *, #2414, .F. ) ;
#13621=CARTESIAN_POINT ( 'NONE',  ( 10.00000000000000000, 21.65267340503250537, 89.93106657554442052 ) ) ;
#13623=CARTESIAN_POINT ( 'NONE',  ( 10.00000000000000000, 0.000000000000000000, 0.000000000000000000 ) ) ;
#13626=CARTESIAN_POINT ( 'NONE',  ( 0.000000000000000000, 0.000000000000000000, 0.000000000000000000 ) ) ;
#13627=VERTEX_POINT ( 'NONE', #15027 ) ;
#13630=CARTESIAN_POINT ( 'NONE',  ( 10.00000000000000000, 83.35585896458619004, 16.94078559807978124 ) ) ;
#13631=ORIENTED_EDGE ( 'NONE', *, *, #14344, .F. ) ;
#13632=EDGE_LOOP ( 'NONE', ( #7039, #16214, #16841, #20042 ) ) ;
#13635=LINE ( 'NONE', #10217, #18534 ) ;
#13637=EDGE_CURVE ( 'NONE', #2166, #610, #18785, .T. ) ;
#13639=CARTESIAN_POINT ( 'NONE',  ( 10.00000000000000000, -10.41137886060045226, -91.91321010181856366 ) ) ;
#13640=EDGE_CURVE ( 'NONE', #1439, #21814, #5205, .T. ) ;
#13642=LINE ( 'NONE', #5360, #5062 ) ;
#13643=CYLINDRICAL_SURFACE ( 'NONE', #15124, 45.00000000000000000 ) ;
#13646=ORIENTED_EDGE ( 'NONE', *, *, #6640, .T. ) ;
#13647=CIRCLE ( 'NONE', #13994, 44.99999999999999289 ) ;
#13648=CYLINDRICAL_SURFACE ( 'NONE', #11991, 44.99999999999999289 ) ;
#13649=LINE ( 'NONE', #19134, #18902 ) ;
#13650=VERTEX_POINT ( 'NONE', #12042 ) ;
#13651=CARTESIAN_POINT ( 'NONE',  ( 10.00000000000000000, 0.000000000000000000, 0.000000000000000000 ) ) ;
#13652=ADVANCED_FACE ( 'NONE', ( #13470 ), #6651, .F. ) ;
#13653=ORIENTED_EDGE ( 'NONE', *, *, #11948, .T. ) ;
#13654=DIRECTION ( 'NONE',  ( 0.000000000000000000, 0.000000000000000000, 1.000000000000000000 ) ) ;
#13656=EDGE_LOOP ( 'NONE', ( #519, #3554, #11782, #3396 ) ) ;
#13657=LINE ( 'NONE', #18429, #14495 ) ;
#13658=EDGE_CURVE ( 'NONE', #20618, #9731, #18576, .T. ) ;
#13659=AXIS2_PLACEMENT_3D ( 'NONE', #3317, #16471, #11501 ) ;
#13660=EDGE_LOOP ( 'NONE', ( #11659, #11157, #19577, #15661 ) ) ;
#13661=VERTEX_POINT ( 'NONE', #10271 ) ;
#13662=AXIS2_PLACEMENT_3D ( 'NONE', #19411, #16094, #958 ) ;
#13663=ORIENTED_EDGE ( 'NONE', *, *, #4878, .T. ) ;
#13664=DIRECTION ( 'NONE',  ( 1.000000000000000000, 0.000000000000000000, 0.000000000000000000 ) ) ;
#13668=DIRECTION ( 'NONE',  ( 0.000000000000000000, 0.8660254037844362651, 0.5000000000000041078 ) ) ;
#13670=CARTESIAN_POINT ( 'NONE',  ( -10.00000000000000000, 0.000000000000000000, 0.000000000000000000 ) ) ;
#13674=DIRECTION ( 'NONE',  ( 1.000000000000000000, 0.000000000000000000, 0.000000000000000000 ) ) ;
#13676=CARTESIAN_POINT ( 'NONE',  ( 10.00000000000000000, 0.000000000000000000, 0.000000000000000000 ) ) ;
#13679=CIRCLE ( 'NONE', #9785, 44.99999999999999289 ) ;
#13680=CIRCLE ( 'NONE', #6287, 88.00000000000000000 ) ;
#13682=EDGE_CURVE ( 'NONE', #10824, #18424, #5087, .T. ) ;
#13683=VERTEX_POINT ( 'NONE', #21767 ) ;
#13687=EDGE_CURVE ( 'NONE', #18956, #6087, #7317, .T. ) ;
#13694=AXIS2_PLACEMENT_3D ( 'NONE', #11518, #20359, #18378 ) ;
#13695=CIRCLE ( 'NONE', #17234, 92.50099999999999056 ) ;
#13697=CARTESIAN_POINT ( 'NONE',  ( 0.000000000000000000, 0.000000000000000000, 0.000000000000000000 ) ) ;
#13698=AXIS2_PLACEMENT_3D ( 'NONE', #21486, #7111, #20582 ) ;
#13699=CIRCLE ( 'NONE', #2040, 44.99999999999999289 ) ;
#13700=VECTOR ( 'NONE', #3232, 1000.000000000000000 ) ;
#13701=CARTESIAN_POINT ( 'NONE',  ( 10.00000000000000000, 0.000000000000000000, 0.000000000000000000 ) ) ;
#13702=DIRECTION ( 'NONE',  ( -1.000000000000000000, 0.000000000000000000, -0.000000000000000000 ) ) ;
#13705=CARTESIAN_POINT ( 'NONE',  ( 10.00000000000000000, 16.79755869217770936, -90.96305306542237190 ) ) ;
#13706=CYLINDRICAL_SURFACE ( 'NONE', #20444, 44.99999999999998579 ) ;
#13708=DIRECTION ( 'NONE',  ( 0.000000000000000000, 0.000000000000000000, 1.000000000000000000 ) ) ;
#13709=AXIS2_PLACEMENT_3D ( 'NONE', #6641, #9823, #16792 ) ;
#13713=CIRCLE ( 'NONE', #19002, 92.50100000000000477 ) ;
#13714=AXIS2_PLACEMENT_3D ( 'NONE', #443, #2105, #16801 ) ;
#13715=VERTEX_POINT ( 'NONE', #17348 ) ;
#13716=CARTESIAN_POINT ( 'NONE',  ( 10.00000000000000000, 79.38136668499790005, -37.98155635597233726 ) ) ;
#13717=ORIENTED_EDGE ( 'NONE', *, *, #18162, .T. ) ;
#13719=CARTESIAN_POINT ( 'NONE',  ( 0.000000000000000000, 29.29369617358468858, 87.74003855418408193 ) ) ;
#13721=CIRCLE ( 'NONE', #21137, 88.00000000000000000 ) ;
#13724=CARTESIAN_POINT ( 'NONE',  ( 5.000000000000000000, 87.44637528609661103, 9.855528870798920593 ) ) ;
#13725=DIRECTION ( 'NONE',  ( -1.000000000000000000, -0.000000000000000000, 0.000000000000000000 ) ) ;
#13726=VECTOR ( 'NONE', #10331, 1000.000000000000000 ) ;
#13727=DIRECTION ( 'NONE',  ( -1.000000000000000000, 0.000000000000000000, 0.000000000000000000 ) ) ;
#13728=AXIS2_PLACEMENT_3D ( 'NONE', #18768, #21752, #20208 ) ;
#13729=VECTOR ( 'NONE', #17570, 1000.000000000000000 ) ;
#13730=DIRECTION ( 'NONE',  ( 0.000000000000000000, 0.9848077530122073542, 0.1736481776669339672 ) ) ;
#13731=CARTESIAN_POINT ( 'NONE',  ( 10.00000000000000000, -51.76708072107932423, 67.49339815138475274 ) ) ;
#13733=ORIENTED_EDGE ( 'NONE', *, *, #9308, .T. ) ;
#13734=CARTESIAN_POINT ( 'NONE',  ( 0.000000000000000000, -85.22372865846305956, 21.92979875759597874 ) ) ;
#13735=AXIS2_PLACEMENT_3D ( 'NONE', #304, #1844, #18540 ) ;
#13737=ORIENTED_EDGE ( 'NONE', *, *, #20708, .F. ) ;
#13738=EDGE_CURVE ( 'NONE', #1178, #879, #6617, .T. ) ;
#13739=CIRCLE ( 'NONE', #3160, 92.50100000000000477 ) ;
#13743=AXIS2_PLACEMENT_3D ( 'NONE', #3296, #15649, #14324 ) ;
#13746=ORIENTED_EDGE ( 'NONE', *, *, #17703, .T. ) ;
#13747=CARTESIAN_POINT ( 'NONE',  ( 0.000000000000000000, 0.000000000000000000, 0.000000000000000000 ) ) ;
#13748=ORIENTED_EDGE ( 'NONE', *, *, #9749, .F. ) ;
#13751=CARTESIAN_POINT ( 'NONE',  ( 0.000000000000000000, 0.000000000000000000, 0.000000000000000000 ) ) ;
#13752=EDGE_CURVE ( 'NONE', #10259, #5155, #16121, .T. ) ;
#13755=DIRECTION ( 'NONE',  ( -1.000000000000000000, -0.000000000000000000, -0.000000000000000000 ) ) ;
#13758=DIRECTION ( 'NONE',  ( 1.000000000000000000, -0.000000000000000000, -0.000000000000000000 ) ) ;
#13759=AXIS2_PLACEMENT_3D ( 'NONE', #18396, #9873, #3138 ) ;
#13760=ORIENTED_EDGE ( 'NONE', *, *, #3376, .T. ) ;
#13762=CARTESIAN_POINT ( 'NONE',  ( 10.00000000000000000, 66.01871308925461790, 64.79170103523043167 ) ) ;
#13763=ORIENTED_EDGE ( 'NONE', *, *, #7548, .T. ) ;
#13764=DIRECTION ( 'NONE',  ( 1.000000000000000000, 0.000000000000000000, 0.000000000000000000 ) ) ;
#13766=DIRECTION ( 'NONE',  ( 0.000000000000000000, 0.5877852522924690293, 0.8090169943749504489 ) ) ;
#13768=EDGE_CURVE ( 'NONE', #18065, #13052, #257, .T. ) ;
#13769=CARTESIAN_POINT ( 'NONE',  ( 10.00000000000000000, 0.000000000000000000, 0.000000000000000000 ) ) ;
#13770=VERTEX_POINT ( 'NONE', #17672 ) ;
#13772=VERTEX_POINT ( 'NONE', #19211 ) ;
#13773=ORIENTED_EDGE ( 'NONE', *, *, #16640, .F. ) ;
#13775=AXIS2_PLACEMENT_3D ( 'NONE', #9394, #2890, #2670 ) ;
#13777=EDGE_LOOP ( 'NONE', ( #7920, #12750, #19930, #3177 ) ) ;
#13778=CARTESIAN_POINT ( 'NONE',  ( 10.00000000000000000, 0.000000000000000000, 0.000000000000000000 ) ) ;
#13780=CARTESIAN_POINT ( 'NONE',  ( 10.00000000000000000, 70.37753541435941429, 60.02863908169658202 ) ) ;
#13781=FACE_OUTER_BOUND ( 'NONE', #4019, .T. ) ;
#13782=CARTESIAN_POINT ( 'NONE',  ( 0.000000000000000000, 0.000000000000000000, 0.000000000000000000 ) ) ;
#13784=EDGE_CURVE ( 'NONE', #3730, #17431, #15788, .T. ) ;
#13786=DIRECTION ( 'NONE',  ( -1.000000000000000000, -0.000000000000000000, 0.000000000000000000 ) ) ;
#13787=ORIENTED_EDGE ( 'NONE', *, *, #11078, .T. ) ;
#13788=EDGE_CURVE ( 'NONE', #2262, #8340, #5741, .T. ) ;
#13789=DIRECTION ( 'NONE',  ( 0.000000000000000000, 0.9993908270190958731, -0.03489949670249761771 ) ) ;
#13791=AXIS2_PLACEMENT_3D ( 'NONE', #15585, #3651, #17468 ) ;
#13793=ORIENTED_EDGE ( 'NONE', *, *, #5829, .T. ) ;
#13794=EDGE_CURVE ( 'NONE', #10604, #3544, #6271, .T. ) ;
#13796=ADVANCED_FACE ( 'NONE', ( #13909 ), #5635, .F. ) ;
#13797=EDGE_CURVE ( 'NONE', #18170, #10147, #9152, .T. ) ;
#13799=CARTESIAN_POINT ( 'NONE',  ( 0.000000000000000000, 18.94217447942673971, -85.93715160505934136 ) ) ;
#13800=ORIENTED_EDGE ( 'NONE', *, *, #16610, .T. ) ;
#13802=EDGE_LOOP ( 'NONE', ( #21842, #191, #9015, #16008 ) ) ;
#13803=ORIENTED_EDGE ( 'NONE', *, *, #3398, .T. ) ;
#13804=DIRECTION ( 'NONE',  ( 0.000000000000000000, 0.9702957262759954737, 0.2419218955996715048 ) ) ;
#13809=DIRECTION ( 'NONE',  ( 0.000000000000000000, 0.000000000000000000, 1.000000000000000000 ) ) ;
#13810=CARTESIAN_POINT ( 'NONE',  ( 10.00000000000000000, -84.80486432185169576, -36.94008646920480743 ) ) ;
#13811=FACE_OUTER_BOUND ( 'NONE', #7688, .T. ) ;
#13812=ADVANCED_FACE ( 'NONE', ( #2309 ), #20655, .F. ) ;
#13814=DIRECTION ( 'NONE',  ( 1.000000000000000000, 0.000000000000000000, 0.000000000000000000 ) ) ;
#13815=ORIENTED_EDGE ( 'NONE', *, *, #1661, .F. ) ;
#13816=EDGE_CURVE ( 'NONE', #9731, #7352, #18605, .T. ) ;
#13821=DIRECTION ( 'NONE',  ( 0.000000000000000000, -0.9945218953682744001, 0.1045284632676437425 ) ) ;
#13822=ADVANCED_FACE ( 'NONE', ( #12364 ), #655, .F. ) ;
#13823=ORIENTED_EDGE ( 'NONE', *, *, #9598, .F. ) ;
#13825=CARTESIAN_POINT ( 'NONE',  ( 0.000000000000000000, 0.000000000000000000, 0.000000000000000000 ) ) ;
#13826=ORIENTED_EDGE ( 'NONE', *, *, #10268, .F. ) ;
#13827=DIRECTION ( 'NONE',  ( 1.000000000000000000, 0.000000000000000000, 0.000000000000000000 ) ) ;
#13829=DIRECTION ( 'NONE',  ( 0.000000000000000000, 0.9702957262759972501, -0.2419218955996647880 ) ) ;
#13830=CARTESIAN_POINT ( 'NONE',  ( 10.00000000000000000, 0.000000000000000000, 0.000000000000000000 ) ) ;
#13831=EDGE_CURVE ( 'NONE', #18291, #4269, #19427, .T. ) ;
#13832=LINE ( 'NONE', #3341, #6851 ) ;
#13835=EDGE_LOOP ( 'NONE', ( #3111, #5480, #14990, #15905 ) ) ;
#13836=EDGE_CURVE ( 'NONE', #750, #21012, #10832, .T. ) ;
#13840=ORIENTED_EDGE ( 'NONE', *, *, #6132, .F. ) ;
#13842=ORIENTED_EDGE ( 'NONE', *, *, #7062, .T. ) ;
#13844=DIRECTION ( 'NONE',  ( 0.000000000000000000, -0.06975647374411138302, -0.9975640502598251969 ) ) ;
#13846=VERTEX_POINT ( 'NONE', #19109 ) ;
#13849=CYLINDRICAL_SURFACE ( 'NONE', #14546, 44.99999999999998579 ) ;
#13851=CYLINDRICAL_SURFACE ( 'NONE', #16753, 92.50100000000000477 ) ;
#13852=CARTESIAN_POINT ( 'NONE',  ( 10.00000000000000000, -3.974475837765555575, 92.41557521768190497 ) ) ;
#13853=DIRECTION ( 'NONE',  ( -1.000000000000000000, -0.000000000000000000, 0.000000000000000000 ) ) ;
#13854=CARTESIAN_POINT ( 'NONE',  ( 10.00000000000000000, 25.56104204395415991, -81.12843256239638379 ) ) ;
#13856=CIRCLE ( 'NONE', #14914, 44.99999999999999289 ) ;
#13857=DIRECTION ( 'NONE',  ( -1.000000000000000000, 0.000000000000000000, 0.000000000000000000 ) ) ;
#13858=CYLINDRICAL_SURFACE ( 'NONE', #17252, 88.00000000000000000 ) ;
#13860=DIRECTION ( 'NONE',  ( 0.000000000000000000, 0.000000000000000000, -1.000000000000000000 ) ) ;
#13862=ORIENTED_EDGE ( 'NONE', *, *, #15134, .T. ) ;
#13863=DIRECTION ( 'NONE',  ( -1.000000000000000000, -0.000000000000000000, -0.000000000000000000 ) ) ;
#13865=AXIS2_PLACEMENT_3D ( 'NONE', #758, #12464, #20551 ) ;
#13866=DIRECTION ( 'NONE',  ( -1.000000000000000000, -0.000000000000000000, -0.000000000000000000 ) ) ;
#13867=DIRECTION ( 'NONE',  ( 0.000000000000000000, 0.000000000000000000, 1.000000000000000000 ) ) ;
#13869=CIRCLE ( 'NONE', #17758, 92.50099999999999056 ) ;
#13871=ORIENTED_EDGE ( 'NONE', *, *, #3681, .F. ) ;
#13872=EDGE_LOOP ( 'NONE', ( #8889, #14027, #9602, #1300 ) ) ;
#13873=DIRECTION ( 'NONE',  ( 1.000000000000000000, -0.000000000000000000, -0.000000000000000000 ) ) ;
#13875=CARTESIAN_POINT ( 'NONE',  ( 10.00000000000000000, 0.000000000000000000, 0.000000000000000000 ) ) ;
#13877=CARTESIAN_POINT ( 'NONE',  ( 10.00000000000000000, 52.34334029047981574, -76.26670130689429072 ) ) ;
#13878=CARTESIAN_POINT ( 'NONE',  ( 10.00000000000000000, -61.60362715318993310, -62.84101464466307618 ) ) ;
#13880=VECTOR ( 'NONE', #13857, 1000.000000000000000 ) ;
#13881=EDGE_CURVE ( 'NONE', #9164, #5724, #17550, .T. ) ;
#13882=DIRECTION ( 'NONE',  ( -1.000000000000000000, 0.000000000000000000, 0.000000000000000000 ) ) ;
#13883=EDGE_LOOP ( 'NONE', ( #2640, #3955, #3653, #4891 ) ) ;
#13884=AXIS2_PLACEMENT_3D ( 'NONE', #20087, #15539, #2065 ) ;
#13888=EDGE_CURVE ( 'NONE', #13385, #20271, #20374, .T. ) ;
#13889=CARTESIAN_POINT ( 'NONE',  ( 0.000000000000000000, 0.000000000000000000, 0.000000000000000000 ) ) ;
#13890=VERTEX_POINT ( 'NONE', #7727 ) ;
#13892=CYLINDRICAL_SURFACE ( 'NONE', #19016, 88.00000000000000000 ) ;
#13893=VERTEX_POINT ( 'NONE', #11587 ) ;
#13895=ORIENTED_EDGE ( 'NONE', *, *, #15927, .T. ) ;
#13896=EDGE_CURVE ( 'NONE', #20086, #13770, #18954, .T. ) ;
#13898=ORIENTED_EDGE ( 'NONE', *, *, #10165, .T. ) ;
#13903=LINE ( 'NONE', #7399, #11389 ) ;
#13906=EDGE_CURVE ( 'NONE', #20618, #19098, #19308, .T. ) ;
#13907=FACE_OUTER_BOUND ( 'NONE', #16132, .T. ) ;
#13908=ADVANCED_FACE ( 'NONE', ( #16114 ), #11353, .T. ) ;
#13909=FACE_OUTER_BOUND ( 'NONE', #7092, .T. ) ;
#13910=DIRECTION ( 'NONE',  ( -1.000000000000000000, 0.000000000000000000, 0.000000000000000000 ) ) ;
#13913=FACE_OUTER_BOUND ( 'NONE', #10625, .T. ) ;
#13914=AXIS2_PLACEMENT_3D ( 'NONE', #20195, #8484, #7051 ) ;
#13916=EDGE_LOOP ( 'NONE', ( #9678, #9030, #13479, #2622 ) ) ;
#13921=ORIENTED_EDGE ( 'NONE', *, *, #9361, .F. ) ;
#13922=EDGE_CURVE ( 'NONE', #16787, #19647, #7655, .T. ) ;
#13923=CARTESIAN_POINT ( 'NONE',  ( 10.00000000000000000, 81.34229909304679040, 33.57723005635394742 ) ) ;
#13924=VECTOR ( 'NONE', #16052, 1000.000000000000000 ) ;
#13927=ORIENTED_EDGE ( 'NONE', *, *, #19847, .T. ) ;
#13928=CIRCLE ( 'NONE', #21688, 88.00000000000000000 ) ;
#13930=VECTOR ( 'NONE', #6020, 1000.000000000000000 ) ;
#13931=DIRECTION ( 'NONE',  ( 1.000000000000000000, 0.000000000000000000, 0.000000000000000000 ) ) ;
#13932=ORIENTED_EDGE ( 'NONE', *, *, #21481, .T. ) ;
#13933=DIRECTION ( 'NONE',  ( 1.000000000000000000, 0.000000000000000000, 0.000000000000000000 ) ) ;
#13934=AXIS2_PLACEMENT_3D ( 'NONE', #6676, #18887, #18380 ) ;
#13937=DIRECTION ( 'NONE',  ( 0.000000000000000000, 0.000000000000000000, 1.000000000000000000 ) ) ;
#13938=DIRECTION ( 'NONE',  ( 0.000000000000000000, -8.943463253924875462E-15, -1.000000000000000000 ) ) ;
#13939=DIRECTION ( 'NONE',  ( 0.000000000000000000, 0.000000000000000000, 1.000000000000000000 ) ) ;
#13941=DIRECTION ( 'NONE',  ( 0.000000000000000000, 0.06975647374411841906, 0.9975640502598247528 ) ) ;
#13942=EDGE_CURVE ( 'NONE', #10178, #21594, #621, .T. ) ;
#13944=ORIENTED_EDGE ( 'NONE', *, *, #10939, .F. ) ;
#13945=AXIS2_PLACEMENT_3D ( 'NONE', #3609, #5493, #17095 ) ;
#13946=VECTOR ( 'NONE', #7204, 1000.000000000000000 ) ;
#13947=CARTESIAN_POINT ( 'NONE',  ( 10.00000000000000000, 0.000000000000000000, 0.000000000000000000 ) ) ;
#13948=EDGE_CURVE ( 'NONE', #12492, #9371, #9418, .T. ) ;
#13949=DIRECTION ( 'NONE',  ( 0.000000000000000000, 0.000000000000000000, 1.000000000000000000 ) ) ;
#13951=AXIS2_PLACEMENT_3D ( 'NONE', #20165, #1390, #9981 ) ;
#13952=DIRECTION ( 'NONE',  ( 1.000000000000000000, 0.000000000000000000, 0.000000000000000000 ) ) ;
#13953=EDGE_CURVE ( 'NONE', #20112, #1976, #21417, .T. ) ;
#13954=ORIENTED_EDGE ( 'NONE', *, *, #12851, .T. ) ;
#13956=DIRECTION ( 'NONE',  ( 1.000000000000000000, 0.000000000000000000, 0.000000000000000000 ) ) ;
#13964=VECTOR ( 'NONE', #16252, 1000.000000000000000 ) ;
#13966=CARTESIAN_POINT ( 'NONE',  ( 10.00000000000000000, 14.02138820414913845, 83.89630571862289798 ) ) ;
#13967=CARTESIAN_POINT ( 'NONE',  ( 0.000000000000000000, 76.53853822673980289, 43.42639941457142072 ) ) ;
#13968=CARTESIAN_POINT ( 'NONE',  ( 5.000000000000002665, -6.797690662955810481, 87.73705831432212676 ) ) ;
#13971=ORIENTED_EDGE ( 'NONE', *, *, #13518, .T. ) ;
#13972=AXIS2_PLACEMENT_3D ( 'NONE', #18056, #1258, #21478 ) ;
#13975=AXIS2_PLACEMENT_3D ( 'NONE', #9157, #7947, #14680 ) ;
#13977=CARTESIAN_POINT ( 'NONE',  ( 0.000000000000000000, 87.96697768756401103, 2.410567674970879981 ) ) ;
#13979=DIRECTION ( 'NONE',  ( 0.000000000000000000, 0.000000000000000000, 1.000000000000000000 ) ) ;
#13980=DIRECTION ( 'NONE',  ( -1.000000000000000000, -0.000000000000000000, -0.000000000000000000 ) ) ;
#13981=VERTEX_POINT ( 'NONE', #21535 ) ;
#13982=( LENGTH_UNIT ( ) NAMED_UNIT ( * ) SI_UNIT ( .MILLI., .METRE. ) );
#13984=VERTEX_POINT ( 'NONE', #2858 ) ;
#13986=CARTESIAN_POINT ( 'NONE',  ( 10.00000000000000000, -60.65655256511276860, 59.63197188857500919 ) ) ;
#13987=ORIENTED_EDGE ( 'NONE', *, *, #8165, .F. ) ;
#13989=LINE ( 'NONE', #13780, #14751 ) ;
#13991=CARTESIAN_POINT ( 'NONE',  ( 0.000000000000000000, 62.44821182181091501, 68.23969402963524544 ) ) ;
#13994=AXIS2_PLACEMENT_3D ( 'NONE', #6327, #11280, #16581 ) ;
#13995=LINE ( 'NONE', #20740, #18062 ) ;
#13996=DIRECTION ( 'NONE',  ( 0.000000000000000000, 1.141062553086966690E-14, -1.000000000000000000 ) ) ;
#13997=VERTEX_POINT ( 'NONE', #9572 ) ;
#13998=CARTESIAN_POINT ( 'NONE',  ( 0.000000000000000000, 84.80486432185190893, 36.94008646920423899 ) ) ;
#14000=DIRECTION ( 'NONE',  ( -1.000000000000000000, -0.000000000000000000, -0.000000000000000000 ) ) ;
#14002=AXIS2_PLACEMENT_3D ( 'NONE', #18134, #21328, #6544 ) ;
#14003=CARTESIAN_POINT ( 'NONE',  ( 0.000000000000000000, 17.64925110578469258, 86.21197095186350623 ) ) ;
#14004=AXIS2_PLACEMENT_3D ( 'NONE', #14213, #6055, #14544 ) ;
#14006=CARTESIAN_POINT ( 'NONE',  ( 10.00000000000000000, 56.05743251323859511, 67.83483072893820065 ) ) ;
#14009=ORIENTED_EDGE ( 'NONE', *, *, #13241, .T. ) ;
#14010=ADVANCED_FACE ( 'NONE', ( #21631 ), #18104, .F. ) ;
#14011=ORIENTED_EDGE ( 'NONE', *, *, #10642, .T. ) ;
#14012=DIRECTION ( 'NONE',  ( 0.000000000000000000, 0.000000000000000000, 1.000000000000000000 ) ) ;
#14017=EDGE_CURVE ( 'NONE', #10738, #8155, #965, .T. ) ;
#14019=VECTOR ( 'NONE', #15861, 1000.000000000000000 ) ;
#14020=DIRECTION ( 'NONE',  ( 1.000000000000000000, 0.000000000000000000, 0.000000000000000000 ) ) ;
#14024=CYLINDRICAL_SURFACE ( 'NONE', #2432, 88.00000000000000000 ) ;
#14027=ORIENTED_EDGE ( 'NONE', *, *, #9840, .F. ) ;
#14028=ORIENTED_EDGE ( 'NONE', *, *, #13816, .F. ) ;
#14030=FACE_OUTER_BOUND ( 'NONE', #21342, .T. ) ;
#14031=ORIENTED_EDGE ( 'NONE', *, *, #16589, .T. ) ;
#14034=ADVANCED_FACE ( 'NONE', ( #10348 ), #3514, .F. ) ;
#14035=VECTOR ( 'NONE', #3721, 1000.000000000000000 ) ;
#14036=EDGE_CURVE ( 'NONE', #21192, #2153, #4852, .T. ) ;
#14037=EDGE_LOOP ( 'NONE', ( #2116, #18447, #14217, #5483 ) ) ;
#14038=CIRCLE ( 'NONE', #6304, 44.99999999999999289 ) ;
#14039=DIRECTION ( 'NONE',  ( 0.000000000000000000, 0.1391731009600657432, -0.9902680687415702510 ) ) ;
#14040=EDGE_CURVE ( 'NONE', #15909, #7517, #6988, .T. ) ;
#14042=CARTESIAN_POINT ( 'NONE',  ( 10.00000000000000000, 16.79755869217650144, 90.96305306542258506 ) ) ;
#14051=DIRECTION ( 'NONE',  ( 0.000000000000000000, 0.7431448254773909134, 0.6691306063588619013 ) ) ;
#14053=AXIS2_PLACEMENT_3D ( 'NONE', #2089, #5398, #3740 ) ;
#14054=AXIS2_PLACEMENT_3D ( 'NONE', #14826, #8194, #1240 ) ;
#14056=AXIS2_PLACEMENT_3D ( 'NONE', #6329, #9600, #8187 ) ;
#14057=EDGE_CURVE ( 'NONE', #6401, #12429, #8386, .T. ) ;
#14059=DIRECTION ( 'NONE',  ( -1.000000000000000000, -0.000000000000000000, -0.000000000000000000 ) ) ;
#14060=VERTEX_POINT ( 'NONE', #204 ) ;
#14061=EDGE_CURVE ( 'NONE', #15549, #3324, #15790, .T. ) ;
#14062=DIRECTION ( 'NONE',  ( 0.000000000000000000, 0.000000000000000000, 1.000000000000000000 ) ) ;
#14066=DIRECTION ( 'NONE',  ( -1.000000000000000000, -0.000000000000000000, -0.000000000000000000 ) ) ;
#14067=EDGE_CURVE ( 'NONE', #15044, #6894, #5289, .T. ) ;
#14068=ORIENTED_EDGE ( 'NONE', *, *, #14861, .T. ) ;
#14069=AXIS2_PLACEMENT_3D ( 'NONE', #16312, #2731, #4276 ) ;
#14070=ORIENTED_EDGE ( 'NONE', *, *, #10008, .T. ) ;
#14071=LINE ( 'NONE', #2354, #9677 ) ;
#14072=VECTOR ( 'NONE', #4172, 1000.000000000000000 ) ;
#14074=FACE_OUTER_BOUND ( 'NONE', #9073, .T. ) ;
#14076=CARTESIAN_POINT ( 'NONE',  ( 10.00000000000000000, 84.80486432185243473, -36.94008646920313055 ) ) ;
#14077=CARTESIAN_POINT ( 'NONE',  ( 10.00000000000000000, 0.000000000000000000, 0.000000000000000000 ) ) ;
#14078=LINE ( 'NONE', #5904, #20247 ) ;
#14079=DIRECTION ( 'NONE',  ( 1.000000000000000000, 0.000000000000000000, 0.000000000000000000 ) ) ;
#14082=EDGE_CURVE ( 'NONE', #14609, #10308, #13680, .T. ) ;
#14084=CIRCLE ( 'NONE', #11635, 88.00000000000000000 ) ;
#14086=EDGE_CURVE ( 'NONE', #8339, #18927, #11695, .T. ) ;
#14088=CIRCLE ( 'NONE', #20110, 45.00000000000000000 ) ;
#14094=ORIENTED_EDGE ( 'NONE', *, *, #20140, .F. ) ;
#14095=ORIENTED_EDGE ( 'NONE', *, *, #2553, .T. ) ;
#14096=EDGE_CURVE ( 'NONE', #19663, #20330, #5925, .T. ) ;
#14097=EDGE_LOOP ( 'NONE', ( #1622, #18114, #232, #5217 ) ) ;
#14099=CARTESIAN_POINT ( 'NONE',  ( 10.00000000000000000, 85.22372865846293166, 21.92979875759657560 ) ) ;
#14100=DIRECTION ( 'NONE',  ( 0.000000000000000000, 0.6946583704589984753, -0.7193398003386500816 ) ) ;
#14101=VERTEX_POINT ( 'NONE', #8705 ) ;
#14103=CARTESIAN_POINT ( 'NONE',  ( 10.00000000000000000, -15.51843147776405729, 83.63233659819645993 ) ) ;
#14104=DIRECTION ( 'NONE',  ( 1.000000000000000000, 0.000000000000000000, 0.000000000000000000 ) ) ;
#14107=CARTESIAN_POINT ( 'NONE',  ( 0.000000000000000000, -75.45728100697571961, -39.26051685139143643 ) ) ;
#14108=CARTESIAN_POINT ( 'NONE',  ( 0.000000000000000000, 85.22372865846293166, 21.92979875759657560 ) ) ;
#14109=ORIENTED_EDGE ( 'NONE', *, *, #1205, .T. ) ;
#14111=CARTESIAN_POINT ( 'NONE',  ( 0.000000000000000000, -17.64925110578410639, -86.21197095186363413 ) ) ;
#14112=EDGE_CURVE ( 'NONE', #10738, #11183, #3293, .T. ) ;
#14114=ORIENTED_EDGE ( 'NONE', *, *, #16407, .T. ) ;
#14117=AXIS2_PLACEMENT_3D ( 'NONE', #14711, #2554, #10848 ) ;
#14118=CARTESIAN_POINT ( 'NONE',  ( 10.00000000000000000, -84.79630770241089976, 6.691460262315113816 ) ) ;
#14119=ORIENTED_EDGE ( 'NONE', *, *, #13213, .F. ) ;
#14121=ORIENTED_EDGE ( 'NONE', *, *, #17571, .T. ) ;
#14123=EDGE_LOOP ( 'NONE', ( #8556, #7866, #3058, #2206 ) ) ;
#14126=DIRECTION ( 'NONE',  ( 0.000000000000000000, 0.000000000000000000, 1.000000000000000000 ) ) ;
#14129=CARTESIAN_POINT ( 'NONE',  ( 10.00000000000000000, 0.000000000000000000, 0.000000000000000000 ) ) ;
#14130=CARTESIAN_POINT ( 'NONE',  ( 10.00000000000000000, 0.000000000000000000, 0.000000000000000000 ) ) ;
#14131=CIRCLE ( 'NONE', #15901, 88.00000000000000000 ) ;
#14135=EDGE_LOOP ( 'NONE', ( #13871, #14121, #1325, #3814 ) ) ;
#14136=CARTESIAN_POINT ( 'NONE',  ( 10.00000000000000000, 0.000000000000000000, 0.000000000000000000 ) ) ;
#14138=VERTEX_POINT ( 'NONE', #8377 ) ;
#14139=ORIENTED_EDGE ( 'NONE', *, *, #8509, .T. ) ;
#14140=VERTEX_POINT ( 'NONE', #20427 ) ;
#14141=ORIENTED_EDGE ( 'NONE', *, *, #3966, .T. ) ;
#14142=ORIENTED_EDGE ( 'NONE', *, *, #12021, .F. ) ;
#14144=ORIENTED_EDGE ( 'NONE', *, *, #16809, .F. ) ;
#14145=DIRECTION ( 'NONE',  ( 0.000000000000000000, -0.9993908270190960952, 0.03489949670249099800 ) ) ;
#14146=DIRECTION ( 'NONE',  ( -1.000000000000000000, 0.000000000000000000, 0.000000000000000000 ) ) ;
#14149=DIRECTION ( 'NONE',  ( -1.000000000000000000, -0.000000000000000000, -0.000000000000000000 ) ) ;
#14150=DIRECTION ( 'NONE',  ( 0.000000000000000000, 0.8987940462991681478, -0.4383711467890751279 ) ) ;
#14151=CARTESIAN_POINT ( 'NONE',  ( 0.000000000000000000, 85.05652083079336023, -0.7600687895862878740 ) ) ;
#14152=CARTESIAN_POINT ( 'NONE',  ( 10.00000000000000000, 87.92084725184948013, 3.731570516143270400 ) ) ;
#14154=ORIENTED_EDGE ( 'NONE', *, *, #12863, .T. ) ;
#14156=EDGE_CURVE ( 'NONE', #17938, #15909, #1522, .T. ) ;
#14157=DIRECTION ( 'NONE',  ( -1.000000000000000000, 0.000000000000000000, -0.000000000000000000 ) ) ;
#14158=CARTESIAN_POINT ( 'NONE',  ( 5.000000000000002665, -29.47587714451095309, 82.91666097089111531 ) ) ;
#14160=DIRECTION ( 'NONE',  ( 0.000000000000000000, 0.000000000000000000, 1.000000000000000000 ) ) ;
#14161=ORIENTED_EDGE ( 'NONE', *, *, #2716, .F. ) ;
#14163=ADVANCED_FACE ( 'NONE', ( #1145 ), #7668, .F. ) ;
#14168=CARTESIAN_POINT ( 'NONE',  ( 10.00000000000000000, 51.10509369859540385, -77.10190917907144126 ) ) ;
#14170=LINE ( 'NONE', #12511, #14988 ) ;
#14171=DIRECTION ( 'NONE',  ( 0.000000000000000000, -1.603655480014115143E-14, -1.000000000000000000 ) ) ;
#14172=DIRECTION ( 'NONE',  ( -1.000000000000000000, 0.000000000000000000, 0.000000000000000000 ) ) ;
#14173=DIRECTION ( 'NONE',  ( 1.000000000000000000, 0.000000000000000000, 0.000000000000000000 ) ) ;
#14174=AXIS2_PLACEMENT_3D ( 'NONE', #8586, #17209, #10343 ) ;
#14175=CARTESIAN_POINT ( 'NONE',  ( 0.000000000000000000, 31.15801000616834315, 79.14775961996400611 ) ) ;
#14176=DIRECTION ( 'NONE',  ( 0.000000000000000000, 0.000000000000000000, 1.000000000000000000 ) ) ;
#14177=CYLINDRICAL_SURFACE ( 'NONE', #3807, 92.50100000000000477 ) ;
#14181=ORIENTED_EDGE ( 'NONE', *, *, #2874, .F. ) ;
#14182=DIRECTION ( 'NONE',  ( 1.000000000000000000, 0.000000000000000000, 0.000000000000000000 ) ) ;
#14183=ADVANCED_FACE ( 'NONE', ( #2362 ), #21366, .F. ) ;
#14184=VERTEX_POINT ( 'NONE', #5906 ) ;
#14186=ORIENTED_EDGE ( 'NONE', *, *, #9277, .T. ) ;
#14188=AXIS2_PLACEMENT_3D ( 'NONE', #17586, #14146, #6991 ) ;
#14190=EDGE_LOOP ( 'NONE', ( #642, #15587, #6876, #20029 ) ) ;
#14191=ADVANCED_FACE ( 'NONE', ( #807 ), #19600, .F. ) ;
#14194=ORIENTED_EDGE ( 'NONE', *, *, #595, .T. ) ;
#14196=DIRECTION ( 'NONE',  ( 1.000000000000000000, 0.000000000000000000, 0.000000000000000000 ) ) ;
#14201=CARTESIAN_POINT ( 'NONE',  ( 0.000000000000000000, 40.72878876293257377, -78.00747250042405767 ) ) ;
#14202=CARTESIAN_POINT ( 'NONE',  ( 10.00000000000000000, -81.97107881582211064, 22.71412948308539370 ) ) ;
#14203=CARTESIAN_POINT ( 'NONE',  ( 0.000000000000000000, 57.06999622551897033, -66.98518889142023625 ) ) ;
#14204=CARTESIAN_POINT ( 'NONE',  ( 10.00000000000000000, 92.32475887865426500, 5.707354816230855832 ) ) ;
#14206=DIRECTION ( 'NONE',  ( 0.000000000000000000, 0.000000000000000000, 1.000000000000000000 ) ) ;
#14208=CARTESIAN_POINT ( 'NONE',  ( 0.000000000000000000, 24.89070495400845573, -84.40647372620476574 ) ) ;
#14209=AXIS2_PLACEMENT_3D ( 'NONE', #13367, #5086, #20120 ) ;
#14210=EDGE_CURVE ( 'NONE', #2159, #13683, #10978, .T. ) ;
#14211=CARTESIAN_POINT ( 'NONE',  ( 0.000000000000000000, -86.54587337002888603, 15.93147207946976707 ) ) ;
#14213=CARTESIAN_POINT ( 'NONE',  ( 10.00000000000000000, 0.000000000000000000, 0.000000000000000000 ) ) ;
#14216=AXIS2_PLACEMENT_3D ( 'NONE', #5765, #2540, #17481 ) ;
#14217=ORIENTED_EDGE ( 'NONE', *, *, #8275, .T. ) ;
#14220=VECTOR ( 'NONE', #21198, 1000.000000000000000 ) ;
#14221=ORIENTED_EDGE ( 'NONE', *, *, #5813, .T. ) ;
#14223=DIRECTION ( 'NONE',  ( 0.000000000000000000, 0.000000000000000000, 1.000000000000000000 ) ) ;
#14224=EDGE_CURVE ( 'NONE', #14686, #6084, #2042, .T. ) ;
#14228=DIRECTION ( 'NONE',  ( 0.000000000000000000, 0.6427876096865353661, 0.7660444431189814551 ) ) ;
#14231=DIRECTION ( 'NONE',  ( -1.000000000000000000, 0.000000000000000000, 0.000000000000000000 ) ) ;
#14232=CIRCLE ( 'NONE', #2244, 92.50100000000000477 ) ;
#14233=EDGE_CURVE ( 'NONE', #4066, #18821, #16056, .T. ) ;
#14234=DIRECTION ( 'NONE',  ( 0.000000000000000000, 0.000000000000000000, 1.000000000000000000 ) ) ;
#14237=LINE ( 'NONE', #16000, #17199 ) ;
#14238=DIRECTION ( 'NONE',  ( 0.000000000000000000, 0.9702957262759955848, 0.2419218955996714493 ) ) ;
#14240=DIRECTION ( 'NONE',  ( -1.000000000000000000, -0.000000000000000000, 0.000000000000000000 ) ) ;
#14245=ORIENTED_EDGE ( 'NONE', *, *, #18493, .T. ) ;
#14246=VERTEX_POINT ( 'NONE', #9103 ) ;
#14247=ORIENTED_EDGE ( 'NONE', *, *, #3392, .F. ) ;
#14248=DIRECTION ( 'NONE',  ( -1.000000000000000000, -0.000000000000000000, -0.000000000000000000 ) ) ;
#14251=DIRECTION ( 'NONE',  ( 0.000000000000000000, 0.000000000000000000, 1.000000000000000000 ) ) ;
#14252=DIRECTION ( 'NONE',  ( 0.000000000000000000, 0.9848077530122084644, -0.1736481776669273336 ) ) ;
#14255=CARTESIAN_POINT ( 'NONE',  ( -10.00000000000000000, 0.000000000000000000, 0.000000000000000000 ) ) ;
#14256=CIRCLE ( 'NONE', #10741, 88.00000000000000000 ) ;
#14257=DIRECTION ( 'NONE',  ( 0.000000000000000000, -0.5299192642332118952, 0.8480480961564216269 ) ) ;
#14259=DIRECTION ( 'NONE',  ( -1.000000000000000000, -0.000000000000000000, -0.000000000000000000 ) ) ;
#14261=CARTESIAN_POINT ( 'NONE',  ( 5.000000000000000000, 76.53853822673980289, 43.42639941457142072 ) ) ;
#14262=AXIS2_PLACEMENT_3D ( 'NONE', #918, #14400, #11082 ) ;
#14263=AXIS2_PLACEMENT_3D ( 'NONE', #18983, #319, #522 ) ;
#14265=VECTOR ( 'NONE', #5788, 1000.000000000000000 ) ;
#14266=FACE_OUTER_BOUND ( 'NONE', #19396, .T. ) ;
#14267=ORIENTED_EDGE ( 'NONE', *, *, #17166, .T. ) ;
#14268=FACE_OUTER_BOUND ( 'NONE', #4654, .T. ) ;
#14269=ORIENTED_EDGE ( 'NONE', *, *, #2018, .T. ) ;
#14270=AXIS2_PLACEMENT_3D ( 'NONE', #16701, #11521, #9853 ) ;
#14272=CARTESIAN_POINT ( 'NONE',  ( 10.00000000000000000, 35.34277389771534672, 85.48288328206398035 ) ) ;
#14273=ORIENTED_EDGE ( 'NONE', *, *, #15577, .F. ) ;
#14274=ADVANCED_FACE ( 'NONE', ( #6027 ), #16278, .F. ) ;
#14276=LINE ( 'NONE', #12302, #13201 ) ;
#14277=CYLINDRICAL_SURFACE ( 'NONE', #9138, 88.00000000000000000 ) ;
#14278=CIRCLE ( 'NONE', #2993, 44.99999999999999289 ) ;
#14279=LINE ( 'NONE', #9298, #10391 ) ;
#14280=DIRECTION ( 'NONE',  ( 0.000000000000000000, 0.000000000000000000, 1.000000000000000000 ) ) ;
#14281=CIRCLE ( 'NONE', #8979, 45.00000000000000000 ) ;
#14283=DIRECTION ( 'NONE',  ( 0.000000000000000000, 0.000000000000000000, 1.000000000000000000 ) ) ;
#14284=ADVANCED_FACE ( 'NONE', ( #2477 ), #14177, .F. ) ;
#14287=LINE ( 'NONE', #19599, #5215 ) ;
#14288=DIRECTION ( 'NONE',  ( 0.000000000000000000, 0.000000000000000000, 1.000000000000000000 ) ) ;
#14291=CIRCLE ( 'NONE', #6561, 92.50100000000000477 ) ;
#14293=EDGE_LOOP ( 'NONE', ( #8847, #2952, #19019, #14721 ) ) ;
#14294=CIRCLE ( 'NONE', #19952, 44.99999999999998579 ) ;
#14297=AXIS2_PLACEMENT_3D ( 'NONE', #1370, #19813, #18388 ) ;
#14298=CIRCLE ( 'NONE', #542, 88.00000000000000000 ) ;
#14299=DIRECTION ( 'NONE',  ( 0.000000000000000000, -0.6427876096865299260, -0.7660444431189857850 ) ) ;
#14301=EDGE_LOOP ( 'NONE', ( #10610, #7251, #6635, #9129 ) ) ;
#14302=( NAMED_UNIT ( * ) SI_UNIT ( $, .STERADIAN. ) SOLID_ANGLE_UNIT ( ) );
#14303=AXIS2_PLACEMENT_3D ( 'NONE', #9382, #17690, #4308 ) ;
#14304=ORIENTED_EDGE ( 'NONE', *, *, #3499, .T. ) ;
#14305=ORIENTED_EDGE ( 'NONE', *, *, #14061, .T. ) ;
#14306=EDGE_CURVE ( 'NONE', #7513, #17141, #15462, .T. ) ;
#14310=DIRECTION ( 'NONE',  ( 0.000000000000000000, 0.3420201433256693235, -0.9396926207859080948 ) ) ;
#14311=DIRECTION ( 'NONE',  ( 0.000000000000000000, -0.6946583704589885944, -0.7193398003386595185 ) ) ;
#14313=EDGE_CURVE ( 'NONE', #2674, #11040, #19683, .T. ) ;
#14314=LINE ( 'NONE', #17532, #4739 ) ;
#14317=DIRECTION ( 'NONE',  ( 0.000000000000000000, 0.9271838545667884235, -0.3746065934159096833 ) ) ;
#14320=CIRCLE ( 'NONE', #2661, 44.99999999999999289 ) ;
#14321=AXIS2_PLACEMENT_3D ( 'NONE', #20069, #64, #6814 ) ;
#14322=EDGE_LOOP ( 'NONE', ( #150, #5720, #3930, #19776 ) ) ;
#14324=DIRECTION ( 'NONE',  ( 0.000000000000000000, 0.000000000000000000, 1.000000000000000000 ) ) ;
#14328=EDGE_CURVE ( 'NONE', #8172, #3525, #8404, .T. ) ;
#14329=DIRECTION ( 'NONE',  ( 0.000000000000000000, 0.000000000000000000, 1.000000000000000000 ) ) ;
#14330=ORIENTED_EDGE ( 'NONE', *, *, #15106, .F. ) ;
#14332=EDGE_LOOP ( 'NONE', ( #12889, #21718, #21136, #16288 ) ) ;
#14337=CIRCLE ( 'NONE', #5175, 92.50100000000000477 ) ;
#14338=ORIENTED_EDGE ( 'NONE', *, *, #15652, .F. ) ;
#14340=CIRCLE ( 'NONE', #10461, 100.0000000000000000 ) ;
#14343=CARTESIAN_POINT ( 'NONE',  ( 0.000000000000000000, -87.58454185039444440, 8.540961822681374827 ) ) ;
#14344=EDGE_CURVE ( 'NONE', #19278, #3086, #11738, .T. ) ;
#14346=FACE_OUTER_BOUND ( 'NONE', #20384, .T. ) ;
#14347=CARTESIAN_POINT ( 'NONE',  ( 10.00000000000000000, 0.000000000000000000, 0.000000000000000000 ) ) ;
#14348=DIRECTION ( 'NONE',  ( -1.000000000000000000, 0.000000000000000000, 0.000000000000000000 ) ) ;
#14349=CARTESIAN_POINT ( 'NONE',  ( 10.00000000000000000, -83.35585896458606214, -16.94078559808036033 ) ) ;
#14351=DIRECTION ( 'NONE',  ( -1.000000000000000000, -0.000000000000000000, 0.000000000000000000 ) ) ;
#14352=DIRECTION ( 'NONE',  ( 1.000000000000000000, 0.000000000000000000, 0.000000000000000000 ) ) ;
#14353=ADVANCED_FACE ( 'NONE', ( #18488 ), #4794, .F. ) ;
#14355=EDGE_CURVE ( 'NONE', #15532, #49, #10080, .T. ) ;
#14356=DIRECTION ( 'NONE',  ( -1.000000000000000000, 0.000000000000000000, 0.000000000000000000 ) ) ;
#14359=EDGE_CURVE ( 'NONE', #17932, #13478, #14038, .T. ) ;
#14360=EDGE_CURVE ( 'NONE', #8996, #21383, #21479, .T. ) ;
#14361=VERTEX_POINT ( 'NONE', #19814 ) ;
#14362=VERTEX_POINT ( 'NONE', #19709 ) ;
#14363=VERTEX_POINT ( 'NONE', #6575 ) ;
#14364=DIRECTION ( 'NONE',  ( 0.000000000000000000, 0.8290375725550428454, -0.5591929034707450175 ) ) ;
#14366=ADVANCED_FACE ( 'NONE', ( #4675 ), #8442, .F. ) ;
#14368=CARTESIAN_POINT ( 'NONE',  ( 10.00000000000000000, 0.000000000000000000, 0.000000000000000000 ) ) ;
#14372=DIRECTION ( 'NONE',  ( 0.000000000000000000, -0.5299192642331944647, -0.8480480961564325071 ) ) ;
#14379=DIRECTION ( 'NONE',  ( -1.000000000000000000, -0.000000000000000000, -0.000000000000000000 ) ) ;
#14382=AXIS2_PLACEMENT_3D ( 'NONE', #6785, #18811, #8753 ) ;
#14383=CARTESIAN_POINT ( 'NONE',  ( 10.00000000000000000, 0.000000000000000000, 0.000000000000000000 ) ) ;
#14386=FACE_OUTER_BOUND ( 'NONE', #19800, .T. ) ;
#14387=EDGE_LOOP ( 'NONE', ( #3652, #5425, #1484, #15840 ) ) ;
#14396=CIRCLE ( 'NONE', #4879, 92.50100000000000477 ) ;
#14397=LINE ( 'NONE', #13166, #13930 ) ;
#14399=DIRECTION ( 'NONE',  ( 0.000000000000000000, 0.000000000000000000, 1.000000000000000000 ) ) ;
#14400=DIRECTION ( 'NONE',  ( 1.000000000000000000, 0.000000000000000000, 0.000000000000000000 ) ) ;
#14401=CIRCLE ( 'NONE', #7004, 44.99999999999999289 ) ;
#14402=CARTESIAN_POINT ( 'NONE',  ( 10.00000000000000000, -86.66425444033941972, 32.33793443156368852 ) ) ;
#14404=CARTESIAN_POINT ( 'NONE',  ( 10.00000000000000000, 45.60224695560570041, 80.47900393021744492 ) ) ;
#14407=ADVANCED_FACE ( 'NONE', ( #11307 ), #16711, .F. ) ;
#14408=VERTEX_POINT ( 'NONE', #8324 ) ;
#14409=CARTESIAN_POINT ( 'NONE',  ( 10.00000000000000000, 43.18649929580192293, 73.28107340219430910 ) ) ;
#14413=AXIS2_PLACEMENT_3D ( 'NONE', #12393, #4004, #4445 ) ;
#14414=CARTESIAN_POINT ( 'NONE',  ( 10.00000000000000000, 0.000000000000000000, 0.000000000000000000 ) ) ;
#14416=CIRCLE ( 'NONE', #651, 92.50099999999999056 ) ;
#14417=ORIENTED_EDGE ( 'NONE', *, *, #20268, .F. ) ;
#14420=EDGE_LOOP ( 'NONE', ( #14782, #2479, #20587, #4277 ) ) ;
#14422=VERTEX_POINT ( 'NONE', #1468 ) ;
#14423=CARTESIAN_POINT ( 'NONE',  ( 10.00000000000000000, -23.10190250628773967, -89.56973317806621537 ) ) ;
#14424=CARTESIAN_POINT ( 'NONE',  ( 0.000000000000000000, 0.000000000000000000, 0.000000000000000000 ) ) ;
#14425=ORIENTED_EDGE ( 'NONE', *, *, #17266, .T. ) ;
#14426=DIRECTION ( 'NONE',  ( -1.000000000000000000, -0.000000000000000000, 0.000000000000000000 ) ) ;
#14427=CARTESIAN_POINT ( 'NONE',  ( 0.000000000000000000, -51.76708072107932423, 67.49339815138475274 ) ) ;
#14431=CARTESIAN_POINT ( 'NONE',  ( 0.000000000000000000, 65.83713140174729972, 58.39068529131218099 ) ) ;
#14434=ORIENTED_EDGE ( 'NONE', *, *, #12851, .F. ) ;
#14435=AXIS2_PLACEMENT_3D ( 'NONE', #18579, #3755, #20555 ) ;
#14438=ADVANCED_FACE ( 'NONE', ( #13289 ), #15056, .F. ) ;
#14441=CYLINDRICAL_SURFACE ( 'NONE', #3493, 92.50100000000000477 ) ;
#14446=CIRCLE ( 'NONE', #17276, 44.99999999999998579 ) ;
#14447=VERTEX_POINT ( 'NONE', #4904 ) ;
#14448=AXIS2_PLACEMENT_3D ( 'NONE', #21806, #9641, #15063 ) ;
#14452=CIRCLE ( 'NONE', #11637, 44.99999999999999289 ) ;
#14455=DIRECTION ( 'NONE',  ( 0.000000000000000000, -0.8660254037844328234, -0.5000000000000101030 ) ) ;
#14456=DIRECTION ( 'NONE',  ( -1.000000000000000000, 0.000000000000000000, 0.000000000000000000 ) ) ;
#14458=LINE ( 'NONE', #17669, #14220 ) ;
#14459=EDGE_CURVE ( 'NONE', #1120, #6202, #17580, .T. ) ;
#14461=DIRECTION ( 'NONE',  ( 0.000000000000000000, -0.9848077530122096857, 0.1736481776669207000 ) ) ;
#14462=DIRECTION ( 'NONE',  ( 0.000000000000000000, 0.000000000000000000, 1.000000000000000000 ) ) ;
#14463=CYLINDRICAL_SURFACE ( 'NONE', #333, 92.50100000000000477 ) ;
#14464=EDGE_CURVE ( 'NONE', #10717, #16982, #11645, .T. ) ;
#14465=EDGE_CURVE ( 'NONE', #535, #20663, #4524, .T. ) ;
#14467=AXIS2_PLACEMENT_3D ( 'NONE', #3350, #13509, #21693 ) ;
#14468=CARTESIAN_POINT ( 'NONE',  ( 10.00000000000000000, 74.74361964203228581, -40.60271866773572214 ) ) ;
#14469=APPLICATION_CONTEXT ( 'automotive_design' ) ;
#14470=EDGE_LOOP ( 'NONE', ( #11646, #16188, #17651, #3176 ) ) ;
#14471=EDGE_CURVE ( 'NONE', #11540, #17704, #14401, .T. ) ;
#14476=EDGE_CURVE ( 'NONE', #2910, #10178, #13617, .T. ) ;
#14477=DIRECTION ( 'NONE',  ( -1.000000000000000000, -0.000000000000000000, -0.000000000000000000 ) ) ;
#14479=CARTESIAN_POINT ( 'NONE',  ( 10.00000000000000000, 0.000000000000000000, 0.000000000000000000 ) ) ;
#14480=AXIS2_PLACEMENT_3D ( 'NONE', #1559, #3325, #4770 ) ;
#14481=EDGE_CURVE ( 'NONE', #6576, #10476, #4882, .T. ) ;
#14483=DIRECTION ( 'NONE',  ( 0.000000000000000000, -9.714451465470122884E-15, -1.000000000000000000 ) ) ;
#14484=EDGE_CURVE ( 'NONE', #11183, #4150, #4867, .T. ) ;
#14485=FACE_OUTER_BOUND ( 'NONE', #20025, .T. ) ;
#14486=CARTESIAN_POINT ( 'NONE',  ( 10.00000000000000000, -41.21966518005896774, -82.80926399530329718 ) ) ;
#14488=EDGE_CURVE ( 'NONE', #8283, #18366, #14754, .T. ) ;
#14489=DIRECTION ( 'NONE',  ( 0.000000000000000000, 0.3420201433256631063, 0.9396926207859105373 ) ) ;
#14493=CARTESIAN_POINT ( 'NONE',  ( 10.00000000000000000, 78.01214607583752070, 33.90124636420136994 ) ) ;
#14494=ADVANCED_FACE ( 'NONE', ( #15376 ), #252, .F. ) ;
#14495=VECTOR ( 'NONE', #21728, 1000.000000000000000 ) ;
#14497=DIRECTION ( 'NONE',  ( 0.000000000000000000, -0.4694715627858797591, -0.8829475928589327616 ) ) ;
#14499=ORIENTED_EDGE ( 'NONE', *, *, #13544, .F. ) ;
#14501=ORIENTED_EDGE ( 'NONE', *, *, #21199, .T. ) ;
#14504=ORIENTED_EDGE ( 'NONE', *, *, #19154, .F. ) ;
#14505=ORIENTED_EDGE ( 'NONE', *, *, #20152, .F. ) ;
#14507=EDGE_CURVE ( 'NONE', #11658, #8121, #17223, .T. ) ;
#14508=CARTESIAN_POINT ( 'NONE',  ( 5.000000000000002665, -17.64925110578410639, -86.21197095186363413 ) ) ;
#14513=CARTESIAN_POINT ( 'NONE',  ( 10.00000000000000000, 0.000000000000000000, 0.000000000000000000 ) ) ;
#14514=ADVANCED_FACE ( 'NONE', ( #17272 ), #10403, .F. ) ;
#14515=CARTESIAN_POINT ( 'NONE',  ( 0.000000000000000000, -15.32665449651862843, -91.22241316115434984 ) ) ;
#14517=ORIENTED_EDGE ( 'NONE', *, *, #8527, .T. ) ;
#14520=CARTESIAN_POINT ( 'NONE',  ( 0.000000000000000000, 82.02147376274727719, -42.76579056660780509 ) ) ;
#14521=DIRECTION ( 'NONE',  ( -1.000000000000000000, 0.000000000000000000, 0.000000000000000000 ) ) ;
#14523=CARTESIAN_POINT ( 'NONE',  ( 10.00000000000000000, 84.90234713953985590, 5.175025661884123274 ) ) ;
#14524=ORIENTED_EDGE ( 'NONE', *, *, #1781, .F. ) ;
#14526=EDGE_LOOP ( 'NONE', ( #16576, #3919, #16860, #15834 ) ) ;
#14529=DIRECTION ( 'NONE',  ( 0.000000000000000000, 0.5299192642332060110, -0.8480480961564252906 ) ) ;
#14530=DIRECTION ( 'NONE',  ( -1.000000000000000000, 0.000000000000000000, 0.000000000000000000 ) ) ;
#14531=EDGE_CURVE ( 'NONE', #18170, #4150, #10159, .T. ) ;
#14532=ORIENTED_EDGE ( 'NONE', *, *, #19778, .T. ) ;
#14534=DIRECTION ( 'NONE',  ( -1.000000000000000000, -0.000000000000000000, -0.000000000000000000 ) ) ;
#14535=DIRECTION ( 'NONE',  ( -1.000000000000000000, -0.000000000000000000, -0.000000000000000000 ) ) ;
#14537=CARTESIAN_POINT ( 'NONE',  ( 5.000000000000000000, -57.06999622551760609, -66.98518889142141575 ) ) ;
#14539=ORIENTED_EDGE ( 'NONE', *, *, #3265, .F. ) ;
#14540=LINE ( 'NONE', #21281, #1848 ) ;
#14541=AXIS2_PLACEMENT_3D ( 'NONE', #9169, #7634, #14252 ) ;
#14542=DIRECTION ( 'NONE',  ( 1.000000000000000000, -0.000000000000000000, -0.000000000000000000 ) ) ;
#14543=ORIENTED_EDGE ( 'NONE', *, *, #675, .F. ) ;
#14544=DIRECTION ( 'NONE',  ( 0.000000000000000000, 0.8660254037844398178, -0.4999999999999979461 ) ) ;
#14545=ORIENTED_EDGE ( 'NONE', *, *, #4083, .F. ) ;
#14546=AXIS2_PLACEMENT_3D ( 'NONE', #5137, #8457, #17063 ) ;
#14548=DIRECTION ( 'NONE',  ( 1.000000000000000000, -0.000000000000000000, -0.000000000000000000 ) ) ;
#14550=DIRECTION ( 'NONE',  ( 1.000000000000000000, 0.000000000000000000, 0.000000000000000000 ) ) ;
#14556=AXIS2_PLACEMENT_3D ( 'NONE', #10045, #13365, #18245 ) ;
#14557=CARTESIAN_POINT ( 'NONE',  ( 0.000000000000000000, -73.32282170386882569, 48.65967342042752364 ) ) ;
#14559=EDGE_CURVE ( 'NONE', #15964, #13385, #6998, .T. ) ;
#14561=CARTESIAN_POINT ( 'NONE',  ( 0.000000000000000000, 0.000000000000000000, 0.000000000000000000 ) ) ;
#14562=DIRECTION ( 'NONE',  ( -1.000000000000000000, 0.000000000000000000, 0.000000000000000000 ) ) ;
#14564=DIRECTION ( 'NONE',  ( 0.000000000000000000, -0.6427876096865456912, 0.7660444431189725734 ) ) ;
#14566=CYLINDRICAL_SURFACE ( 'NONE', #18594, 44.99999999999998579 ) ;
#14567=ADVANCED_FACE ( 'NONE', ( #17044 ), #1904, .F. ) ;
#14568=ORIENTED_EDGE ( 'NONE', *, *, #21733, .F. ) ;
#14571=EDGE_LOOP ( 'NONE', ( #16730, #17969, #6704, #15415 ) ) ;
#14573=AXIS2_PLACEMENT_3D ( 'NONE', #12901, #7609, #6068 ) ;
#14574=ORIENTED_EDGE ( 'NONE', *, *, #272, .T. ) ;
#14575=VECTOR ( 'NONE', #5131, 1000.000000000000000 ) ;
#14576=ORIENTED_EDGE ( 'NONE', *, *, #3947, .T. ) ;
#14577=CARTESIAN_POINT ( 'NONE',  ( 10.00000000000000000, 0.000000000000000000, 0.000000000000000000 ) ) ;
#14579=ORIENTED_EDGE ( 'NONE', *, *, #8246, .T. ) ;
#14580=CARTESIAN_POINT ( 'NONE',  ( 10.00000000000000000, 92.22057093985031884, 7.197311757040840696 ) ) ;
#14581=EDGE_CURVE ( 'NONE', #5619, #6428, #4168, .T. ) ;
#14586=FACE_OUTER_BOUND ( 'NONE', #10299, .T. ) ;
#14587=DIRECTION ( 'NONE',  ( 0.000000000000000000, 0.8987940462991649282, 0.4383711467890815117 ) ) ;
#14588=DIRECTION ( 'NONE',  ( -1.000000000000000000, -0.000000000000000000, -0.000000000000000000 ) ) ;
#14591=DIRECTION ( 'NONE',  ( 1.000000000000000000, 0.000000000000000000, 0.000000000000000000 ) ) ;
#14592=CIRCLE ( 'NONE', #1896, 45.00000000000000000 ) ;
#14594=CIRCLE ( 'NONE', #15648, 45.00000000000000000 ) ;
#14595=FACE_OUTER_BOUND ( 'NONE', #6870, .T. ) ;
#14596=EDGE_CURVE ( 'NONE', #1794, #16126, #9114, .T. ) ;
#14597=ORIENTED_EDGE ( 'NONE', *, *, #8112, .F. ) ;
#14598=FACE_OUTER_BOUND ( 'NONE', #963, .T. ) ;
#14599=EDGE_CURVE ( 'NONE', #18557, #3682, #10519, .T. ) ;
#14600=DIRECTION ( 'NONE',  ( 1.000000000000000000, 0.000000000000000000, 0.000000000000000000 ) ) ;
#14601=AXIS2_PLACEMENT_3D ( 'NONE', #5824, #7583, #10893 ) ;
#14602=VERTEX_POINT ( 'NONE', #9176 ) ;
#14603=CARTESIAN_POINT ( 'NONE',  ( 0.000000000000000000, 84.33453774737672859, -11.08490790852044405 ) ) ;
#14605=ORIENTED_EDGE ( 'NONE', *, *, #12702, .T. ) ;
#14607=VECTOR ( 'NONE', #8895, 1000.000000000000000 ) ;
#14609=VERTEX_POINT ( 'NONE', #9071 ) ;
#14610=ORIENTED_EDGE ( 'NONE', *, *, #10161, .F. ) ;
#14614=CARTESIAN_POINT ( 'NONE',  ( 0.000000000000000000, -61.33825423015638734, -69.23910433416007493 ) ) ;
#14616=DIRECTION ( 'NONE',  ( 0.000000000000000000, 0.9271838545667857590, 0.3746065934159159561 ) ) ;
#14617=LINE ( 'NONE', #4459, #17469 ) ;
#14618=CARTESIAN_POINT ( 'NONE',  ( 10.00000000000000000, 81.97107881582195432, 22.71412948308594437 ) ) ;
#14620=DIRECTION ( 'NONE',  ( -1.000000000000000000, -0.000000000000000000, -0.000000000000000000 ) ) ;
#14623=DIRECTION ( 'NONE',  ( -1.000000000000000000, 0.000000000000000000, 0.000000000000000000 ) ) ;
#14624=EDGE_CURVE ( 'NONE', #20437, #21516, #14774, .T. ) ;
#14627=EDGE_CURVE ( 'NONE', #8596, #13627, #6318, .T. ) ;
#14629=CARTESIAN_POINT ( 'NONE',  ( 10.00000000000000000, 68.36541360927260769, -50.60987712331631627 ) ) ;
#14632=ORIENTED_EDGE ( 'NONE', *, *, #1620, .F. ) ;
#14636=ORIENTED_EDGE ( 'NONE', *, *, #20676, .F. ) ;
#14638=ORIENTED_EDGE ( 'NONE', *, *, #20256, .T. ) ;
#14640=CARTESIAN_POINT ( 'NONE',  ( 10.00000000000000000, -85.05652083079338865, -0.7600687895868707411 ) ) ;
#14641=ORIENTED_EDGE ( 'NONE', *, *, #12275, .F. ) ;
#14642=AXIS2_PLACEMENT_3D ( 'NONE', #1517, #6835, #13559 ) ;
#14646=CARTESIAN_POINT ( 'NONE',  ( 0.000000000000000000, 0.000000000000000000, 0.000000000000000000 ) ) ;
#14647=CIRCLE ( 'NONE', #12522, 44.99999999999999289 ) ;
#14648=CARTESIAN_POINT ( 'NONE',  ( 10.00000000000000000, 56.35896156215049047, -73.34918167666251065 ) ) ;
#14650=CARTESIAN_POINT ( 'NONE',  ( 10.00000000000000000, 77.39385041987100067, 35.28996114464738554 ) ) ;
#14651=DIRECTION ( 'NONE',  ( 0.000000000000000000, 2.929755203871941151E-14, -1.000000000000000000 ) ) ;
#14652=ORIENTED_EDGE ( 'NONE', *, *, #15040, .F. ) ;
#14655=AXIS2_PLACEMENT_3D ( 'NONE', #10459, #20423, #10344 ) ;
#14657=AXIS2_PLACEMENT_3D ( 'NONE', #15259, #1797, #32 ) ;
#14659=CARTESIAN_POINT ( 'NONE',  ( 0.000000000000000000, -46.07110168784768689, -74.97635353408431058 ) ) ;
#14660=CARTESIAN_POINT ( 'NONE',  ( 10.00000000000000000, 0.000000000000000000, 0.000000000000000000 ) ) ;
#14662=CARTESIAN_POINT ( 'NONE',  ( 0.000000000000000000, -81.83745710415297481, 32.35167097270122838 ) ) ;
#14663=VERTEX_POINT ( 'NONE', #20894 ) ;
#14664=ORIENTED_EDGE ( 'NONE', *, *, #4449, .F. ) ;
#14666=ORIENTED_EDGE ( 'NONE', *, *, #8700, .T. ) ;
#14667=CARTESIAN_POINT ( 'NONE',  ( 0.000000000000000000, 92.49798535263882115, 0.7467976319023850174 ) ) ;
#14668=CARTESIAN_POINT ( 'NONE',  ( 10.00000000000000000, 15.32665449651924661, 91.22241316115426457 ) ) ;
#14672=CARTESIAN_POINT ( 'NONE',  ( 10.00000000000000000, 0.000000000000000000, 0.000000000000000000 ) ) ;
#14673=CIRCLE ( 'NONE', #4093, 92.50100000000000477 ) ;
#14674=AXIS2_PLACEMENT_3D ( 'NONE', #1113, #11169, #14223 ) ;
#14675=CARTESIAN_POINT ( 'NONE',  ( 0.000000000000000000, 0.000000000000000000, 0.000000000000000000 ) ) ;
#14676=DIRECTION ( 'NONE',  ( 0.000000000000000000, -0.8987940462991711454, 0.4383711467890689661 ) ) ;
#14677=CARTESIAN_POINT ( 'NONE',  ( 0.000000000000000000, 0.000000000000000000, 0.000000000000000000 ) ) ;
#14678=CARTESIAN_POINT ( 'NONE',  ( 0.000000000000000000, 52.96496548042853192, 66.55750800669373746 ) ) ;
#14679=CARTESIAN_POINT ( 'NONE',  ( 0.000000000000000000, 25.56104204395304080, 81.12843256239672485 ) ) ;
#14680=DIRECTION ( 'NONE',  ( 0.000000000000000000, 0.000000000000000000, 1.000000000000000000 ) ) ;
#14681=ORIENTED_EDGE ( 'NONE', *, *, #12557, .T. ) ;
#14682=EDGE_CURVE ( 'NONE', #14906, #18352, #6663, .T. ) ;
#14683=CIRCLE ( 'NONE', #4452, 44.99999999999999289 ) ;
#14686=VERTEX_POINT ( 'NONE', #14152 ) ;
#14687=EDGE_LOOP ( 'NONE', ( #10592, #15479, #12913, #14921 ) ) ;
#14688=EDGE_CURVE ( 'NONE', #13148, #7101, #20765, .T. ) ;
#14689=EDGE_LOOP ( 'NONE', ( #403, #12975, #20158, #17810 ) ) ;
#14690=CARTESIAN_POINT ( 'NONE',  ( 10.00000000000000000, 60.65279801375431390, -63.75921967137554702 ) ) ;
#14691=ORIENTED_EDGE ( 'NONE', *, *, #13130, .T. ) ;
#14692=DIRECTION ( 'NONE',  ( -1.000000000000000000, 0.000000000000000000, 0.000000000000000000 ) ) ;
#14694=DIRECTION ( 'NONE',  ( 0.000000000000000000, 0.000000000000000000, -1.000000000000000000 ) ) ;
#14695=AXIS2_PLACEMENT_3D ( 'NONE', #15515, #10428, #17067 ) ;
#14696=DIRECTION ( 'NONE',  ( -1.000000000000000000, -0.000000000000000000, -0.000000000000000000 ) ) ;
#14698=CARTESIAN_POINT ( 'NONE',  ( 10.00000000000000000, 8.925965667928872804, 92.06933331948788179 ) ) ;
#14700=DIRECTION ( 'NONE',  ( -1.000000000000000000, -0.000000000000000000, -0.000000000000000000 ) ) ;
#14702=ORIENTED_EDGE ( 'NONE', *, *, #6891, .T. ) ;
#14703=LINE ( 'NONE', #16028, #13246 ) ;
#14704=EDGE_CURVE ( 'NONE', #239, #21406, #17486, .T. ) ;
#14706=ORIENTED_EDGE ( 'NONE', *, *, #6496, .F. ) ;
#14707=EDGE_LOOP ( 'NONE', ( #21085, #6773, #4113, #15043 ) ) ;
#14708=CARTESIAN_POINT ( 'NONE',  ( 10.00000000000000000, 69.25892805976580746, -49.38005998797770246 ) ) ;
#14709=AXIS2_PLACEMENT_3D ( 'NONE', #441, #7180, #16916 ) ;
#14710=EDGE_CURVE ( 'NONE', #7036, #20191, #15111, .T. ) ;
#14711=CARTESIAN_POINT ( 'NONE',  ( -10.00000000000000000, 0.000000000000000000, 0.000000000000000000 ) ) ;
#14713=AXIS2_PLACEMENT_3D ( 'NONE', #6491, #8356, #10001 ) ;
#14714=LINE ( 'NONE', #21458, #4535 ) ;
#14715=VERTEX_POINT ( 'NONE', #10840 ) ;
#14716=VERTEX_POINT ( 'NONE', #17592 ) ;
#14717=AXIS2_PLACEMENT_3D ( 'NONE', #8931, #21094, #15676 ) ;
#14721=ORIENTED_EDGE ( 'NONE', *, *, #18243, .T. ) ;
#14726=DIRECTION ( 'NONE',  ( 0.000000000000000000, -6.982962677686266711E-15, 1.000000000000000000 ) ) ;
#14729=LINE ( 'NONE', #18055, #19895 ) ;
#14732=DIRECTION ( 'NONE',  ( 0.000000000000000000, 0.000000000000000000, 1.000000000000000000 ) ) ;
#14735=VERTEX_POINT ( 'NONE', #2544 ) ;
#14737=EDGE_CURVE ( 'NONE', #10208, #17938, #16540, .T. ) ;
#14740=CYLINDRICAL_SURFACE ( 'NONE', #13698, 45.00000000000000000 ) ;
#14741=ADVANCED_FACE ( 'NONE', ( #19676 ), #1339, .F. ) ;
#14743=DIRECTION ( 'NONE',  ( 1.000000000000000000, -0.000000000000000000, -0.000000000000000000 ) ) ;
#14744=ORIENTED_EDGE ( 'NONE', *, *, #13881, .F. ) ;
#14745=AXIS2_PLACEMENT_3D ( 'NONE', #10068, #16817, #1685 ) ;
#14746=VECTOR ( 'NONE', #4014, 1000.000000000000000 ) ;
#14748=ORIENTED_EDGE ( 'NONE', *, *, #21201, .F. ) ;
#14749=CIRCLE ( 'NONE', #5572, 92.50100000000001899 ) ;
#14750=ORIENTED_EDGE ( 'NONE', *, *, #17489, .T. ) ;
#14751=VECTOR ( 'NONE', #12224, 1000.000000000000000 ) ;
#14752=FACE_OUTER_BOUND ( 'NONE', #14707, .T. ) ;
#14753=CARTESIAN_POINT ( 'NONE',  ( 10.00000000000000000, 15.32665449652044920, -91.22241316115403720 ) ) ;
#14754=CIRCLE ( 'NONE', #15806, 44.99999999999999289 ) ;
#14755=VERTEX_POINT ( 'NONE', #2880 ) ;
#14758=DIRECTION ( 'NONE',  ( 1.000000000000000000, 0.000000000000000000, 0.000000000000000000 ) ) ;
#14759=CARTESIAN_POINT ( 'NONE',  ( 10.00000000000000000, -86.66425444033897918, -32.33793443156484670 ) ) ;
#14762=AXIS2_PLACEMENT_3D ( 'NONE', #776, #5878, #10835 ) ;
#14763=CYLINDRICAL_SURFACE ( 'NONE', #9276, 44.99999999999999289 ) ;
#14764=DIRECTION ( 'NONE',  ( -1.000000000000000000, 0.000000000000000000, 0.000000000000000000 ) ) ;
#14767=ADVANCED_FACE ( 'NONE', ( #18254 ), #9716, .F. ) ;
#14769=AXIS2_PLACEMENT_3D ( 'NONE', #3880, #3654, #10614 ) ;
#14771=VECTOR ( 'NONE', #15559, 1000.000000000000000 ) ;
#14772=ORIENTED_EDGE ( 'NONE', *, *, #5385, .T. ) ;
#14773=CIRCLE ( 'NONE', #17251, 88.00000000000000000 ) ;
#14774=CIRCLE ( 'NONE', #11234, 88.00000000000000000 ) ;
#14775=DIRECTION ( 'NONE',  ( -1.000000000000000000, 0.000000000000000000, 0.000000000000000000 ) ) ;
#14777=EDGE_CURVE ( 'NONE', #845, #11182, #15476, .T. ) ;
#14779=CARTESIAN_POINT ( 'NONE',  ( 0.000000000000000000, 0.000000000000000000, 0.000000000000000000 ) ) ;
#14780=ORIENTED_EDGE ( 'NONE', *, *, #15427, .T. ) ;
#14782=ORIENTED_EDGE ( 'NONE', *, *, #10115, .T. ) ;
#14783=ORIENTED_EDGE ( 'NONE', *, *, #9584, .T. ) ;
#14784=DIRECTION ( 'NONE',  ( 0.000000000000000000, 0.000000000000000000, 1.000000000000000000 ) ) ;
#14788=CARTESIAN_POINT ( 'NONE',  ( 0.000000000000000000, 0.000000000000000000, 0.000000000000000000 ) ) ;
#14789=DIRECTION ( 'NONE',  ( 1.000000000000000000, 0.000000000000000000, 0.000000000000000000 ) ) ;
#14790=CIRCLE ( 'NONE', #5262, 88.00000000000000000 ) ;
#14791=VECTOR ( 'NONE', #7706, 1000.000000000000000 ) ;
#14792=AXIS2_PLACEMENT_3D ( 'NONE', #17676, #7617, #11028 ) ;
#14793=SURFACE_STYLE_USAGE ( .BOTH. , #1312 ) ;
#14794=DIRECTION ( 'NONE',  ( 0.000000000000000000, 0.5877852522924689183, 0.8090169943749504489 ) ) ;
#14795=FACE_OUTER_BOUND ( 'NONE', #15589, .T. ) ;
#14796=EDGE_CURVE ( 'NONE', #12932, #21704, #8773, .T. ) ;
#14797=CARTESIAN_POINT ( 'NONE',  ( 0.000000000000000000, 0.000000000000000000, 0.000000000000000000 ) ) ;
#14798=CARTESIAN_POINT ( 'NONE',  ( 10.00000000000000000, 0.000000000000000000, 0.000000000000000000 ) ) ;
#14800=FACE_OUTER_BOUND ( 'NONE', #5731, .T. ) ;
#14801=VECTOR ( 'NONE', #913, 1000.000000000000000 ) ;
#14804=AXIS2_PLACEMENT_3D ( 'NONE', #15324, #11911, #16995 ) ;
#14806=VERTEX_POINT ( 'NONE', #4546 ) ;
#14808=DIRECTION ( 'NONE',  ( 1.000000000000000000, 0.000000000000000000, 0.000000000000000000 ) ) ;
#14809=ORIENTED_EDGE ( 'NONE', *, *, #11447, .T. ) ;
#14811=DIRECTION ( 'NONE',  ( 1.000000000000000000, -0.000000000000000000, -0.000000000000000000 ) ) ;
#14812=DIRECTION ( 'NONE',  ( 0.000000000000000000, 0.6427876096865405842, -0.7660444431189771253 ) ) ;
#14817=DIRECTION ( 'NONE',  ( 1.000000000000000000, 0.000000000000000000, 0.000000000000000000 ) ) ;
#14818=ORIENTED_EDGE ( 'NONE', *, *, #6537, .T. ) ;
#14819=EDGE_CURVE ( 'NONE', #9851, #10156, #13344, .T. ) ;
#14821=ORIENTED_EDGE ( 'NONE', *, *, #18160, .F. ) ;
#14822=VERTEX_POINT ( 'NONE', #13045 ) ;
#14824=VERTEX_POINT ( 'NONE', #21658 ) ;
#14825=AXIS2_PLACEMENT_3D ( 'NONE', #8309, #15039, #11723 ) ;
#14826=CARTESIAN_POINT ( 'NONE',  ( 10.00000000000000000, 64.66851233300799606, -55.25552418572899427 ) ) ;
#14828=ORIENTED_EDGE ( 'NONE', *, *, #18657, .F. ) ;
#14829=DIRECTION ( 'NONE',  ( 0.000000000000000000, -9.772275581336014350E-15, -1.000000000000000000 ) ) ;
#14832=DIRECTION ( 'NONE',  ( 0.000000000000000000, 0.9510565162951521989, 0.3090169943749514481 ) ) ;
#14833=DIRECTION ( 'NONE',  ( -1.000000000000000000, 0.000000000000000000, 0.000000000000000000 ) ) ;
#14834=CARTESIAN_POINT ( 'NONE',  ( 10.00000000000000000, -41.89587599971600440, 77.38692120905457728 ) ) ;
#14835=ADVANCED_FACE ( 'NONE', ( #11715 ), #11284, .F. ) ;
#14836=DIRECTION ( 'NONE',  ( 0.000000000000000000, 0.000000000000000000, 1.000000000000000000 ) ) ;
#14837=CARTESIAN_POINT ( 'NONE',  ( 10.00000000000000000, 19.83954325428771881, -82.71385593638672162 ) ) ;
#14838=DIRECTION ( 'NONE',  ( -1.000000000000000000, -0.000000000000000000, -0.000000000000000000 ) ) ;
#14845=FACE_OUTER_BOUND ( 'NONE', #10958, .T. ) ;
#14846=EDGE_CURVE ( 'NONE', #12774, #19231, #5594, .T. ) ;
#14847=DIRECTION ( 'NONE',  ( 1.000000000000000000, 0.000000000000000000, 0.000000000000000000 ) ) ;
#14848=ORIENTED_EDGE ( 'NONE', *, *, #410, .T. ) ;
#14850=CARTESIAN_POINT ( 'NONE',  ( 5.000000000000000000, -68.93609746931124960, -54.69748134696530428 ) ) ;
#14854=DIRECTION ( 'NONE',  ( 0.000000000000000000, 0.9993908270190956511, 0.03489949670250451497 ) ) ;
#14855=VERTEX_POINT ( 'NONE', #11382 ) ;
#14856=ORIENTED_EDGE ( 'NONE', *, *, #7042, .F. ) ;
#14857=AXIS2_PLACEMENT_3D ( 'NONE', #3277, #297, #6611 ) ;
#14858=CARTESIAN_POINT ( 'NONE',  ( 0.000000000000000000, 0.000000000000000000, 0.000000000000000000 ) ) ;
#14859=DIRECTION ( 'NONE',  ( 1.000000000000000000, 0.000000000000000000, 0.000000000000000000 ) ) ;
#14860=ORIENTED_EDGE ( 'NONE', *, *, #20918, .T. ) ;
#14861=EDGE_CURVE ( 'NONE', #1477, #4091, #6435, .T. ) ;
#14863=CARTESIAN_POINT ( 'NONE',  ( 10.00000000000000000, -74.39348546125087580, 54.97312363261389834 ) ) ;
#14864=EDGE_CURVE ( 'NONE', #3479, #750, #14416, .T. ) ;
#14865=CARTESIAN_POINT ( 'NONE',  ( 10.00000000000000000, 23.10190250628953379, -89.56973317806578905 ) ) ;
#14866=EDGE_CURVE ( 'NONE', #3599, #17431, #4901, .T. ) ;
#14867=CARTESIAN_POINT ( 'NONE',  ( 0.000000000000000000, -84.80486432185219314, 36.94008646920367056 ) ) ;
#14868=CARTESIAN_POINT ( 'NONE',  ( 0.000000000000000000, 75.27139873020959726, -53.76477968147737840 ) ) ;
#14869=DIRECTION ( 'NONE',  ( -1.000000000000000000, -0.000000000000000000, 0.000000000000000000 ) ) ;
#14870=EDGE_CURVE ( 'NONE', #11727, #14824, #21476, .T. ) ;
#14872=CARTESIAN_POINT ( 'NONE',  ( 10.00000000000000000, -84.33453774737651543, -11.08490790852216534 ) ) ;
#14873=DIRECTION ( 'NONE',  ( 1.000000000000000000, 0.000000000000000000, 0.000000000000000000 ) ) ;
#14874=VERTEX_POINT ( 'NONE', #20125 ) ;
#14877=EDGE_CURVE ( 'NONE', #9931, #20811, #4981, .T. ) ;
#14879=FACE_OUTER_BOUND ( 'NONE', #7601, .T. ) ;
#14881=ORIENTED_EDGE ( 'NONE', *, *, #18160, .T. ) ;
#14883=ADVANCED_FACE ( 'NONE', ( #9832 ), #16584, .F. ) ;
#14884=VERTEX_POINT ( 'NONE', #18899 ) ;
#14886=LINE ( 'NONE', #19525, #11107 ) ;
#14888=ORIENTED_EDGE ( 'NONE', *, *, #9306, .T. ) ;
#14889=DIRECTION ( 'NONE',  ( -1.000000000000000000, -0.000000000000000000, -0.000000000000000000 ) ) ;
#14890=DIRECTION ( 'NONE',  ( 1.000000000000000000, 0.000000000000000000, 0.000000000000000000 ) ) ;
#14894=EDGE_CURVE ( 'NONE', #536, #6705, #1367, .T. ) ;
#14897=CARTESIAN_POINT ( 'NONE',  ( 0.000000000000000000, 24.89070495400735794, 84.40647372620510680 ) ) ;
#14898=AXIS2_PLACEMENT_3D ( 'NONE', #6856, #9934, #13139 ) ;
#14901=EDGE_CURVE ( 'NONE', #16742, #15174, #4186, .T. ) ;
#14902=VERTEX_POINT ( 'NONE', #14 ) ;
#14904=EDGE_CURVE ( 'NONE', #20733, #18352, #19357, .T. ) ;
#14905=ORIENTED_EDGE ( 'NONE', *, *, #3390, .F. ) ;
#14906=VERTEX_POINT ( 'NONE', #7087 ) ;
#14908=ADVANCED_FACE ( 'NONE', ( #13913 ), #13706, .F. ) ;
#14909=ORIENTED_EDGE ( 'NONE', *, *, #19078, .F. ) ;
#14910=DIRECTION ( 'NONE',  ( 0.000000000000000000, 0.000000000000000000, 1.000000000000000000 ) ) ;
#14911=EDGE_LOOP ( 'NONE', ( #11008, #15655, #19460, #18519 ) ) ;
#14914=AXIS2_PLACEMENT_3D ( 'NONE', #18442, #3294, #10022 ) ;
#14916=CARTESIAN_POINT ( 'NONE',  ( -10.00000000000000000, 0.000000000000000000, 0.000000000000000000 ) ) ;
#14918=CARTESIAN_POINT ( 'NONE',  ( 10.00000000000000000, 83.03980459022480431, -18.42770452393272862 ) ) ;
#14919=DIRECTION ( 'NONE',  ( -1.000000000000000000, -0.000000000000000000, -0.000000000000000000 ) ) ;
#14920=CIRCLE ( 'NONE', #15972, 92.50099999999999056 ) ;
#14921=ORIENTED_EDGE ( 'NONE', *, *, #12404, .T. ) ;
#14923=AXIS2_PLACEMENT_3D ( 'NONE', #15570, #19108, #14234 ) ;
#14925=ORIENTED_EDGE ( 'NONE', *, *, #272, .F. ) ;
#14926=CIRCLE ( 'NONE', #17410, 88.00000000000000000 ) ;
#14927=VERTEX_POINT ( 'NONE', #20455 ) ;
#14930=CARTESIAN_POINT ( 'NONE',  ( 0.000000000000000000, 83.03980459022454852, 18.42770452393382641 ) ) ;
#14931=ORIENTED_EDGE ( 'NONE', *, *, #17427, .T. ) ;
#14932=EDGE_LOOP ( 'NONE', ( #10585, #2864, #10875, #10286 ) ) ;
#14934=CIRCLE ( 'NONE', #10688, 44.99999999999999289 ) ;
#14935=EDGE_LOOP ( 'NONE', ( #10796, #13840, #4923, #1125 ) ) ;
#14936=LINE ( 'NONE', #1985, #5801 ) ;
#14938=CIRCLE ( 'NONE', #5424, 44.99999999999999289 ) ;
#14939=FACE_OUTER_BOUND ( 'NONE', #7816, .T. ) ;
#14940=DIRECTION ( 'NONE',  ( 1.000000000000000000, 0.000000000000000000, 0.000000000000000000 ) ) ;
#14941=CIRCLE ( 'NONE', #17064, 44.99999999999999289 ) ;
#14943=DIRECTION ( 'NONE',  ( 0.000000000000000000, 0.000000000000000000, 1.000000000000000000 ) ) ;
#14944=DIRECTION ( 'NONE',  ( 0.000000000000000000, 0.7431448254773953543, -0.6691306063588569053 ) ) ;
#14947=DIRECTION ( 'NONE',  ( -1.000000000000000000, 0.000000000000000000, -0.000000000000000000 ) ) ;
#14949=ORIENTED_EDGE ( 'NONE', *, *, #5560, .T. ) ;
#14950=ADVANCED_FACE ( 'NONE', ( #6761 ), #1669, .F. ) ;
#14952=VERTEX_POINT ( 'NONE', #8410 ) ;
#14957=VERTEX_POINT ( 'NONE', #5419 ) ;
#14958=DIRECTION ( 'NONE',  ( 0.000000000000000000, 0.000000000000000000, 1.000000000000000000 ) ) ;
#14959=CARTESIAN_POINT ( 'NONE',  ( 0.000000000000000000, 0.000000000000000000, 0.000000000000000000 ) ) ;
#14961=VERTEX_POINT ( 'NONE', #1777 ) ;
#14962=AXIS2_PLACEMENT_3D ( 'NONE', #277, #5148, #2146 ) ;
#14967=LINE ( 'NONE', #18308, #4704 ) ;
#14968=DIRECTION ( 'NONE',  ( -1.000000000000000000, -0.000000000000000000, 0.000000000000000000 ) ) ;
#14972=CIRCLE ( 'NONE', #17462, 88.00000000000000000 ) ;
#14973=CARTESIAN_POINT ( 'NONE',  ( 5.000000000000002665, -86.77540292929711541, 14.62974526292689426 ) ) ;
#14975=ORIENTED_EDGE ( 'NONE', *, *, #12179, .T. ) ;
#14976=DIRECTION ( 'NONE',  ( -1.000000000000000000, -0.000000000000000000, -0.000000000000000000 ) ) ;
#14978=AXIS2_PLACEMENT_3D ( 'NONE', #4132, #17622, #2572 ) ;
#14980=EDGE_CURVE ( 'NONE', #12538, #13997, #10553, .T. ) ;
#14981=AXIS2_PLACEMENT_3D ( 'NONE', #9267, #459, #16015 ) ;
#14982=ADVANCED_FACE ( 'NONE', ( #15136 ), #3434, .F. ) ;
#14984=LINE ( 'NONE', #10118, #20093 ) ;
#14988=VECTOR ( 'NONE', #915, 1000.000000000000000 ) ;
#14990=ORIENTED_EDGE ( 'NONE', *, *, #4508, .T. ) ;
#14991=ORIENTED_EDGE ( 'NONE', *, *, #18244, .F. ) ;
#14992=FACE_OUTER_BOUND ( 'NONE', #2839, .T. ) ;
#14994=FACE_OUTER_BOUND ( 'NONE', #13777, .T. ) ;
#14996=CARTESIAN_POINT ( 'NONE',  ( 10.00000000000000000, 83.03980459022480431, -18.42770452393272862 ) ) ;
#14997=CARTESIAN_POINT ( 'NONE',  ( 0.000000000000000000, 40.72878876293147954, 78.00747250042462611 ) ) ;
#14999=ADVANCED_FACE ( 'NONE', ( #13590 ), #20346, .F. ) ;
#15000=CARTESIAN_POINT ( 'NONE',  ( 10.00000000000000000, -91.70173545986510533, -12.13370160540135423 ) ) ;
#15002=FACE_OUTER_BOUND ( 'NONE', #15062, .T. ) ;
#15005=CARTESIAN_POINT ( 'NONE',  ( 10.00000000000000000, -65.83713140174766920, 58.39068529131174756 ) ) ;
#15006=VECTOR ( 'NONE', #18481, 1000.000000000000000 ) ;
#15007=CARTESIAN_POINT ( 'NONE',  ( 0.000000000000000000, 56.35896156215049047, -73.34918167666251065 ) ) ;
#15012=ORIENTED_EDGE ( 'NONE', *, *, #10807, .T. ) ;
#15013=ORIENTED_EDGE ( 'NONE', *, *, #1508, .F. ) ;
#15016=CIRCLE ( 'NONE', #5496, 45.00000000000000000 ) ;
#15017=CIRCLE ( 'NONE', #12884, 45.00000000000000000 ) ;
#15018=CIRCLE ( 'NONE', #15731, 44.99999999999999289 ) ;
#15022=ORIENTED_EDGE ( 'NONE', *, *, #6650, .T. ) ;
#15023=DIRECTION ( 'NONE',  ( 0.000000000000000000, 0.000000000000000000, 1.000000000000000000 ) ) ;
#15024=LINE ( 'NONE', #20002, #13147 ) ;
#15026=DIRECTION ( 'NONE',  ( 1.000000000000000000, 0.000000000000000000, 0.000000000000000000 ) ) ;
#15027=CARTESIAN_POINT ( 'NONE',  ( 0.000000000000000000, 60.65279801375431390, -63.75921967137554702 ) ) ;
#15028=ADVANCED_FACE ( 'NONE', ( #19009 ), #19112, .F. ) ;
#15029=CARTESIAN_POINT ( 'NONE',  ( 0.000000000000000000, -91.49386717542212466, -13.61276130277086693 ) ) ;
#15031=AXIS2_PLACEMENT_3D ( 'NONE', #18256, #11943, #3545 ) ;
#15032=EDGE_CURVE ( 'NONE', #21406, #510, #18337, .T. ) ;
#15033=ORIENTED_EDGE ( 'NONE', *, *, #15427, .F. ) ;
#15035=EDGE_CURVE ( 'NONE', #1766, #21050, #21148, .T. ) ;
#15039=DIRECTION ( 'NONE',  ( 1.000000000000000000, 0.000000000000000000, 0.000000000000000000 ) ) ;
#15040=EDGE_CURVE ( 'NONE', #14952, #14101, #20096, .T. ) ;
#15042=CARTESIAN_POINT ( 'NONE',  ( 10.00000000000000000, -89.12061559554314272, -24.77803214283632727 ) ) ;
#15043=ORIENTED_EDGE ( 'NONE', *, *, #15411, .T. ) ;
#15044=VERTEX_POINT ( 'NONE', #2199 ) ;
#15046=DIRECTION ( 'NONE',  ( 0.000000000000000000, -0.9848077530122062440, -0.1736481776669404897 ) ) ;
#15048=AXIS2_PLACEMENT_3D ( 'NONE', #16235, #14240, #11029 ) ;
#15050=AXIS2_PLACEMENT_3D ( 'NONE', #13612, #11964, #10399 ) ;
#15051=DIRECTION ( 'NONE',  ( -1.000000000000000000, 0.000000000000000000, 0.000000000000000000 ) ) ;
#15052=FACE_OUTER_BOUND ( 'NONE', #15595, .T. ) ;
#15053=FACE_OUTER_BOUND ( 'NONE', #18700, .T. ) ;
#15054=CARTESIAN_POINT ( 'NONE',  ( 0.000000000000000000, -51.76708072107842185, -67.49339815138544907 ) ) ;
#15055=DIRECTION ( 'NONE',  ( -1.000000000000000000, 0.000000000000000000, 0.000000000000000000 ) ) ;
#15056=CYLINDRICAL_SURFACE ( 'NONE', #18986, 45.00000000000000000 ) ;
#15057=VERTEX_POINT ( 'NONE', #10703 ) ;
#15058=AXIS2_PLACEMENT_3D ( 'NONE', #17920, #7641, #2543 ) ;
#15059=VECTOR ( 'NONE', #110, 1000.000000000000000 ) ;
#15061=CARTESIAN_POINT ( 'NONE',  ( 10.00000000000000000, -5.479102470011078196, 87.82926298292112222 ) ) ;
#15062=EDGE_LOOP ( 'NONE', ( #19610, #11881, #3066, #7838 ) ) ;
#15063=DIRECTION ( 'NONE',  ( 0.000000000000000000, 0.000000000000000000, -1.000000000000000000 ) ) ;
#15065=EDGE_LOOP ( 'NONE', ( #11812, #20606, #12616, #11680 ) ) ;
#15071=EDGE_LOOP ( 'NONE', ( #2949, #7221, #8005, #13404 ) ) ;
#15072=CARTESIAN_POINT ( 'NONE',  ( 0.000000000000000000, 72.58367602204188529, 49.75550195834890843 ) ) ;
#15074=CARTESIAN_POINT ( 'NONE',  ( 0.000000000000000000, 91.49386717542222414, 13.61276130277023810 ) ) ;
#15076=AXIS2_PLACEMENT_3D ( 'NONE', #12116, #9304, #14288 ) ;
#15081=ORIENTED_EDGE ( 'NONE', *, *, #11271, .F. ) ;
#15082=DIRECTION ( 'NONE',  ( -1.000000000000000000, 0.000000000000000000, -0.000000000000000000 ) ) ;
#15083=DIRECTION ( 'NONE',  ( -1.000000000000000000, -0.000000000000000000, -0.000000000000000000 ) ) ;
#15086=DIRECTION ( 'NONE',  ( -1.000000000000000000, 0.000000000000000000, 0.000000000000000000 ) ) ;
#15088=CIRCLE ( 'NONE', #9093, 44.99999999999999289 ) ;
#15089=CARTESIAN_POINT ( 'NONE',  ( 5.000000000000002665, -23.62010150527165919, -84.77081340225927875 ) ) ;
#15090=AXIS2_PLACEMENT_3D ( 'NONE', #7646, #19038, #17813 ) ;
#15092=FACE_OUTER_BOUND ( 'NONE', #2298, .T. ) ;
#15094=EDGE_LOOP ( 'NONE', ( #7843, #12025, #14330, #19395 ) ) ;
#15095=ORIENTED_EDGE ( 'NONE', *, *, #10313, .T. ) ;
#15096=VERTEX_POINT ( 'NONE', #19432 ) ;
#15098=CARTESIAN_POINT ( 'NONE',  ( 0.000000000000000000, -56.35896156214896280, -73.34918167666369015 ) ) ;
#15100=CARTESIAN_POINT ( 'NONE',  ( 0.000000000000000000, -68.36541360927220978, 50.60987712331682076 ) ) ;
#15103=CARTESIAN_POINT ( 'NONE',  ( 10.00000000000000000, 74.74361964203228581, 40.60271866773572214 ) ) ;
#15104=CYLINDRICAL_SURFACE ( 'NONE', #5072, 44.99999999999999289 ) ;
#15105=AXIS2_PLACEMENT_3D ( 'NONE', #21111, #11158, #16011 ) ;
#15106=EDGE_CURVE ( 'NONE', #6477, #17060, #8935, .T. ) ;
#15107=CIRCLE ( 'NONE', #7722, 88.00000000000000000 ) ;
#15108=DIRECTION ( 'NONE',  ( -1.000000000000000000, 0.000000000000000000, -0.000000000000000000 ) ) ;
#15109=CARTESIAN_POINT ( 'NONE',  ( 10.00000000000000000, 0.000000000000000000, 0.000000000000000000 ) ) ;
#15111=CIRCLE ( 'NONE', #998, 92.50100000000000477 ) ;
#15112=CARTESIAN_POINT ( 'NONE',  ( 0.000000000000000000, 0.000000000000000000, 0.000000000000000000 ) ) ;
#15115=ORIENTED_EDGE ( 'NONE', *, *, #10407, .F. ) ;
#15117=VERTEX_POINT ( 'NONE', #17459 ) ;
#15118=CARTESIAN_POINT ( 'NONE',  ( 10.00000000000000000, 81.55207211302078463, -24.17537951050094236 ) ) ;
#15120=EDGE_CURVE ( 'NONE', #14060, #20435, #15845, .T. ) ;
#15121=AXIS2_PLACEMENT_3D ( 'NONE', #5404, #18681, #13804 ) ;
#15124=AXIS2_PLACEMENT_3D ( 'NONE', #8782, #17397, #20715 ) ;
#15126=ADVANCED_FACE ( 'NONE', ( #15792 ), #14463, .F. ) ;
#15127=DIRECTION ( 'NONE',  ( -1.000000000000000000, 0.000000000000000000, 0.000000000000000000 ) ) ;
#15130=CARTESIAN_POINT ( 'NONE',  ( 5.000000000000002665, -11.59241532900687233, 87.23311244498734141 ) ) ;
#15131=EDGE_CURVE ( 'NONE', #12455, #14957, #21492, .T. ) ;
#15132=CARTESIAN_POINT ( 'NONE',  ( 10.00000000000000000, 3.728035544477412255, -84.97818067823766341 ) ) ;
#15133=EDGE_CURVE ( 'NONE', #4328, #18178, #2423, .T. ) ;
#15134=EDGE_CURVE ( 'NONE', #16786, #52, #19719, .T. ) ;
#15135=CARTESIAN_POINT ( 'NONE',  ( 0.000000000000000000, -31.15801000616886896, 79.14775961996379294 ) ) ;
#15136=FACE_OUTER_BOUND ( 'NONE', #3677, .T. ) ;
#15137=CIRCLE ( 'NONE', #20789, 92.50100000000000477 ) ;
#15138=ADVANCED_FACE ( 'NONE', ( #15903 ), #14024, .F. ) ;
#15140=VERTEX_POINT ( 'NONE', #19327 ) ;
#15142=DIRECTION ( 'NONE',  ( 0.000000000000000000, 0.1391731009600591373, 0.9902680687415712502 ) ) ;
#15144=ORIENTED_EDGE ( 'NONE', *, *, #21302, .F. ) ;
#15145=ADVANCED_FACE ( 'NONE', ( #10926 ), #4293, .F. ) ;
#15146=FACE_OUTER_BOUND ( 'NONE', #17678, .T. ) ;
#15147=EDGE_LOOP ( 'NONE', ( #5621, #1021, #20696, #15196 ) ) ;
#15148=CARTESIAN_POINT ( 'NONE',  ( 10.00000000000000000, -61.33825423015729683, 69.23910433415923649 ) ) ;
#15149=VERTEX_POINT ( 'NONE', #15005 ) ;
#15150=VERTEX_POINT ( 'NONE', #21634 ) ;
#15152=CIRCLE ( 'NONE', #11277, 88.00000000000000000 ) ;
#15155=AXIS2_PLACEMENT_3D ( 'NONE', #475, #693, #2132 ) ;
#15156=VECTOR ( 'NONE', #416, 1000.000000000000000 ) ;
#15158=EDGE_CURVE ( 'NONE', #20507, #12373, #6685, .T. ) ;
#15159=CYLINDRICAL_SURFACE ( 'NONE', #2647, 92.50100000000000477 ) ;
#15160=FACE_OUTER_BOUND ( 'NONE', #17540, .T. ) ;
#15163=DIRECTION ( 'NONE',  ( 1.000000000000000000, 0.000000000000000000, 0.000000000000000000 ) ) ;
#15164=DIRECTION ( 'NONE',  ( -1.000000000000000000, 0.000000000000000000, 0.000000000000000000 ) ) ;
#15170=DIRECTION ( 'NONE',  ( 0.000000000000000000, 0.2079116908177532363, 0.9781476007338069101 ) ) ;
#15173=EDGE_CURVE ( 'NONE', #14408, #6716, #19017, .T. ) ;
#15174=VERTEX_POINT ( 'NONE', #11475 ) ;
#15176=ORIENTED_EDGE ( 'NONE', *, *, #12846, .T. ) ;
#15177=DIRECTION ( 'NONE',  ( -1.000000000000000000, -0.000000000000000000, -0.000000000000000000 ) ) ;
#15178=ORIENTED_EDGE ( 'NONE', *, *, #182, .T. ) ;
#15179=ORIENTED_EDGE ( 'NONE', *, *, #15946, .T. ) ;
#15180=DIRECTION ( 'NONE',  ( 0.000000000000000000, 0.000000000000000000, 1.000000000000000000 ) ) ;
#15181=DIRECTION ( 'NONE',  ( 0.000000000000000000, 0.1391731009600591928, 0.9902680687415711391 ) ) ;
#15184=DIRECTION ( 'NONE',  ( -1.000000000000000000, 0.000000000000000000, 0.000000000000000000 ) ) ;
#15189=CARTESIAN_POINT ( 'NONE',  ( 0.000000000000000000, -23.10190250628774322, -89.56973317806621537 ) ) ;
#15190=CARTESIAN_POINT ( 'NONE',  ( 10.00000000000000000, 46.07110168784820559, 74.97635353408399794 ) ) ;
#15191=VERTEX_POINT ( 'NONE', #3079 ) ;
#15192=DIRECTION ( 'NONE',  ( 1.000000000000000000, -0.000000000000000000, -0.000000000000000000 ) ) ;
#15195=CYLINDRICAL_SURFACE ( 'NONE', #9429, 92.50100000000000477 ) ;
#15196=ORIENTED_EDGE ( 'NONE', *, *, #6086, .F. ) ;
#15199=CARTESIAN_POINT ( 'NONE',  ( 0.000000000000000000, -78.83848282823942100, 48.38314403117473006 ) ) ;
#15200=ADVANCED_FACE ( 'NONE', ( #19656 ), #13123, .F. ) ;
#15201=ORIENTED_EDGE ( 'NONE', *, *, #16107, .F. ) ;
#15204=EDGE_LOOP ( 'NONE', ( #13550, #2323, #124, #5673 ) ) ;
#15207=ORIENTED_EDGE ( 'NONE', *, *, #11483, .F. ) ;
#15208=CARTESIAN_POINT ( 'NONE',  ( 10.00000000000000000, -57.53593069156421791, 72.42963261300944566 ) ) ;
#15211=DIRECTION ( 'NONE',  ( 0.000000000000000000, 0.000000000000000000, -1.000000000000000000 ) ) ;
#15212=CARTESIAN_POINT ( 'NONE',  ( 10.00000000000000000, -21.31452625070983231, 82.34610137166113475 ) ) ;
#15213=CARTESIAN_POINT ( 'NONE',  ( 10.00000000000000000, 0.000000000000000000, 0.000000000000000000 ) ) ;
#15214=DIRECTION ( 'NONE',  ( 0.000000000000000000, 0.2756373558169998295, -0.9612616959383187831 ) ) ;
#15215=DIRECTION ( 'NONE',  ( -1.000000000000000000, -0.000000000000000000, -0.000000000000000000 ) ) ;
#15218=ORIENTED_EDGE ( 'NONE', *, *, #20504, .T. ) ;
#15219=CARTESIAN_POINT ( 'NONE',  ( 0.000000000000000000, 92.32475887865433606, -5.707354816229567973 ) ) ;
#15220=ORIENTED_EDGE ( 'NONE', *, *, #11376, .T. ) ;
#15221=LINE ( 'NONE', #6105, #5608 ) ;
#15222=ORIENTED_EDGE ( 'NONE', *, *, #21523, .F. ) ;
#15223=ORIENTED_EDGE ( 'NONE', *, *, #6689, .F. ) ;
#15224=ADVANCED_FACE ( 'NONE', ( #7830 ), #21307, .F. ) ;
#15227=CARTESIAN_POINT ( 'NONE',  ( 0.000000000000000000, -79.66702613806795341, 29.80527447819410369 ) ) ;
#15228=ORIENTED_EDGE ( 'NONE', *, *, #2748, .F. ) ;
#15229=CARTESIAN_POINT ( 'NONE',  ( 0.000000000000000000, 86.77540292929722909, -14.62974526292624944 ) ) ;
#15234=CARTESIAN_POINT ( 'NONE',  ( 10.00000000000000000, -67.05625154133495869, 63.71729851637790176 ) ) ;
#15235=DIRECTION ( 'NONE',  ( 0.000000000000000000, 0.9945218953682736229, -0.1045284632676503761 ) ) ;
#15238=DIRECTION ( 'NONE',  ( -1.000000000000000000, 0.000000000000000000, 0.000000000000000000 ) ) ;
#15239=VERTEX_POINT ( 'NONE', #2862 ) ;
#15242=ORIENTED_EDGE ( 'NONE', *, *, #2584, .T. ) ;
#15245=CIRCLE ( 'NONE', #14898, 88.00000000000000000 ) ;
#15248=EDGE_CURVE ( 'NONE', #8096, #20717, #1032, .T. ) ;
#15249=CARTESIAN_POINT ( 'NONE',  ( 10.00000000000000000, 14.02138820414913845, 83.89630571862289798 ) ) ;
#15250=ORIENTED_EDGE ( 'NONE', *, *, #2325, .F. ) ;
#15255=EDGE_CURVE ( 'NONE', #10982, #21052, #16922, .T. ) ;
#15256=ORIENTED_EDGE ( 'NONE', *, *, #15867, .F. ) ;
#15257=CYLINDRICAL_SURFACE ( 'NONE', #3869, 44.99999999999999289 ) ;
#15259=CARTESIAN_POINT ( 'NONE',  ( 0.000000000000000000, 37.96946988134275358, -76.11510229470822253 ) ) ;
#15260=DIRECTION ( 'NONE',  ( -1.000000000000000000, -0.000000000000000000, -0.000000000000000000 ) ) ;
#15264=ADVANCED_FACE ( 'NONE', ( #1316 ), #2964, .F. ) ;
#15265=DIRECTION ( 'NONE',  ( -1.000000000000000000, -0.000000000000000000, 0.000000000000000000 ) ) ;
#15266=AXIS2_PLACEMENT_3D ( 'NONE', #548, #10808, #5520 ) ;
#15268=ORIENTED_EDGE ( 'NONE', *, *, #18247, .T. ) ;
#15269=CIRCLE ( 'NONE', #7514, 88.00000000000000000 ) ;
#15270=EDGE_CURVE ( 'NONE', #16155, #21814, #1048, .T. ) ;
#15271=LINE ( 'NONE', #15601, #9801 ) ;
#15273=VERTEX_POINT ( 'NONE', #8168 ) ;
#15274=CARTESIAN_POINT ( 'NONE',  ( 0.000000000000000000, 57.47876254627226444, -62.70072803846332476 ) ) ;
#15275=VERTEX_POINT ( 'NONE', #14897 ) ;
#15276=ORIENTED_EDGE ( 'NONE', *, *, #10591, .T. ) ;
#15278=DIRECTION ( 'NONE',  ( 1.000000000000000000, 0.000000000000000000, 0.000000000000000000 ) ) ;
#15279=CIRCLE ( 'NONE', #18120, 45.00000000000000711 ) ;
#15280=ADVANCED_FACE ( 'NONE', ( #20529 ), #10023, .F. ) ;
#15282=ORIENTED_EDGE ( 'NONE', *, *, #6197, .F. ) ;
#15285=AXIS2_PLACEMENT_3D ( 'NONE', #1628, #78, #10127 ) ;
#15286=VERTEX_POINT ( 'NONE', #6740 ) ;
#15287=CARTESIAN_POINT ( 'NONE',  ( 5.000000000000000000, -52.25832601289145884, 70.80301803122767978 ) ) ;
#15289=CARTESIAN_POINT ( 'NONE',  ( 10.00000000000000000, 0.000000000000000000, 0.000000000000000000 ) ) ;
#15290=LINE ( 'NONE', #13968, #1201 ) ;
#15291=CYLINDRICAL_SURFACE ( 'NONE', #11754, 88.00000000000000000 ) ;
#15292=FACE_OUTER_BOUND ( 'NONE', #17467, .T. ) ;
#15293=EDGE_CURVE ( 'NONE', #5244, #12424, #10207, .T. ) ;
#15294=AXIS2_PLACEMENT_3D ( 'NONE', #21278, #15761, #6155 ) ;
#15296=ADVANCED_FACE ( 'NONE', ( #318 ), #12121, .F. ) ;
#15297=CARTESIAN_POINT ( 'NONE',  ( 0.000000000000000000, 69.25892805976512534, 49.38005998797868301 ) ) ;
#15298=AXIS2_PLACEMENT_3D ( 'NONE', #14175, #16276, #19597 ) ;
#15299=DIRECTION ( 'NONE',  ( 0.000000000000000000, 0.000000000000000000, -1.000000000000000000 ) ) ;
#15300=ORIENTED_EDGE ( 'NONE', *, *, #2755, .T. ) ;
#15301=EDGE_CURVE ( 'NONE', #17030, #393, #2449, .T. ) ;
#15303=EDGE_CURVE ( 'NONE', #8003, #3473, #7061, .T. ) ;
#15307=CARTESIAN_POINT ( 'NONE',  ( 10.00000000000000000, 0.000000000000000000, 0.000000000000000000 ) ) ;
#15309=ORIENTED_EDGE ( 'NONE', *, *, #3911, .T. ) ;
#15310=VERTEX_POINT ( 'NONE', #18552 ) ;
#15312=DIRECTION ( 'NONE',  ( 0.000000000000000000, -8.866364432770349300E-15, -1.000000000000000000 ) ) ;
#15313=ORIENTED_EDGE ( 'NONE', *, *, #8700, .F. ) ;
#15314=DIRECTION ( 'NONE',  ( 0.000000000000000000, 0.000000000000000000, 1.000000000000000000 ) ) ;
#15315=VECTOR ( 'NONE', #623, 1000.000000000000000 ) ;
#15317=DIRECTION ( 'NONE',  ( 1.000000000000000000, 0.000000000000000000, 0.000000000000000000 ) ) ;
#15321=CARTESIAN_POINT ( 'NONE',  ( 10.00000000000000000, 33.95793648385932784, -86.04239391577952745 ) ) ;
#15322=CARTESIAN_POINT ( 'NONE',  ( 0.000000000000000000, -83.03980459022491800, 18.42770452393216374 ) ) ;
#15323=DIRECTION ( 'NONE',  ( -1.000000000000000000, -0.000000000000000000, -0.000000000000000000 ) ) ;
#15324=CARTESIAN_POINT ( 'NONE',  ( 10.00000000000000000, -61.71252885873347793, -58.53847642588656441 ) ) ;
#15326=CARTESIAN_POINT ( 'NONE',  ( 5.000000000000002665, 29.47587714451147534, -82.91666097089093057 ) ) ;
#15327=AXIS2_PLACEMENT_3D ( 'NONE', #4140, #14182, #17302 ) ;
#15328=CARTESIAN_POINT ( 'NONE',  ( 0.000000000000000000, -12.90135963484022241, -87.04915231966658951 ) ) ;
#15331=ORIENTED_EDGE ( 'NONE', *, *, #12288, .F. ) ;
#15332=FACE_OUTER_BOUND ( 'NONE', #13883, .T. ) ;
#15333=VECTOR ( 'NONE', #12459, 1000.000000000000000 ) ;
#15334=VERTEX_POINT ( 'NONE', #18763 ) ;
#15335=ORIENTED_EDGE ( 'NONE', *, *, #1052, .F. ) ;
#15336=ORIENTED_EDGE ( 'NONE', *, *, #19145, .F. ) ;
#15339=ORIENTED_EDGE ( 'NONE', *, *, #14344, .T. ) ;
#15340=DIRECTION ( 'NONE',  ( 1.000000000000000000, 0.000000000000000000, 0.000000000000000000 ) ) ;
#15343=AXIS2_PLACEMENT_3D ( 'NONE', #11112, #7474, #21174 ) ;
#15345=CARTESIAN_POINT ( 'NONE',  ( 10.00000000000000000, -90.32141448704669529, -19.96189084378313794 ) ) ;
#15347=CARTESIAN_POINT ( 'NONE',  ( 10.00000000000000000, 0.000000000000000000, 0.000000000000000000 ) ) ;
#15348=CIRCLE ( 'NONE', #2652, 92.50100000000000477 ) ;
#15349=DIRECTION ( 'NONE',  ( -1.000000000000000000, -0.000000000000000000, -0.000000000000000000 ) ) ;
#15350=DIRECTION ( 'NONE',  ( -1.000000000000000000, 0.000000000000000000, -0.000000000000000000 ) ) ;
#15351=EDGE_CURVE ( 'NONE', #4335, #7874, #1404, .T. ) ;
#15353=ORIENTED_EDGE ( 'NONE', *, *, #20131, .T. ) ;
#15355=CIRCLE ( 'NONE', #17829, 88.00000000000000000 ) ;
#15357=VECTOR ( 'NONE', #4121, 1000.000000000000000 ) ;
#15358=EDGE_CURVE ( 'NONE', #10039, #16416, #13376, .T. ) ;
#15360=ORIENTED_EDGE ( 'NONE', *, *, #936, .F. ) ;
#15361=AXIS2_PLACEMENT_3D ( 'NONE', #19346, #7521, #10945 ) ;
#15362=CARTESIAN_POINT ( 'NONE',  ( 10.00000000000000000, -23.62010150527279961, 84.77081340225898032 ) ) ;
#15364=EDGE_LOOP ( 'NONE', ( #12242, #16316, #21268, #8892 ) ) ;
#15368=CARTESIAN_POINT ( 'NONE',  ( 10.00000000000000000, 83.48638250753266732, -27.82128566055030916 ) ) ;
#15370=VECTOR ( 'NONE', #7431, 1000.000000000000000 ) ;
#15372=AXIS2_PLACEMENT_3D ( 'NONE', #7557, #2480, #9206 ) ;
#15376=FACE_OUTER_BOUND ( 'NONE', #5980, .T. ) ;
#15377=VECTOR ( 'NONE', #10913, 1000.000000000000000 ) ;
#15378=ADVANCED_FACE ( 'NONE', ( #210 ), #3732, .F. ) ;
#15380=VERTEX_POINT ( 'NONE', #20202 ) ;
#15381=DIRECTION ( 'NONE',  ( 0.000000000000000000, 0.000000000000000000, 1.000000000000000000 ) ) ;
#15382=CARTESIAN_POINT ( 'NONE',  ( 0.000000000000000000, 0.000000000000000000, 0.000000000000000000 ) ) ;
#15383=ORIENTED_EDGE ( 'NONE', *, *, #2440, .F. ) ;
#15384=CIRCLE ( 'NONE', #15031, 45.00000000000000711 ) ;
#15385=DIRECTION ( 'NONE',  ( -1.000000000000000000, -0.000000000000000000, 0.000000000000000000 ) ) ;
#15386=ORIENTED_EDGE ( 'NONE', *, *, #8900, .F. ) ;
#15389=EDGE_CURVE ( 'NONE', #8475, #20752, #3164, .T. ) ;
#15390=ORIENTED_EDGE ( 'NONE', *, *, #7215, .F. ) ;
#15391=DIRECTION ( 'NONE',  ( -1.000000000000000000, -0.000000000000000000, -0.000000000000000000 ) ) ;
#15395=DIRECTION ( 'NONE',  ( -1.000000000000000000, -0.000000000000000000, -0.000000000000000000 ) ) ;
#15396=ADVANCED_FACE ( 'NONE', ( #11803 ), #8815, .F. ) ;
#15397=DIRECTION ( 'NONE',  ( -1.000000000000000000, -0.000000000000000000, -0.000000000000000000 ) ) ;
#15399=DIRECTION ( 'NONE',  ( 0.000000000000000000, 1.773272886554069860E-14, -1.000000000000000000 ) ) ;
#15400=DIRECTION ( 'NONE',  ( -1.000000000000000000, 0.000000000000000000, 0.000000000000000000 ) ) ;
#15401=DIRECTION ( 'NONE',  ( 0.000000000000000000, -1.063963731932441790E-14, -1.000000000000000000 ) ) ;
#15402=DIRECTION ( 'NONE',  ( 0.000000000000000000, -0.5299192642331943537, -0.8480480961564326181 ) ) ;
#15403=CIRCLE ( 'NONE', #8714, 88.00000000000000000 ) ;
#15404=ADVANCED_FACE ( 'NONE', ( #4961 ), #10138, .F. ) ;
#15406=CIRCLE ( 'NONE', #17188, 45.00000000000000000 ) ;
#15407=EDGE_CURVE ( 'NONE', #6576, #19966, #8103, .T. ) ;
#15408=ORIENTED_EDGE ( 'NONE', *, *, #21481, .F. ) ;
#15411=EDGE_CURVE ( 'NONE', #13148, #8199, #14452, .T. ) ;
#15413=EDGE_LOOP ( 'NONE', ( #12982, #4034, #1831, #236 ) ) ;
#15414=CARTESIAN_POINT ( 'NONE',  ( 10.00000000000000000, 74.39348546125053474, 54.97312363261438151 ) ) ;
#15415=ORIENTED_EDGE ( 'NONE', *, *, #10807, .F. ) ;
#15417=CYLINDRICAL_SURFACE ( 'NONE', #8433, 88.00000000000000000 ) ;
#15419=CARTESIAN_POINT ( 'NONE',  ( 10.00000000000000000, -84.19736439813780748, -38.30455363801015523 ) ) ;
#15420=EDGE_CURVE ( 'NONE', #20207, #13148, #8710, .T. ) ;
#15422=ORIENTED_EDGE ( 'NONE', *, *, #15134, .F. ) ;
#15424=CIRCLE ( 'NONE', #14004, 92.50100000000000477 ) ;
#15425=ORIENTED_EDGE ( 'NONE', *, *, #8241, .T. ) ;
#15427=EDGE_CURVE ( 'NONE', #7563, #14716, #2110, .T. ) ;
#15428=AXIS2_PLACEMENT_3D ( 'NONE', #12686, #2419, #19006 ) ;
#15429=ORIENTED_EDGE ( 'NONE', *, *, #8001, .F. ) ;
#15430=CARTESIAN_POINT ( 'NONE',  ( 10.00000000000000000, -78.83848282823942100, 48.38314403117473006 ) ) ;
#15433=DIRECTION ( 'NONE',  ( -1.000000000000000000, -0.000000000000000000, -0.000000000000000000 ) ) ;
#15435=EDGE_CURVE ( 'NONE', #21564, #17607, #19032, .T. ) ;
#15437=DIRECTION ( 'NONE',  ( 0.000000000000000000, 0.000000000000000000, 1.000000000000000000 ) ) ;
#15439=ORIENTED_EDGE ( 'NONE', *, *, #8749, .F. ) ;
#15440=CARTESIAN_POINT ( 'NONE',  ( 5.000000000000000000, -72.58367602204151581, -49.75550195834942002 ) ) ;
#15441=AXIS2_PLACEMENT_3D ( 'NONE', #21097, #657, #983 ) ;
#15443=CARTESIAN_POINT ( 'NONE',  ( 10.00000000000000000, 72.58367602204188529, 49.75550195834890843 ) ) ;
#15444=AXIS2_PLACEMENT_3D ( 'NONE', #6606, #20078, #3382 ) ;
#15445=FACE_OUTER_BOUND ( 'NONE', #14123, .T. ) ;
#15446=ORIENTED_EDGE ( 'NONE', *, *, #18671, .T. ) ;
#15447=LINE ( 'NONE', #5073, #17596 ) ;
#15449=LINE ( 'NONE', #325, #8069 ) ;
#15450=ORIENTED_EDGE ( 'NONE', *, *, #1503, .T. ) ;
#15452=ORIENTED_EDGE ( 'NONE', *, *, #17851, .F. ) ;
#15453=VERTEX_POINT ( 'NONE', #21067 ) ;
#15455=VECTOR ( 'NONE', #10774, 1000.000000000000000 ) ;
#15456=CIRCLE ( 'NONE', #18998, 44.99999999999999289 ) ;
#15457=ORIENTED_EDGE ( 'NONE', *, *, #5196, .T. ) ;
#15460=AXIS2_PLACEMENT_3D ( 'NONE', #8861, #12181, #13507 ) ;
#15462=CIRCLE ( 'NONE', #5576, 88.00000000000000000 ) ;
#15464=ADVANCED_FACE ( 'NONE', ( #2175 ), #2610, .F. ) ;
#15465=LINE ( 'NONE', #5413, #13150 ) ;
#15467=CARTESIAN_POINT ( 'NONE',  ( 10.00000000000000000, 81.55207211302078463, -24.17537951050094236 ) ) ;
#15470=CARTESIAN_POINT ( 'NONE',  ( 10.00000000000000000, 32.56745702629739014, 78.57830605990665163 ) ) ;
#15472=DIRECTION ( 'NONE',  ( 1.000000000000000000, 0.000000000000000000, 0.000000000000000000 ) ) ;
#15474=ORIENTED_EDGE ( 'NONE', *, *, #20788, .F. ) ;
#15476=CIRCLE ( 'NONE', #18319, 45.00000000000000000 ) ;
#15477=ORIENTED_EDGE ( 'NONE', *, *, #9092, .T. ) ;
#15478=CARTESIAN_POINT ( 'NONE',  ( 10.00000000000000000, 0.000000000000000000, 0.000000000000000000 ) ) ;
#15479=ORIENTED_EDGE ( 'NONE', *, *, #15270, .F. ) ;
#15480=VERTEX_POINT ( 'NONE', #14208 ) ;
#15482=EDGE_LOOP ( 'NONE', ( #7110, #20896, #11728, #1029 ) ) ;
#15483=AXIS2_PLACEMENT_3D ( 'NONE', #17752, #11003, #6048 ) ;
#15488=AXIS2_PLACEMENT_3D ( 'NONE', #21078, #4503, #21405 ) ;
#15491=AXIS2_PLACEMENT_3D ( 'NONE', #10603, #17351, #14238 ) ;
#15492=EDGE_CURVE ( 'NONE', #6690, #16592, #7055, .T. ) ;
#15494=CARTESIAN_POINT ( 'NONE',  ( 10.00000000000000000, 52.96496548042853192, 66.55750800669373746 ) ) ;
#15495=CARTESIAN_POINT ( 'NONE',  ( 10.00000000000000000, 0.000000000000000000, 0.000000000000000000 ) ) ;
#15496=ORIENTED_EDGE ( 'NONE', *, *, #11790, .F. ) ;
#15498=DIRECTION ( 'NONE',  ( 1.000000000000000000, 0.000000000000000000, 0.000000000000000000 ) ) ;
#15499=AXIS2_PLACEMENT_3D ( 'NONE', #13445, #11462, #11580 ) ;
#15501=VERTEX_POINT ( 'NONE', #7272 ) ;
#15503=AXIS2_PLACEMENT_3D ( 'NONE', #12416, #13866, #19165 ) ;
#15504=LINE ( 'NONE', #17379, #17139 ) ;
#15506=AXIS2_PLACEMENT_3D ( 'NONE', #14678, #6307, #13024 ) ;
#15507=ORIENTED_EDGE ( 'NONE', *, *, #8381, .F. ) ;
#15509=ORIENTED_EDGE ( 'NONE', *, *, #20268, .T. ) ;
#15510=ADVANCED_FACE ( 'NONE', ( #20743 ), #11005, .F. ) ;
#15512=CARTESIAN_POINT ( 'NONE',  ( 0.000000000000000000, 0.000000000000000000, 0.000000000000000000 ) ) ;
#15513=CYLINDRICAL_SURFACE ( 'NONE', #17726, 44.99999999999999289 ) ;
#15515=CARTESIAN_POINT ( 'NONE',  ( -10.00000000000000000, 0.000000000000000000, 0.000000000000000000 ) ) ;
#15516=CARTESIAN_POINT ( 'NONE',  ( 5.000000000000000000, 56.05743251323859511, 67.83483072893820065 ) ) ;
#15517=DIRECTION ( 'NONE',  ( 1.000000000000000000, 0.000000000000000000, 0.000000000000000000 ) ) ;
#15520=DIRECTION ( 'NONE',  ( 0.000000000000000000, 0.000000000000000000, 1.000000000000000000 ) ) ;
#15521=AXIS2_PLACEMENT_3D ( 'NONE', #14629, #8009, #16065 ) ;
#15522=VERTEX_POINT ( 'NONE', #7482 ) ;
#15523=VECTOR ( 'NONE', #12880, 1000.000000000000000 ) ;
#15524=DIRECTION ( 'NONE',  ( 0.000000000000000000, 0.000000000000000000, 1.000000000000000000 ) ) ;
#15526=ORIENTED_EDGE ( 'NONE', *, *, #18562, .T. ) ;
#15527=DIRECTION ( 'NONE',  ( 1.000000000000000000, 0.000000000000000000, 0.000000000000000000 ) ) ;
#15528=ORIENTED_EDGE ( 'NONE', *, *, #17215, .F. ) ;
#15530=DIRECTION ( 'NONE',  ( 0.000000000000000000, 0.2079116908177532363, 0.9781476007338069101 ) ) ;
#15531=VERTEX_POINT ( 'NONE', #13998 ) ;
#15532=VERTEX_POINT ( 'NONE', #5613 ) ;
#15534=VERTEX_POINT ( 'NONE', #3944 ) ;
#15535=EDGE_CURVE ( 'NONE', #11159, #5897, #17652, .T. ) ;
#15537=EDGE_CURVE ( 'NONE', #14927, #16153, #14088, .T. ) ;
#15538=AXIS2_PLACEMENT_3D ( 'NONE', #4225, #9182, #10957 ) ;
#15539=DIRECTION ( 'NONE',  ( 1.000000000000000000, 0.000000000000000000, 0.000000000000000000 ) ) ;
#15541=CARTESIAN_POINT ( 'NONE',  ( 10.00000000000000000, 83.48638250753229784, 27.82128566055142826 ) ) ;
#15543=FACE_OUTER_BOUND ( 'NONE', #7602, .T. ) ;
#15544=CARTESIAN_POINT ( 'NONE',  ( 0.000000000000000000, -61.71252885873347793, -58.53847642588656441 ) ) ;
#15546=CARTESIAN_POINT ( 'NONE',  ( 10.00000000000000000, 84.12297548659704205, 12.59025161327141618 ) ) ;
#15547=CARTESIAN_POINT ( 'NONE',  ( 0.000000000000000000, 43.18649929580291058, -73.28107340219372645 ) ) ;
#15549=VERTEX_POINT ( 'NONE', #12663 ) ;
#15550=CARTESIAN_POINT ( 'NONE',  ( 10.00000000000000000, -65.64563793391867819, 54.09103124042793098 ) ) ;
#15551=EDGE_CURVE ( 'NONE', #9664, #21294, #9144, .T. ) ;
#15553=AXIS2_PLACEMENT_3D ( 'NONE', #3109, #10062, #9843 ) ;
#15554=EDGE_CURVE ( 'NONE', #15334, #8596, #5715, .T. ) ;
#15555=DIRECTION ( 'NONE',  ( 0.000000000000000000, -0.5877852522924632561, -0.8090169943749546677 ) ) ;
#15556=ORIENTED_EDGE ( 'NONE', *, *, #12994, .T. ) ;
#15558=VERTEX_POINT ( 'NONE', #7383 ) ;
#15559=DIRECTION ( 'NONE',  ( -1.000000000000000000, 0.000000000000000000, 0.000000000000000000 ) ) ;
#15560=VERTEX_POINT ( 'NONE', #17541 ) ;
#15563=DIRECTION ( 'NONE',  ( 1.000000000000000000, 0.000000000000000000, 0.000000000000000000 ) ) ;
#15565=CARTESIAN_POINT ( 'NONE',  ( 10.00000000000000000, -90.32141448704695108, 19.96189084378191936 ) ) ;
#15566=CARTESIAN_POINT ( 'NONE',  ( 5.000000000000000000, -61.60362715318993310, -62.84101464466307618 ) ) ;
#15567=AXIS2_PLACEMENT_3D ( 'NONE', #21837, #20187, #17085 ) ;
#15570=CARTESIAN_POINT ( 'NONE',  ( 10.00000000000000000, 68.36541360927188293, 50.60987712331726840 ) ) ;
#15572=DIRECTION ( 'NONE',  ( 1.000000000000000000, 0.000000000000000000, 0.000000000000000000 ) ) ;
#15577=EDGE_CURVE ( 'NONE', #6845, #8545, #19757, .T. ) ;
#15582=EDGE_CURVE ( 'NONE', #20085, #16931, #4380, .T. ) ;
#15583=ADVANCED_FACE ( 'NONE', ( #3054 ), #13202, .F. ) ;
#15585=CARTESIAN_POINT ( 'NONE',  ( 10.00000000000000000, 0.000000000000000000, 0.000000000000000000 ) ) ;
#15586=VERTEX_POINT ( 'NONE', #11120 ) ;
#15587=ORIENTED_EDGE ( 'NONE', *, *, #14061, .F. ) ;
#15588=DIRECTION ( 'NONE',  ( -1.000000000000000000, -0.000000000000000000, -0.000000000000000000 ) ) ;
#15589=EDGE_LOOP ( 'NONE', ( #12860, #7619, #17254, #4251 ) ) ;
#15590=DIRECTION ( 'NONE',  ( 1.000000000000000000, 0.000000000000000000, 0.000000000000000000 ) ) ;
#15591=DIRECTION ( 'NONE',  ( 0.000000000000000000, -0.3420201433256569445, -0.9396926207859125357 ) ) ;
#15593=DIRECTION ( 'NONE',  ( 0.000000000000000000, 0.000000000000000000, 1.000000000000000000 ) ) ;
#15595=EDGE_LOOP ( 'NONE', ( #15807, #3143, #13390, #19306 ) ) ;
#15598=DIRECTION ( 'NONE',  ( 1.000000000000000000, 0.000000000000000000, 0.000000000000000000 ) ) ;
#15599=ORIENTED_EDGE ( 'NONE', *, *, #13407, .F. ) ;
#15600=CIRCLE ( 'NONE', #19483, 44.99999999999999289 ) ;
#15601=CARTESIAN_POINT ( 'NONE',  ( 5.000000000000000000, 81.34229909304679040, 33.57723005635394742 ) ) ;
#15603=ORIENTED_EDGE ( 'NONE', *, *, #12033, .T. ) ;
#15604=DIRECTION ( 'NONE',  ( 0.000000000000000000, -0.06975647374413236623, 0.9975640502598237536 ) ) ;
#15605=ORIENTED_EDGE ( 'NONE', *, *, #7337, .T. ) ;
#15606=DIRECTION ( 'NONE',  ( 1.000000000000000000, 0.000000000000000000, 0.000000000000000000 ) ) ;
#15607=CIRCLE ( 'NONE', #10653, 88.00000000000000000 ) ;
#15609=ORIENTED_EDGE ( 'NONE', *, *, #5535, .F. ) ;
#15610=CARTESIAN_POINT ( 'NONE',  ( 10.00000000000000000, 0.000000000000000000, 0.000000000000000000 ) ) ;
#15611=CARTESIAN_POINT ( 'NONE',  ( 10.00000000000000000, -51.10509369859486384, 77.10190917907182495 ) ) ;
#15613=CARTESIAN_POINT ( 'NONE',  ( 5.000000000000002665, -87.96697768756401103, -2.410567674971490604 ) ) ;
#15615=FACE_OUTER_BOUND ( 'NONE', #18931, .T. ) ;
#15616=DIRECTION ( 'NONE',  ( 0.000000000000000000, -0.5299192642332118952, 0.8480480961564216269 ) ) ;
#15619=DIRECTION ( 'NONE',  ( 1.000000000000000000, 0.000000000000000000, 0.000000000000000000 ) ) ;
#15620=ORIENTED_EDGE ( 'NONE', *, *, #7088, .T. ) ;
#15621=LINE ( 'NONE', #19159, #16788 ) ;
#15624=ORIENTED_EDGE ( 'NONE', *, *, #72, .T. ) ;
#15626=VERTEX_POINT ( 'NONE', #9444 ) ;
#15627=CIRCLE ( 'NONE', #9259, 45.00000000000000000 ) ;
#15630=CARTESIAN_POINT ( 'NONE',  ( 0.000000000000000000, 0.000000000000000000, 0.000000000000000000 ) ) ;
#15631=EDGE_LOOP ( 'NONE', ( #19192, #16671, #5580, #18536 ) ) ;
#15633=AXIS2_PLACEMENT_3D ( 'NONE', #1916, #15606, #13844 ) ;
#15636=VERTEX_POINT ( 'NONE', #7916 ) ;
#15638=CARTESIAN_POINT ( 'NONE',  ( 0.000000000000000000, 0.000000000000000000, 0.000000000000000000 ) ) ;
#15639=ORIENTED_EDGE ( 'NONE', *, *, #18884, .F. ) ;
#15642=CARTESIAN_POINT ( 'NONE',  ( 10.00000000000000000, 0.000000000000000000, 0.000000000000000000 ) ) ;
#15644=DIRECTION ( 'NONE',  ( 1.000000000000000000, 0.000000000000000000, 0.000000000000000000 ) ) ;
#15648=AXIS2_PLACEMENT_3D ( 'NONE', #9188, #2560, #21243 ) ;
#15649=DIRECTION ( 'NONE',  ( -1.000000000000000000, -0.000000000000000000, -0.000000000000000000 ) ) ;
#15650=DIRECTION ( 'NONE',  ( -1.000000000000000000, -0.000000000000000000, 0.000000000000000000 ) ) ;
#15652=EDGE_CURVE ( 'NONE', #7603, #15964, #19043, .T. ) ;
#15653=EDGE_CURVE ( 'NONE', #21244, #21645, #8468, .T. ) ;
#15654=CARTESIAN_POINT ( 'NONE',  ( 0.000000000000000000, -15.51843147776405729, 83.63233659819645993 ) ) ;
#15655=ORIENTED_EDGE ( 'NONE', *, *, #13130, .F. ) ;
#15657=AXIS2_PLACEMENT_3D ( 'NONE', #3724, #18656, #8898 ) ;
#15658=DIRECTION ( 'NONE',  ( -1.000000000000000000, 0.000000000000000000, 0.000000000000000000 ) ) ;
#15659=ORIENTED_EDGE ( 'NONE', *, *, #9044, .T. ) ;
#15660=CARTESIAN_POINT ( 'NONE',  ( 10.00000000000000000, 84.80486432185243473, -36.94008646920313055 ) ) ;
#15661=ORIENTED_EDGE ( 'NONE', *, *, #14465, .T. ) ;
#15662=CIRCLE ( 'NONE', #2954, 88.00000000000000000 ) ;
#15664=VERTEX_POINT ( 'NONE', #9552 ) ;
#15666=CIRCLE ( 'NONE', #2958, 88.00000000000000000 ) ;
#15668=EDGE_CURVE ( 'NONE', #11004, #17333, #5642, .T. ) ;
#15673=EDGE_CURVE ( 'NONE', #16358, #15586, #20472, .T. ) ;
#15675=CARTESIAN_POINT ( 'NONE',  ( 0.000000000000000000, 89.12061559554365431, -24.77803214283454736 ) ) ;
#15676=DIRECTION ( 'NONE',  ( 0.000000000000000000, 0.000000000000000000, 1.000000000000000000 ) ) ;
#15678=FACE_OUTER_BOUND ( 'NONE', #15751, .T. ) ;
#15679=CARTESIAN_POINT ( 'NONE',  ( 10.00000000000000000, 0.000000000000000000, 0.000000000000000000 ) ) ;
#15683=AXIS2_PLACEMENT_3D ( 'NONE', #3904, #20815, #20592 ) ;
#15686=EDGE_CURVE ( 'NONE', #1324, #18185, #14540, .T. ) ;
#15690=AXIS2_PLACEMENT_3D ( 'NONE', #11194, #8512, #15235 ) ;
#15691=ORIENTED_EDGE ( 'NONE', *, *, #6776, .T. ) ;
#15693=ORIENTED_EDGE ( 'NONE', *, *, #7594, .F. ) ;
#15694=CIRCLE ( 'NONE', #15745, 44.99999999999999289 ) ;
#15695=EDGE_CURVE ( 'NONE', #6705, #20437, #11444, .T. ) ;
#15697=DIRECTION ( 'NONE',  ( -1.000000000000000000, -0.000000000000000000, -0.000000000000000000 ) ) ;
#15699=EDGE_CURVE ( 'NONE', #2112, #19416, #3528, .T. ) ;
#15700=CARTESIAN_POINT ( 'NONE',  ( 0.000000000000000000, -33.95793648385753727, -86.04239391578025220 ) ) ;
#15704=CYLINDRICAL_SURFACE ( 'NONE', #21274, 88.00000000000000000 ) ;
#15705=DIRECTION ( 'NONE',  ( -1.000000000000000000, 0.000000000000000000, -0.000000000000000000 ) ) ;
#15706=ADVANCED_FACE ( 'NONE', ( #284 ), #18521, .F. ) ;
#15707=ADVANCED_FACE ( 'NONE', ( #3592 ), #1610, .F. ) ;
#15711=AXIS2_PLACEMENT_3D ( 'NONE', #13171, #2907, #21796 ) ;
#15714=AXIS2_PLACEMENT_3D ( 'NONE', #15933, #9286, #14160 ) ;
#15715=AXIS2_PLACEMENT_3D ( 'NONE', #18976, #1958, #3936 ) ;
#15716=VECTOR ( 'NONE', #5223, 1000.000000000000000 ) ;
#15717=EDGE_CURVE ( 'NONE', #7130, #15626, #10227, .T. ) ;
#15718=DIRECTION ( 'NONE',  ( -1.000000000000000000, 0.000000000000000000, -0.000000000000000000 ) ) ;
#15720=ORIENTED_EDGE ( 'NONE', *, *, #14112, .T. ) ;
#15721=AXIS2_PLACEMENT_3D ( 'NONE', #14959, #380, #7120 ) ;
#15722=CARTESIAN_POINT ( 'NONE',  ( 10.00000000000000000, 8.134922360106093819, 84.67002113262482510 ) ) ;
#15725=DIRECTION ( 'NONE',  ( 1.000000000000000000, 0.000000000000000000, 0.000000000000000000 ) ) ;
#15727=AXIS2_PLACEMENT_3D ( 'NONE', #21333, #6216, #16475 ) ;
#15728=ORIENTED_EDGE ( 'NONE', *, *, #7705, .T. ) ;
#15729=DIRECTION ( 'NONE',  ( 0.000000000000000000, 0.000000000000000000, 1.000000000000000000 ) ) ;
#15730=CIRCLE ( 'NONE', #166, 44.99999999999999289 ) ;
#15731=AXIS2_PLACEMENT_3D ( 'NONE', #1926, #5358, #18625 ) ;
#15732=DIRECTION ( 'NONE',  ( -1.000000000000000000, -0.000000000000000000, -0.000000000000000000 ) ) ;
#15734=CARTESIAN_POINT ( 'NONE',  ( 10.00000000000000000, -64.66851233300690183, -55.25552418573029456 ) ) ;
#15735=DIRECTION ( 'NONE',  ( 1.000000000000000000, -0.000000000000000000, 0.000000000000000000 ) ) ;
#15738=DIRECTION ( 'NONE',  ( -1.000000000000000000, -0.000000000000000000, -0.000000000000000000 ) ) ;
#15739=ORIENTED_EDGE ( 'NONE', *, *, #5288, .F. ) ;
#15740=DIRECTION ( 'NONE',  ( 1.000000000000000000, -0.000000000000000000, 0.000000000000000000 ) ) ;
#15741=EDGE_LOOP ( 'NONE', ( #8221, #18452, #16456, #4415 ) ) ;
#15742=CIRCLE ( 'NONE', #19626, 44.99999999999999289 ) ;
#15744=CARTESIAN_POINT ( 'NONE',  ( 0.000000000000000000, 11.59241532900628258, 87.23311244498744088 ) ) ;
#15745=AXIS2_PLACEMENT_3D ( 'NONE', #2740, #9463, #4619 ) ;
#15747=CARTESIAN_POINT ( 'NONE',  ( 0.000000000000000000, 52.25832601289194201, -70.80301803122729609 ) ) ;
#15749=ORIENTED_EDGE ( 'NONE', *, *, #3112, .F. ) ;
#15750=( LENGTH_UNIT ( ) NAMED_UNIT ( * ) SI_UNIT ( .MILLI., .METRE. ) );
#15751=EDGE_LOOP ( 'NONE', ( #5779, #16958, #812, #13134 ) ) ;
#15752=EDGE_LOOP ( 'NONE', ( #6375, #6259, #18205, #20926 ) ) ;
#15756=VERTEX_POINT ( 'NONE', #6925 ) ;
#15761=DIRECTION ( 'NONE',  ( 1.000000000000000000, 0.000000000000000000, 0.000000000000000000 ) ) ;
#15763=CARTESIAN_POINT ( 'NONE',  ( 10.00000000000000000, -25.56104204395249369, -81.12843256239690959 ) ) ;
#15764=VERTEX_POINT ( 'NONE', #11674 ) ;
#15767=CARTESIAN_POINT ( 'NONE',  ( 10.00000000000000000, -39.87723064937059547, -83.46401306393613595 ) ) ;
#15770=DIRECTION ( 'NONE',  ( 0.000000000000000000, 0.000000000000000000, 1.000000000000000000 ) ) ;
#15771=CIRCLE ( 'NONE', #12940, 88.00000000000000000 ) ;
#15772=ORIENTED_EDGE ( 'NONE', *, *, #5820, .T. ) ;
#15774=AXIS2_PLACEMENT_3D ( 'NONE', #14349, #9042, #5521 ) ;
#15776=ORIENTED_EDGE ( 'NONE', *, *, #7471, .F. ) ;
#15777=ORIENTED_EDGE ( 'NONE', *, *, #19730, .T. ) ;
#15778=CYLINDRICAL_SURFACE ( 'NONE', #17871, 88.00000000000000000 ) ;
#15779=ORIENTED_EDGE ( 'NONE', *, *, #10146, .F. ) ;
#15781=DIRECTION ( 'NONE',  ( 0.000000000000000000, 0.000000000000000000, 1.000000000000000000 ) ) ;
#15782=FACE_OUTER_BOUND ( 'NONE', #17466, .T. ) ;
#15783=EDGE_CURVE ( 'NONE', #18185, #16931, #6011, .T. ) ;
#15784=DIRECTION ( 'NONE',  ( -1.000000000000000000, 0.000000000000000000, -0.000000000000000000 ) ) ;
#15785=AXIS2_PLACEMENT_3D ( 'NONE', #14677, #12909, #19767 ) ;
#15787=AXIS2_PLACEMENT_3D ( 'NONE', #1940, #13764, #3702 ) ;
#15788=LINE ( 'NONE', #20869, #2718 ) ;
#15790=CIRCLE ( 'NONE', #10489, 44.99999999999998579 ) ;
#15791=CYLINDRICAL_SURFACE ( 'NONE', #9075, 44.99999999999999289 ) ;
#15792=FACE_OUTER_BOUND ( 'NONE', #5944, .T. ) ;
#15793=EDGE_LOOP ( 'NONE', ( #20357, #20141, #13520, #6036 ) ) ;
#15795=EDGE_CURVE ( 'NONE', #9608, #1843, #4940, .T. ) ;
#15796=ORIENTED_EDGE ( 'NONE', *, *, #4777, .F. ) ;
#15797=ORIENTED_EDGE ( 'NONE', *, *, #6411, .T. ) ;
#15798=ORIENTED_EDGE ( 'NONE', *, *, #6760, .F. ) ;
#15799=AXIS2_PLACEMENT_3D ( 'NONE', #13389, #20139, #4993 ) ;
#15804=AXIS2_PLACEMENT_3D ( 'NONE', #14427, #21391, #6045 ) ;
#15806=AXIS2_PLACEMENT_3D ( 'NONE', #16947, #5339, #3780 ) ;
#15807=ORIENTED_EDGE ( 'NONE', *, *, #12828, .F. ) ;
#15809=ADVANCED_FACE ( 'NONE', ( #18419 ), #13648, .F. ) ;
#15813=CARTESIAN_POINT ( 'NONE',  ( 0.000000000000000000, -76.53853822673953289, -43.42639941457193231 ) ) ;
#15814=CARTESIAN_POINT ( 'NONE',  ( 10.00000000000000000, 0.000000000000000000, 0.000000000000000000 ) ) ;
#15816=EDGE_CURVE ( 'NONE', #10938, #1, #20810, .T. ) ;
#15818=CARTESIAN_POINT ( 'NONE',  ( 0.000000000000000000, -85.05652083079337444, 0.7600687895857258791 ) ) ;
#15819=DIRECTION ( 'NONE',  ( 1.000000000000000000, 0.000000000000000000, 0.000000000000000000 ) ) ;
#15821=LINE ( 'NONE', #5660, #12613 ) ;
#15822=DIRECTION ( 'NONE',  ( 0.000000000000000000, 0.000000000000000000, 1.000000000000000000 ) ) ;
#15823=AXIS2_PLACEMENT_3D ( 'NONE', #5873, #16130, #12592 ) ;
#15824=ADVANCED_FACE ( 'NONE', ( #20398 ), #10110, .F. ) ;
#15825=AXIS2_PLACEMENT_3D ( 'NONE', #8499, #425, #20438 ) ;
#15826=CIRCLE ( 'NONE', #21474, 44.99999999999999289 ) ;
#15828=AXIS2_PLACEMENT_3D ( 'NONE', #3207, #4875, #18365 ) ;
#15829=DIRECTION ( 'NONE',  ( -1.000000000000000000, -0.000000000000000000, 0.000000000000000000 ) ) ;
#15833=CARTESIAN_POINT ( 'NONE',  ( 10.00000000000000000, -81.97107881582179800, -22.71412948308650925 ) ) ;
#15834=ORIENTED_EDGE ( 'NONE', *, *, #18418, .T. ) ;
#15837=EDGE_CURVE ( 'NONE', #12265, #17743, #17155, .T. ) ;
#15838=AXIS2_PLACEMENT_3D ( 'NONE', #20644, #17118, #7168 ) ;
#15839=FACE_OUTER_BOUND ( 'NONE', #14293, .T. ) ;
#15840=ORIENTED_EDGE ( 'NONE', *, *, #14488, .T. ) ;
#15841=CIRCLE ( 'NONE', #19029, 88.00000000000000000 ) ;
#15843=CARTESIAN_POINT ( 'NONE',  ( 0.000000000000000000, 0.000000000000000000, 0.000000000000000000 ) ) ;
#15845=CIRCLE ( 'NONE', #1016, 88.00000000000000000 ) ;
#15846=EDGE_CURVE ( 'NONE', #10476, #5510, #20287, .T. ) ;
#15850=FACE_OUTER_BOUND ( 'NONE', #4652, .T. ) ;
#15851=DIRECTION ( 'NONE',  ( -1.000000000000000000, -0.000000000000000000, 0.000000000000000000 ) ) ;
#15852=DIRECTION ( 'NONE',  ( 0.000000000000000000, 0.000000000000000000, 1.000000000000000000 ) ) ;
#15853=DIRECTION ( 'NONE',  ( -1.000000000000000000, -0.000000000000000000, -0.000000000000000000 ) ) ;
#15855=FACE_OUTER_BOUND ( 'NONE', #2370, .T. ) ;
#15857=CIRCLE ( 'NONE', #11264, 92.50100000000000477 ) ;
#15861=DIRECTION ( 'NONE',  ( -1.000000000000000000, 0.000000000000000000, 0.000000000000000000 ) ) ;
#15862=EDGE_LOOP ( 'NONE', ( #1786, #11920, #1321, #14070 ) ) ;
#15865=DIRECTION ( 'NONE',  ( 1.000000000000000000, 0.000000000000000000, 0.000000000000000000 ) ) ;
#15867=EDGE_CURVE ( 'NONE', #20116, #11272, #15730, .T. ) ;
#15868=ORIENTED_EDGE ( 'NONE', *, *, #19746, .T. ) ;
#15869=ORIENTED_EDGE ( 'NONE', *, *, #16464, .F. ) ;
#15871=DIRECTION ( 'NONE',  ( 0.000000000000000000, -0.9510565162951503115, -0.3090169943749573322 ) ) ;
#15872=DIRECTION ( 'NONE',  ( 1.000000000000000000, 0.000000000000000000, 0.000000000000000000 ) ) ;
#15873=ORIENTED_EDGE ( 'NONE', *, *, #12604, .F. ) ;
#15874=DIRECTION ( 'NONE',  ( 1.000000000000000000, 0.000000000000000000, 0.000000000000000000 ) ) ;
#15876=CARTESIAN_POINT ( 'NONE',  ( 10.00000000000000000, 0.000000000000000000, 0.000000000000000000 ) ) ;
#15877=AXIS2_PLACEMENT_3D ( 'NONE', #15833, #12071, #10627 ) ;
#15878=AXIS2_PLACEMENT_3D ( 'NONE', #8469, #9996, #6717 ) ;
#15879=CARTESIAN_POINT ( 'NONE',  ( 10.00000000000000000, -87.92084725184945171, -3.731570516143874361 ) ) ;
#15881=EDGE_LOOP ( 'NONE', ( #19563, #20782, #12835, #8799 ) ) ;
#15885=EDGE_LOOP ( 'NONE', ( #20777, #2974, #1239, #5267 ) ) ;
#15891=ORIENTED_EDGE ( 'NONE', *, *, #7064, .T. ) ;
#15894=ORIENTED_EDGE ( 'NONE', *, *, #20039, .T. ) ;
#15895=CARTESIAN_POINT ( 'NONE',  ( 10.00000000000000000, 46.89573839703386682, -79.73220629831438089 ) ) ;
#15897=DIRECTION ( 'NONE',  ( 1.000000000000000000, 0.000000000000000000, 0.000000000000000000 ) ) ;
#15898=DIRECTION ( 'NONE',  ( 0.000000000000000000, 0.000000000000000000, 1.000000000000000000 ) ) ;
#15899=CARTESIAN_POINT ( 'NONE',  ( 10.00000000000000000, 74.39348546125053474, 54.97312363261438151 ) ) ;
#15901=AXIS2_PLACEMENT_3D ( 'NONE', #15478, #12155, #12051 ) ;
#15902=CARTESIAN_POINT ( 'NONE',  ( 5.000000000000000000, 51.18896083639268113, 71.57995730992199412 ) ) ;
#15903=FACE_OUTER_BOUND ( 'NONE', #11135, .T. ) ;
#15905=ORIENTED_EDGE ( 'NONE', *, *, #15158, .T. ) ;
#15908=VERTEX_POINT ( 'NONE', #20719 ) ;
#15909=VERTEX_POINT ( 'NONE', #2253 ) ;
#15915=VERTEX_POINT ( 'NONE', #12206 ) ;
#15916=DIRECTION ( 'NONE',  ( -1.000000000000000000, -0.000000000000000000, -0.000000000000000000 ) ) ;
#15919=FACE_OUTER_BOUND ( 'NONE', #13835, .T. ) ;
#15921=CARTESIAN_POINT ( 'NONE',  ( 0.000000000000000000, -74.39348546125016526, -54.97312363261490731 ) ) ;
#15924=ORIENTED_EDGE ( 'NONE', *, *, #21528, .F. ) ;
#15926=ADVANCED_FACE ( 'NONE', ( #8882 ), #17191, .F. ) ;
#15927=EDGE_CURVE ( 'NONE', #11004, #9608, #12495, .T. ) ;
#15928=EDGE_CURVE ( 'NONE', #18327, #17060, #21379, .T. ) ;
#15929=DIRECTION ( 'NONE',  ( 1.000000000000000000, 0.000000000000000000, 0.000000000000000000 ) ) ;
#15932=ORIENTED_EDGE ( 'NONE', *, *, #18787, .F. ) ;
#15933=CARTESIAN_POINT ( 'NONE',  ( 10.00000000000000000, 0.000000000000000000, 0.000000000000000000 ) ) ;
#15934=ORIENTED_EDGE ( 'NONE', *, *, #670, .F. ) ;
#15935=DIRECTION ( 'NONE',  ( 1.000000000000000000, -0.000000000000000000, 0.000000000000000000 ) ) ;
#15936=ORIENTED_EDGE ( 'NONE', *, *, #170, .T. ) ;
#15937=EDGE_LOOP ( 'NONE', ( #13554, #21694, #8745, #19993 ) ) ;
#15938=CARTESIAN_POINT ( 'NONE',  ( 10.00000000000000000, 90.32141448704683739, 19.96189084378252332 ) ) ;
#15940=EDGE_CURVE ( 'NONE', #454, #4660, #2319, .T. ) ;
#15944=CYLINDRICAL_SURFACE ( 'NONE', #7555, 88.00000000000000000 ) ;
#15946=EDGE_CURVE ( 'NONE', #2427, #21518, #15621, .T. ) ;
#15947=CARTESIAN_POINT ( 'NONE',  ( 0.000000000000000000, 92.32475887865426500, 5.707354816230865602 ) ) ;
#15952=ORIENTED_EDGE ( 'NONE', *, *, #17435, .T. ) ;
#15953=DIRECTION ( 'NONE',  ( -1.000000000000000000, 0.000000000000000000, -0.000000000000000000 ) ) ;
#15954=ORIENTED_EDGE ( 'NONE', *, *, #10940, .T. ) ;
#15956=DIRECTION ( 'NONE',  ( -1.000000000000000000, 0.000000000000000000, 0.000000000000000000 ) ) ;
#15957=ORIENTED_EDGE ( 'NONE', *, *, #21116, .T. ) ;
#15959=CIRCLE ( 'NONE', #11009, 92.50100000000000477 ) ;
#15962=DIRECTION ( 'NONE',  ( -1.000000000000000000, 0.000000000000000000, -0.000000000000000000 ) ) ;
#15964=VERTEX_POINT ( 'NONE', #12635 ) ;
#15965=ADVANCED_FACE ( 'NONE', ( #17516 ), #19062, .F. ) ;
#15967=DIRECTION ( 'NONE',  ( 0.000000000000000000, 0.1391731009600657709, -0.9902680687415702510 ) ) ;
#15968=CARTESIAN_POINT ( 'NONE',  ( 0.000000000000000000, 36.60317927562579854, 76.78148674856777234 ) ) ;
#15969=EDGE_CURVE ( 'NONE', #20720, #14715, #17627, .T. ) ;
#15970=DIRECTION ( 'NONE',  ( -1.000000000000000000, -0.000000000000000000, -0.000000000000000000 ) ) ;
#15972=AXIS2_PLACEMENT_3D ( 'NONE', #19554, #10943, #7960 ) ;
#15973=ADVANCED_FACE ( 'NONE', ( #15855 ), #717, .F. ) ;
#15974=ORIENTED_EDGE ( 'NONE', *, *, #6, .T. ) ;
#15975=ADVANCED_FACE ( 'NONE', ( #5798 ), #12523, .F. ) ;
#15976=DIRECTION ( 'NONE',  ( -1.000000000000000000, -0.000000000000000000, -0.000000000000000000 ) ) ;
#15980=ORIENTED_EDGE ( 'NONE', *, *, #8114, .F. ) ;
#15983=ORIENTED_EDGE ( 'NONE', *, *, #7599, .T. ) ;
#15984=DIRECTION ( 'NONE',  ( 0.000000000000000000, 0.9702957262759955848, 0.2419218955996714493 ) ) ;
#15986=ORIENTED_EDGE ( 'NONE', *, *, #5940, .F. ) ;
#15988=CARTESIAN_POINT ( 'NONE',  ( 10.00000000000000000, 51.18896083639267403, 71.57995730992199412 ) ) ;
#15990=DIRECTION ( 'NONE',  ( 0.000000000000000000, 0.8660254037844399289, -0.4999999999999979461 ) ) ;
#15992=LINE ( 'NONE', #4284, #17113 ) ;
#15994=DIRECTION ( 'NONE',  ( 1.000000000000000000, 0.000000000000000000, 0.000000000000000000 ) ) ;
#15995=CIRCLE ( 'NONE', #13884, 92.50100000000003320 ) ;
#15996=CIRCLE ( 'NONE', #1179, 88.00000000000000000 ) ;
#16000=CARTESIAN_POINT ( 'NONE',  ( 5.000000000000000000, -65.83713140174687339, -58.39068529131263574 ) ) ;
#16001=DIRECTION ( 'NONE',  ( -1.000000000000000000, -0.000000000000000000, -0.000000000000000000 ) ) ;
#16002=AXIS2_PLACEMENT_3D ( 'NONE', #7692, #15970, #836 ) ;
#16003=CARTESIAN_POINT ( 'NONE',  ( 10.00000000000000000, 15.51843147776349063, 83.63233659819657362 ) ) ;
#16004=CIRCLE ( 'NONE', #16716, 88.00000000000000000 ) ;
#16005=ORIENTED_EDGE ( 'NONE', *, *, #10940, .F. ) ;
#16008=ORIENTED_EDGE ( 'NONE', *, *, #15255, .T. ) ;
#16010=VERTEX_POINT ( 'NONE', #12852 ) ;
#16011=DIRECTION ( 'NONE',  ( 0.000000000000000000, -0.8660254037844328234, -0.5000000000000101030 ) ) ;
#16012=AXIS2_PLACEMENT_3D ( 'NONE', #168, #15517, #10318 ) ;
#16013=ORIENTED_EDGE ( 'NONE', *, *, #4326, .T. ) ;
#16014=DIRECTION ( 'NONE',  ( 1.000000000000000000, 0.000000000000000000, 0.000000000000000000 ) ) ;
#16015=DIRECTION ( 'NONE',  ( 0.000000000000000000, -1.603655480014115143E-14, -1.000000000000000000 ) ) ;
#16016=DIRECTION ( 'NONE',  ( -1.000000000000000000, 0.000000000000000000, 0.000000000000000000 ) ) ;
#16017=AXIS2_PLACEMENT_3D ( 'NONE', #8585, #12110, #13668 ) ;
#16018=CARTESIAN_POINT ( 'NONE',  ( 10.00000000000000000, 41.87002153499211232, -74.04114219178001122 ) ) ;
#16019=CARTESIAN_POINT ( 'NONE',  ( 10.00000000000000000, -16.79755869217711250, 90.96305306542248559 ) ) ;
#16020=EDGE_CURVE ( 'NONE', #17231, #15586, #10076, .T. ) ;
#16023=CARTESIAN_POINT ( 'NONE',  ( 10.00000000000000000, 0.000000000000000000, 0.000000000000000000 ) ) ;
#16025=DIRECTION ( 'NONE',  ( 1.000000000000000000, 0.000000000000000000, 0.000000000000000000 ) ) ;
#16026=VERTEX_POINT ( 'NONE', #6131 ) ;
#16028=CARTESIAN_POINT ( 'NONE',  ( 10.00000000000000000, -87.17509410653602231, -30.93441398372672069 ) ) ;
#16029=AXIS2_PLACEMENT_3D ( 'NONE', #6859, #228, #12954 ) ;
#16032=FACE_OUTER_BOUND ( 'NONE', #15147, .T. ) ;
#16035=ORIENTED_EDGE ( 'NONE', *, *, #7314, .T. ) ;
#16037=ORIENTED_EDGE ( 'NONE', *, *, #13285, .F. ) ;
#16039=VECTOR ( 'NONE', #16555, 1000.000000000000000 ) ;
#16040=CARTESIAN_POINT ( 'NONE',  ( 10.00000000000000000, 0.000000000000000000, 0.000000000000000000 ) ) ;
#16044=CARTESIAN_POINT ( 'NONE',  ( 10.00000000000000000, 87.44637528609675314, -9.855528870797693131 ) ) ;
#16046=DIRECTION ( 'NONE',  ( -1.000000000000000000, -0.000000000000000000, -0.000000000000000000 ) ) ;
#16048=EDGE_CURVE ( 'NONE', #20174, #9814, #16060, .T. ) ;
#16049=CIRCLE ( 'NONE', #8659, 92.50100000000000477 ) ;
#16051=DIRECTION ( 'NONE',  ( -1.000000000000000000, 0.000000000000000000, -0.000000000000000000 ) ) ;
#16052=DIRECTION ( 'NONE',  ( -1.000000000000000000, -0.000000000000000000, 0.000000000000000000 ) ) ;
#16055=CARTESIAN_POINT ( 'NONE',  ( 5.000000000000002665, -81.83745710415254848, -32.35167097270233683 ) ) ;
#16056=LINE ( 'NONE', #14404, #17204 ) ;
#16060=LINE ( 'NONE', #7786, #4092 ) ;
#16064=EDGE_CURVE ( 'NONE', #11402, #1182, #4467, .T. ) ;
#16065=DIRECTION ( 'NONE',  ( 0.000000000000000000, -0.1391731009600517543, -0.9902680687415721383 ) ) ;
#16066=CIRCLE ( 'NONE', #12550, 44.99999999999999289 ) ;
#16067=CYLINDRICAL_SURFACE ( 'NONE', #1401, 92.50100000000000477 ) ;
#16069=ORIENTED_EDGE ( 'NONE', *, *, #20574, .T. ) ;
#16072=VECTOR ( 'NONE', #20576, 1000.000000000000000 ) ;
#16073=ORIENTED_EDGE ( 'NONE', *, *, #16472, .T. ) ;
#16074=ORIENTED_EDGE ( 'NONE', *, *, #18512, .F. ) ;
#16076=CARTESIAN_POINT ( 'NONE',  ( 0.000000000000000000, 88.70892494636740366, 26.21376805916615282 ) ) ;
#16078=ORIENTED_EDGE ( 'NONE', *, *, #9308, .F. ) ;
#16079=EDGE_CURVE ( 'NONE', #11398, #10855, #17730, .T. ) ;
#16083=ADVANCED_FACE ( 'NONE', ( #21370 ), #12745, .F. ) ;
#16085=CIRCLE ( 'NONE', #17864, 88.00000000000000000 ) ;
#16086=CARTESIAN_POINT ( 'NONE',  ( 10.00000000000000000, -92.22057093985026199, -7.197311757041478408 ) ) ;
#16087=ADVANCED_FACE ( 'NONE', ( #1042 ), #21260, .F. ) ;
#16088=AXIS2_PLACEMENT_3D ( 'NONE', #20017, #13592, #3437 ) ;
#16089=ORIENTED_EDGE ( 'NONE', *, *, #6678, .F. ) ;
#16090=AXIS2_PLACEMENT_3D ( 'NONE', #2687, #803, #7449 ) ;
#16091=DIRECTION ( 'NONE',  ( -1.000000000000000000, -0.000000000000000000, -0.000000000000000000 ) ) ;
#16092=CIRCLE ( 'NONE', #8983, 44.99999999999998579 ) ;
#16094=DIRECTION ( 'NONE',  ( -1.000000000000000000, -0.000000000000000000, -0.000000000000000000 ) ) ;
#16095=ADVANCED_FACE ( 'NONE', ( #17688 ), #20886, .F. ) ;
#16097=CARTESIAN_POINT ( 'NONE',  ( 10.00000000000000000, -88.70892494636720471, -26.21376805916674613 ) ) ;
#16098=ORIENTED_EDGE ( 'NONE', *, *, #5125, .F. ) ;
#16101=ORIENTED_EDGE ( 'NONE', *, *, #5166, .F. ) ;
#16102=VERTEX_POINT ( 'NONE', #17261 ) ;
#16105=CARTESIAN_POINT ( 'NONE',  ( 10.00000000000000000, -33.95793648385753727, -86.04239391578025220 ) ) ;
#16107=EDGE_CURVE ( 'NONE', #453, #6547, #6930, .T. ) ;
#16112=CARTESIAN_POINT ( 'NONE',  ( 0.000000000000000000, 27.00677879429026618, 80.65868421664441712 ) ) ;
#16113=ADVANCED_FACE ( 'NONE', ( #677 ), #19344, .F. ) ;
#16114=FACE_OUTER_BOUND ( 'NONE', #7259, .T. ) ;
#16115=CARTESIAN_POINT ( 'NONE',  ( 10.00000000000000000, -47.19205848891713373, -74.27590198428171675 ) ) ;
#16116=CARTESIAN_POINT ( 'NONE',  ( 0.000000000000000000, 75.87763420127832603, 44.57111876559751096 ) ) ;
#16118=CIRCLE ( 'NONE', #17899, 92.50100000000000477 ) ;
#16120=CIRCLE ( 'NONE', #17534, 92.50100000000000477 ) ;
#16121=CIRCLE ( 'NONE', #10128, 92.50100000000000477 ) ;
#16122=CARTESIAN_POINT ( 'NONE',  ( 0.000000000000000000, -18.94217447942616417, 85.93715160505946926 ) ) ;
#16123=ORIENTED_EDGE ( 'NONE', *, *, #10115, .F. ) ;
#16125=EDGE_CURVE ( 'NONE', #20835, #7559, #9719, .T. ) ;
#16126=VERTEX_POINT ( 'NONE', #5875 ) ;
#16129=ORIENTED_EDGE ( 'NONE', *, *, #7432, .F. ) ;
#16130=DIRECTION ( 'NONE',  ( 1.000000000000000000, 0.000000000000000000, 0.000000000000000000 ) ) ;
#16132=EDGE_LOOP ( 'NONE', ( #10322, #8501, #12917, #4827 ) ) ;
#16133=DIRECTION ( 'NONE',  ( 0.000000000000000000, -0.6946583704590034714, 0.7193398003386453077 ) ) ;
#16134=AXIS2_PLACEMENT_3D ( 'NONE', #6280, #11565, #1502 ) ;
#16136=AXIS2_PLACEMENT_3D ( 'NONE', #13228, #9475, #7825 ) ;
#16138=DIRECTION ( 'NONE',  ( 0.000000000000000000, -0.9510565162951503115, -0.3090169943749573878 ) ) ;
#16139=DIRECTION ( 'NONE',  ( -1.000000000000000000, 0.000000000000000000, -0.000000000000000000 ) ) ;
#16144=ORIENTED_EDGE ( 'NONE', *, *, #6354, .T. ) ;
#16147=AXIS2_PLACEMENT_3D ( 'NONE', #21708, #8233, #8134 ) ;
#16150=EDGE_CURVE ( 'NONE', #5864, #16720, #6874, .T. ) ;
#16152=DIRECTION ( 'NONE',  ( 1.000000000000000000, 0.000000000000000000, 0.000000000000000000 ) ) ;
#16153=VERTEX_POINT ( 'NONE', #12273 ) ;
#16155=VERTEX_POINT ( 'NONE', #15700 ) ;
#16156=VERTEX_POINT ( 'NONE', #14042 ) ;
#16159=DIRECTION ( 'NONE',  ( -1.000000000000000000, -0.000000000000000000, -0.000000000000000000 ) ) ;
#16161=VERTEX_POINT ( 'NONE', #17478 ) ;
#16164=AXIS2_PLACEMENT_3D ( 'NONE', #356, #13931, #20673 ) ;
#16166=DIRECTION ( 'NONE',  ( 0.000000000000000000, 0.000000000000000000, 1.000000000000000000 ) ) ;
#16168=VECTOR ( 'NONE', #474, 1000.000000000000000 ) ;
#16169=CARTESIAN_POINT ( 'NONE',  ( 0.000000000000000000, 0.000000000000000000, 0.000000000000000000 ) ) ;
#16171=DIRECTION ( 'NONE',  ( 1.000000000000000000, 0.000000000000000000, 0.000000000000000000 ) ) ;
#16173=DIRECTION ( 'NONE',  ( 0.000000000000000000, 0.000000000000000000, 1.000000000000000000 ) ) ;
#16174=DIRECTION ( 'NONE',  ( -1.000000000000000000, 0.000000000000000000, 0.000000000000000000 ) ) ;
#16178=ORIENTED_EDGE ( 'NONE', *, *, #19673, .F. ) ;
#16180=AXIS2_PLACEMENT_3D ( 'NONE', #18454, #8286, #14910 ) ;
#16182=EDGE_CURVE ( 'NONE', #286, #1246, #7570, .T. ) ;
#16188=ORIENTED_EDGE ( 'NONE', *, *, #2748, .T. ) ;
#16190=ORIENTED_EDGE ( 'NONE', *, *, #17489, .F. ) ;
#16191=DIRECTION ( 'NONE',  ( 1.000000000000000000, 0.000000000000000000, 0.000000000000000000 ) ) ;
#16193=EDGE_CURVE ( 'NONE', #21294, #4861, #3986, .T. ) ;
#16196=DIRECTION ( 'NONE',  ( 0.000000000000000000, 0.000000000000000000, 1.000000000000000000 ) ) ;
#16197=CARTESIAN_POINT ( 'NONE',  ( 0.000000000000000000, -25.56104204395249369, -81.12843256239690959 ) ) ;
#16198=DIRECTION ( 'NONE',  ( 0.000000000000000000, -0.8290375725550467312, 0.5591929034707392443 ) ) ;
#16200=EDGE_CURVE ( 'NONE', #13661, #13981, #9324, .T. ) ;
#16204=DIRECTION ( 'NONE',  ( 0.000000000000000000, -0.06975647374411138302, -0.9975640502598251969 ) ) ;
#16207=DIRECTION ( 'NONE',  ( -1.000000000000000000, -0.000000000000000000, -0.000000000000000000 ) ) ;
#16208=ORIENTED_EDGE ( 'NONE', *, *, #18772, .F. ) ;
#16213=DIRECTION ( 'NONE',  ( 0.000000000000000000, -0.5877852522924797984, 0.8090169943749424553 ) ) ;
#16214=ORIENTED_EDGE ( 'NONE', *, *, #6102, .F. ) ;
#16215=CYLINDRICAL_SURFACE ( 'NONE', #6039, 44.99999999999999289 ) ;
#16216=EDGE_CURVE ( 'NONE', #18291, #7130, #2282, .T. ) ;
#16218=VERTEX_POINT ( 'NONE', #7633 ) ;
#16219=ORIENTED_EDGE ( 'NONE', *, *, #19892, .T. ) ;
#16220=CIRCLE ( 'NONE', #9142, 92.50099999999999056 ) ;
#16221=DIRECTION ( 'NONE',  ( -1.000000000000000000, -0.000000000000000000, -0.000000000000000000 ) ) ;
#16222=AXIS2_PLACEMENT_3D ( 'NONE', #14650, #3165, #16204 ) ;
#16223=VERTEX_POINT ( 'NONE', #15813 ) ;
#16226=DIRECTION ( 'NONE',  ( 0.000000000000000000, -0.5877852522924632561, -0.8090169943749545567 ) ) ;
#16229=DIRECTION ( 'NONE',  ( -1.000000000000000000, -0.000000000000000000, -0.000000000000000000 ) ) ;
#16230=DIRECTION ( 'NONE',  ( 0.000000000000000000, 0.000000000000000000, 1.000000000000000000 ) ) ;
#16231=DIRECTION ( 'NONE',  ( -1.000000000000000000, -0.000000000000000000, -0.000000000000000000 ) ) ;
#16232=ADVANCED_FACE ( 'NONE', ( #19447 ), #570, .F. ) ;
#16234=AXIS2_PLACEMENT_3D ( 'NONE', #6367, #9535, #13076 ) ;
#16235=CARTESIAN_POINT ( 'NONE',  ( 10.00000000000000000, 0.000000000000000000, 0.000000000000000000 ) ) ;
#16236=ORIENTED_EDGE ( 'NONE', *, *, #3830, .T. ) ;
#16238=ORIENTED_EDGE ( 'NONE', *, *, #18418, .F. ) ;
#16240=VERTEX_POINT ( 'NONE', #15007 ) ;
#16241=ORIENTED_EDGE ( 'NONE', *, *, #7879, .F. ) ;
#16242=CARTESIAN_POINT ( 'NONE',  ( 10.00000000000000000, 10.41137886060228901, -91.91321010181836471 ) ) ;
#16243=ORIENTED_EDGE ( 'NONE', *, *, #12879, .F. ) ;
#16244=CYLINDRICAL_SURFACE ( 'NONE', #5373, 88.00000000000000000 ) ;
#16245=AXIS2_PLACEMENT_3D ( 'NONE', #4322, #1020, #2790 ) ;
#16246=CARTESIAN_POINT ( 'NONE',  ( 0.000000000000000000, -0.6609040254605957898, -87.99751818016876825 ) ) ;
#16249=CARTESIAN_POINT ( 'NONE',  ( 5.000000000000002665, -18.94217447942616417, 85.93715160505946926 ) ) ;
#16251=EDGE_CURVE ( 'NONE', #14961, #11159, #6892, .T. ) ;
#16252=DIRECTION ( 'NONE',  ( -1.000000000000000000, 0.000000000000000000, 0.000000000000000000 ) ) ;
#16254=DIRECTION ( 'NONE',  ( -1.000000000000000000, -0.000000000000000000, -0.000000000000000000 ) ) ;
#16256=ORIENTED_EDGE ( 'NONE', *, *, #17886, .F. ) ;
#16258=DIRECTION ( 'NONE',  ( 0.000000000000000000, -0.2079116908177664480, 0.9781476007338041345 ) ) ;
#16259=VECTOR ( 'NONE', #18701, 1000.000000000000000 ) ;
#16262=DIRECTION ( 'NONE',  ( -1.000000000000000000, 0.000000000000000000, 0.000000000000000000 ) ) ;
#16267=DIRECTION ( 'NONE',  ( 1.000000000000000000, -0.000000000000000000, 0.000000000000000000 ) ) ;
#16268=ORIENTED_EDGE ( 'NONE', *, *, #21246, .T. ) ;
#16269=ORIENTED_EDGE ( 'NONE', *, *, #13237, .T. ) ;
#16273=DIRECTION ( 'NONE',  ( 0.000000000000000000, 0.000000000000000000, 1.000000000000000000 ) ) ;
#16274=COLOUR_RGB ( '', 0.31764706, 0.68627451, 0.89019608) ;
#16275=LINE ( 'NONE', #20224, #9667 ) ;
#16276=DIRECTION ( 'NONE',  ( -1.000000000000000000, -0.000000000000000000, -0.000000000000000000 ) ) ;
#16277=CARTESIAN_POINT ( 'NONE',  ( 10.00000000000000000, 0.000000000000000000, 0.000000000000000000 ) ) ;
#16278=CYLINDRICAL_SURFACE ( 'NONE', #8060, 88.00000000000000000 ) ;
#16280=CARTESIAN_POINT ( 'NONE',  ( -10.00000000000000000, 0.000000000000000000, 0.000000000000000000 ) ) ;
#16281=ORIENTED_EDGE ( 'NONE', *, *, #17299, .F. ) ;
#16282=CARTESIAN_POINT ( 'NONE',  ( 10.00000000000000000, 86.54587337002878655, 15.93147207947034971 ) ) ;
#16285=EDGE_LOOP ( 'NONE', ( #17313, #21259, #12030, #8736 ) ) ;
#16288=ORIENTED_EDGE ( 'NONE', *, *, #14777, .T. ) ;
#16292=ORIENTED_EDGE ( 'NONE', *, *, #18059, .F. ) ;
#16294=CARTESIAN_POINT ( 'NONE',  ( 10.00000000000000000, 0.000000000000000000, 0.000000000000000000 ) ) ;
#16295=CARTESIAN_POINT ( 'NONE',  ( 10.00000000000000000, -52.34334029047928993, 76.26670130689468863 ) ) ;
#16297=DIRECTION ( 'NONE',  ( 0.000000000000000000, 0.6946583704589983643, -0.7193398003386500816 ) ) ;
#16302=VERTEX_POINT ( 'NONE', #1526 ) ;
#16303=CARTESIAN_POINT ( 'NONE',  ( 0.000000000000000000, 0.000000000000000000, 0.000000000000000000 ) ) ;
#16305=DIRECTION ( 'NONE',  ( -1.000000000000000000, 0.000000000000000000, -0.000000000000000000 ) ) ;
#16308=CARTESIAN_POINT ( 'NONE',  ( 10.00000000000000000, -56.05743251323810483, -67.83483072893858434 ) ) ;
#16311=DIRECTION ( 'NONE',  ( -1.000000000000000000, -0.000000000000000000, -0.000000000000000000 ) ) ;
#16312=CARTESIAN_POINT ( 'NONE',  ( 0.000000000000000000, 84.12297548659721258, -12.59025161327029529 ) ) ;
#16316=ORIENTED_EDGE ( 'NONE', *, *, #8812, .F. ) ;
#16317=EDGE_LOOP ( 'NONE', ( #9942, #6065, #2063, #10721 ) ) ;
#16318=CARTESIAN_POINT ( 'NONE',  ( 10.00000000000000000, 15.32665449651924661, 91.22241316115426457 ) ) ;
#16319=ORIENTED_EDGE ( 'NONE', *, *, #14156, .T. ) ;
#16320=CARTESIAN_POINT ( 'NONE',  ( 5.000000000000000000, -81.34229909304701778, 33.57723005635337898 ) ) ;
#16321=VECTOR ( 'NONE', #13582, 1000.000000000000000 ) ;
#16322=FACE_OUTER_BOUND ( 'NONE', #4208, .T. ) ;
#16324=CARTESIAN_POINT ( 'NONE',  ( 0.000000000000000000, 56.34908017029645322, -63.71789861856395731 ) ) ;
#16325=VECTOR ( 'NONE', #19005, 1000.000000000000000 ) ;
#16326=AXIS2_PLACEMENT_3D ( 'NONE', #17009, #18457, #106 ) ;
#16327=ADVANCED_FACE ( 'NONE', ( #9808 ), #5069, .F. ) ;
#16328=DIRECTION ( 'NONE',  ( -1.000000000000000000, -0.000000000000000000, -0.000000000000000000 ) ) ;
#16329=ADVANCED_FACE ( 'NONE', ( #4632 ), #19769, .F. ) ;
#16332=CARTESIAN_POINT ( 'NONE',  ( 0.000000000000000000, -5.479102470011078196, 87.82926298292112222 ) ) ;
#16334=ADVANCED_FACE ( 'NONE', ( #13125 ), #13235, .F. ) ;
#16335=DIRECTION ( 'NONE',  ( 0.000000000000000000, 0.3420201433256630508, 0.9396926207859104263 ) ) ;
#16336=ORIENTED_EDGE ( 'NONE', *, *, #20845, .T. ) ;
#16338=ORIENTED_EDGE ( 'NONE', *, *, #9509, .T. ) ;
#16339=VERTEX_POINT ( 'NONE', #18445 ) ;
#16341=ORIENTED_EDGE ( 'NONE', *, *, #143, .T. ) ;
#16342=AXIS2_PLACEMENT_3D ( 'NONE', #794, #16159, #6345 ) ;
#16345=DIRECTION ( 'NONE',  ( 0.000000000000000000, 0.000000000000000000, 1.000000000000000000 ) ) ;
#16348=CARTESIAN_POINT ( 'NONE',  ( 10.00000000000000000, 0.000000000000000000, 100.0000000000000000 ) ) ;
#16350=CARTESIAN_POINT ( 'NONE',  ( 10.00000000000000000, 0.000000000000000000, 0.000000000000000000 ) ) ;
#16351=DIRECTION ( 'NONE',  ( 1.000000000000000000, -0.000000000000000000, -0.000000000000000000 ) ) ;
#16352=CARTESIAN_POINT ( 'NONE',  ( 10.00000000000000000, -87.17509410653602231, -30.93441398372672069 ) ) ;
#16354=CARTESIAN_POINT ( 'NONE',  ( 0.000000000000000000, -52.25832601289046409, -70.80301803122840454 ) ) ;
#16356=CIRCLE ( 'NONE', #20605, 44.99999999999998579 ) ;
#16358=VERTEX_POINT ( 'NONE', #6520 ) ;
#16359=AXIS2_PLACEMENT_3D ( 'NONE', #10773, #2268, #12330 ) ;
#16360=DIRECTION ( 'NONE',  ( -1.000000000000000000, 0.000000000000000000, 0.000000000000000000 ) ) ;
#16361=VERTEX_POINT ( 'NONE', #4850 ) ;
#16362=ORIENTED_EDGE ( 'NONE', *, *, #14596, .F. ) ;
#16363=LINE ( 'NONE', #13050, #8414 ) ;
#16365=FACE_OUTER_BOUND ( 'NONE', #17840, .T. ) ;
#16367=ORIENTED_EDGE ( 'NONE', *, *, #21329, .F. ) ;
#16368=DIRECTION ( 'NONE',  ( 0.000000000000000000, -2.035408878479454078E-14, -1.000000000000000000 ) ) ;
#16369=ORIENTED_EDGE ( 'NONE', *, *, #12879, .T. ) ;
#16376=ORIENTED_EDGE ( 'NONE', *, *, #20414, .T. ) ;
#16377=FACE_OUTER_BOUND ( 'NONE', #10422, .T. ) ;
#16379=CYLINDRICAL_SURFACE ( 'NONE', #8805, 45.00000000000000000 ) ;
#16380=EDGE_CURVE ( 'NONE', #6192, #5341, #12513, .T. ) ;
#16382=CYLINDRICAL_SURFACE ( 'NONE', #8055, 44.99999999999998579 ) ;
#16384=CARTESIAN_POINT ( 'NONE',  ( 10.00000000000000000, 27.87320266523557777, 88.20158487341770126 ) ) ;
#16387=CARTESIAN_POINT ( 'NONE',  ( 0.000000000000000000, -78.01214607583727911, -33.90124636420193838 ) ) ;
#16388=AXIS2_PLACEMENT_3D ( 'NONE', #15347, #1874, #4672 ) ;
#16389=EDGE_CURVE ( 'NONE', #13540, #2135, #16401, .T. ) ;
#16391=VECTOR ( 'NONE', #5026, 1000.000000000000000 ) ;
#16393=CARTESIAN_POINT ( 'NONE',  ( 0.000000000000000000, -67.05625154133495869, 63.71729851637790176 ) ) ;
#16395=CARTESIAN_POINT ( 'NONE',  ( 10.00000000000000000, 81.97107881582226696, -22.71412948308482171 ) ) ;
#16398=AXIS2_PLACEMENT_3D ( 'NONE', #19428, #6073, #16230 ) ;
#16399=ORIENTED_EDGE ( 'NONE', *, *, #48, .F. ) ;
#16401=CIRCLE ( 'NONE', #17105, 88.00000000000000000 ) ;
#16402=ORIENTED_EDGE ( 'NONE', *, *, #1265, .T. ) ;
#16405=ORIENTED_EDGE ( 'NONE', *, *, #11468, .F. ) ;
#16406=AXIS2_PLACEMENT_3D ( 'NONE', #13218, #19970, #4836 ) ;
#16407=EDGE_CURVE ( 'NONE', #13052, #10717, #3692, .T. ) ;
#16408=FACE_OUTER_BOUND ( 'NONE', #6109, .T. ) ;
#16412=VECTOR ( 'NONE', #17667, 1000.000000000000000 ) ;
#16413=FACE_OUTER_BOUND ( 'NONE', #10732, .T. ) ;
#16414=DIRECTION ( 'NONE',  ( 0.000000000000000000, -0.9945218953682722907, -0.1045284632676635739 ) ) ;
#16416=VERTEX_POINT ( 'NONE', #3618 ) ;
#16417=DIRECTION ( 'NONE',  ( -1.000000000000000000, 0.000000000000000000, 0.000000000000000000 ) ) ;
#16419=VECTOR ( 'NONE', #16174, 1000.000000000000000 ) ;
#16421=CIRCLE ( 'NONE', #1593, 45.00000000000000000 ) ;
#16422=CIRCLE ( 'NONE', #2304, 92.50099999999999056 ) ;
#16424=AXIS2_PLACEMENT_3D ( 'NONE', #11163, #6205, #14694 ) ;
#16426=DIRECTION ( 'NONE',  ( 0.000000000000000000, 0.9271838545667858700, 0.3746065934159160116 ) ) ;
#16427=DIRECTION ( 'NONE',  ( 0.000000000000000000, 0.000000000000000000, 1.000000000000000000 ) ) ;
#16430=DIRECTION ( 'NONE',  ( 1.000000000000000000, 0.000000000000000000, -0.000000000000000000 ) ) ;
#16433=CIRCLE ( 'NONE', #11481, 92.50100000000000477 ) ;
#16436=VERTEX_POINT ( 'NONE', #15443 ) ;
#16439=DIRECTION ( 'NONE',  ( -1.000000000000000000, 0.000000000000000000, -0.000000000000000000 ) ) ;
#16440=VECTOR ( 'NONE', #19385, 1000.000000000000000 ) ;
#16443=AXIS2_PLACEMENT_3D ( 'NONE', #3693, #11985, #15399 ) ;
#16444=AXIS2_PLACEMENT_3D ( 'NONE', #16023, #12601, #13939 ) ;
#16448=DIRECTION ( 'NONE',  ( 1.000000000000000000, 0.000000000000000000, 0.000000000000000000 ) ) ;
#16449=DIRECTION ( 'NONE',  ( 1.000000000000000000, 0.000000000000000000, 0.000000000000000000 ) ) ;
#16452=ORIENTED_EDGE ( 'NONE', *, *, #18133, .F. ) ;
#16453=CIRCLE ( 'NONE', #21737, 44.99999999999999289 ) ;
#16454=ORIENTED_EDGE ( 'NONE', *, *, #15389, .T. ) ;
#16455=CIRCLE ( 'NONE', #3068, 44.99999999999998579 ) ;
#16456=ORIENTED_EDGE ( 'NONE', *, *, #9044, .F. ) ;
#16457=ORIENTED_EDGE ( 'NONE', *, *, #7937, .F. ) ;
#16458=EDGE_CURVE ( 'NONE', #14138, #797, #18528, .T. ) ;
#16461=ORIENTED_EDGE ( 'NONE', *, *, #18689, .T. ) ;
#16462=DIRECTION ( 'NONE',  ( 0.000000000000000000, 0.000000000000000000, 1.000000000000000000 ) ) ;
#16464=EDGE_CURVE ( 'NONE', #11867, #3268, #14281, .T. ) ;
#16466=AXIS2_PLACEMENT_3D ( 'NONE', #8775, #5571, #3481 ) ;
#16467=LINE ( 'NONE', #16249, #12641 ) ;
#16468=AXIS2_PLACEMENT_3D ( 'NONE', #5504, #20434, #2180 ) ;
#16471=DIRECTION ( 'NONE',  ( -1.000000000000000000, -0.000000000000000000, 0.000000000000000000 ) ) ;
#16472=EDGE_CURVE ( 'NONE', #9671, #18821, #4752, .T. ) ;
#16473=DIRECTION ( 'NONE',  ( 1.000000000000000000, 0.000000000000000000, 0.000000000000000000 ) ) ;
#16475=DIRECTION ( 'NONE',  ( 0.000000000000000000, 0.000000000000000000, 1.000000000000000000 ) ) ;
#16476=VERTEX_POINT ( 'NONE', #8594 ) ;
#16477=ORIENTED_EDGE ( 'NONE', *, *, #7726, .F. ) ;
#16478=CIRCLE ( 'NONE', #14002, 88.00000000000000000 ) ;
#16479=CYLINDRICAL_SURFACE ( 'NONE', #15553, 44.99999999999999289 ) ;
#16480=EDGE_CURVE ( 'NONE', #6845, #11540, #20322, .T. ) ;
#16481=ORIENTED_EDGE ( 'NONE', *, *, #7726, .T. ) ;
#16483=VECTOR ( 'NONE', #8712, 1000.000000000000000 ) ;
#16484=EDGE_CURVE ( 'NONE', #3028, #19897, #10467, .T. ) ;
#16485=DIRECTION ( 'NONE',  ( 0.000000000000000000, 0.000000000000000000, -1.000000000000000000 ) ) ;
#16486=ORIENTED_EDGE ( 'NONE', *, *, #16458, .F. ) ;
#16487=ORIENTED_EDGE ( 'NONE', *, *, #12164, .T. ) ;
#16488=AXIS2_PLACEMENT_3D ( 'NONE', #14675, #1087, #9802 ) ;
#16490=DIRECTION ( 'NONE',  ( -1.000000000000000000, -0.000000000000000000, 0.000000000000000000 ) ) ;
#16493=LINE ( 'NONE', #17939, #7222 ) ;
#16494=DIRECTION ( 'NONE',  ( 1.000000000000000000, 0.000000000000000000, 0.000000000000000000 ) ) ;
#16495=CARTESIAN_POINT ( 'NONE',  ( 10.00000000000000000, 30.71797041605808687, 82.46457599186561538 ) ) ;
#16496=CYLINDRICAL_SURFACE ( 'NONE', #1542, 88.00000000000000000 ) ;
#16497=LINE ( 'NONE', #8107, #18581 ) ;
#16500=CARTESIAN_POINT ( 'NONE',  ( 5.000000000000002665, 87.44637528609675314, -9.855528870797686025 ) ) ;
#16502=DIRECTION ( 'NONE',  ( -1.000000000000000000, 0.000000000000000000, 0.000000000000000000 ) ) ;
#16503=CIRCLE ( 'NONE', #8038, 44.99999999999999289 ) ;
#16504=AXIS2_PLACEMENT_3D ( 'NONE', #3238, #8119, #2817 ) ;
#16509=ADVANCED_FACE ( 'NONE', ( #5614 ), #19089, .F. ) ;
#16511=CARTESIAN_POINT ( 'NONE',  ( 0.000000000000000000, 0.000000000000000000, 0.000000000000000000 ) ) ;
#16512=ORIENTED_EDGE ( 'NONE', *, *, #19588, .T. ) ;
#16514=ORIENTED_EDGE ( 'NONE', *, *, #20161, .F. ) ;
#16520=CARTESIAN_POINT ( 'NONE',  ( 10.00000000000000000, -80.18694381077126820, 28.37681241246628616 ) ) ;
#16521=DIRECTION ( 'NONE',  ( 1.000000000000000000, 0.000000000000000000, 0.000000000000000000 ) ) ;
#16523=ORIENTED_EDGE ( 'NONE', *, *, #2840, .F. ) ;
#16524=CYLINDRICAL_SURFACE ( 'NONE', #9673, 44.99999999999998579 ) ;
#16525=FACE_OUTER_BOUND ( 'NONE', #19245, .T. ) ;
#16526=DIRECTION ( 'NONE',  ( -1.000000000000000000, 0.000000000000000000, -0.000000000000000000 ) ) ;
#16528=FACE_OUTER_BOUND ( 'NONE', #17415, .T. ) ;
#16529=CARTESIAN_POINT ( 'NONE',  ( 5.000000000000000000, 72.58367602204188529, 49.75550195834890843 ) ) ;
#16533=DIRECTION ( 'NONE',  ( 0.000000000000000000, 0.000000000000000000, 1.000000000000000000 ) ) ;
#16534=AXIS2_PLACEMENT_3D ( 'NONE', #13359, #21431, #11370 ) ;
#16535=DIRECTION ( 'NONE',  ( 0.000000000000000000, 0.000000000000000000, -1.000000000000000000 ) ) ;
#16537=ORIENTED_EDGE ( 'NONE', *, *, #7761, .F. ) ;
#16538=EDGE_CURVE ( 'NONE', #879, #20835, #843, .T. ) ;
#16539=AXIS2_PLACEMENT_3D ( 'NONE', #2672, #17930, #9396 ) ;
#16540=CIRCLE ( 'NONE', #16888, 45.00000000000000000 ) ;
#16541=EDGE_CURVE ( 'NONE', #5399, #5754, #15355, .T. ) ;
#16542=LINE ( 'NONE', #11334, #21766 ) ;
#16543=ORIENTED_EDGE ( 'NONE', *, *, #19998, .T. ) ;
#16544=DIRECTION ( 'NONE',  ( 0.000000000000000000, -0.9848077530122096857, 0.1736481776669207000 ) ) ;
#16545=DIRECTION ( 'NONE',  ( -1.000000000000000000, 0.000000000000000000, 0.000000000000000000 ) ) ;
#16546=ORIENTED_EDGE ( 'NONE', *, *, #21344, .T. ) ;
#16547=DIRECTION ( 'NONE',  ( 0.000000000000000000, 0.000000000000000000, 1.000000000000000000 ) ) ;
#16548=EDGE_LOOP ( 'NONE', ( #21157, #13056, #10607, #8826 ) ) ;
#16551=CARTESIAN_POINT ( 'NONE',  ( 10.00000000000000000, 2.481790431840499966, -92.46770094066590673 ) ) ;
#16552=ORIENTED_EDGE ( 'NONE', *, *, #9479, .F. ) ;
#16554=CIRCLE ( 'NONE', #8430, 45.00000000000000000 ) ;
#16555=DIRECTION ( 'NONE',  ( -1.000000000000000000, 0.000000000000000000, 0.000000000000000000 ) ) ;
#16556=DIRECTION ( 'NONE',  ( -1.000000000000000000, 0.000000000000000000, 0.000000000000000000 ) ) ;
#16557=DIRECTION ( 'NONE',  ( -1.000000000000000000, -0.000000000000000000, -0.000000000000000000 ) ) ;
#16560=DIRECTION ( 'NONE',  ( 0.000000000000000000, -0.6427876096865299260, -0.7660444431189857850 ) ) ;
#16563=CYLINDRICAL_SURFACE ( 'NONE', #12958, 92.50100000000000477 ) ;
#16564=DIRECTION ( 'NONE',  ( 1.000000000000000000, 0.000000000000000000, 0.000000000000000000 ) ) ;
#16567=AXIS2_PLACEMENT_3D ( 'NONE', #12734, #1136, #19474 ) ;
#16568=ORIENTED_EDGE ( 'NONE', *, *, #16793, .F. ) ;
#16569=AXIS2_PLACEMENT_3D ( 'NONE', #12602, #892, #17485 ) ;
#16574=EDGE_LOOP ( 'NONE', ( #1100, #7284, #20615, #2935 ) ) ;
#16576=ORIENTED_EDGE ( 'NONE', *, *, #7094, .T. ) ;
#16579=DIRECTION ( 'NONE',  ( -1.000000000000000000, -0.000000000000000000, -0.000000000000000000 ) ) ;
#16581=DIRECTION ( 'NONE',  ( 0.000000000000000000, -2.312964634635743213E-14, -1.000000000000000000 ) ) ;
#16582=VECTOR ( 'NONE', #16417, 1000.000000000000000 ) ;
#16584=CYLINDRICAL_SURFACE ( 'NONE', #3823, 45.00000000000000000 ) ;
#16587=LINE ( 'NONE', #4877, #2679 ) ;
#16588=ORIENTED_EDGE ( 'NONE', *, *, #20708, .T. ) ;
#16589=EDGE_CURVE ( 'NONE', #8158, #3795, #17542, .T. ) ;
#16592=VERTEX_POINT ( 'NONE', #7590 ) ;
#16594=CARTESIAN_POINT ( 'NONE',  ( 0.000000000000000000, -66.01871308925505843, 64.79170103522999113 ) ) ;
#16595=VERTEX_POINT ( 'NONE', #956 ) ;
#16596=ORIENTED_EDGE ( 'NONE', *, *, #16994, .T. ) ;
#16598=CARTESIAN_POINT ( 'NONE',  ( 0.000000000000000000, -60.65655256511276860, 59.63197188857500919 ) ) ;
#16601=LINE ( 'NONE', #8202, #6797 ) ;
#16602=DIRECTION ( 'NONE',  ( 0.000000000000000000, 0.000000000000000000, 1.000000000000000000 ) ) ;
#16603=DIRECTION ( 'NONE',  ( -1.000000000000000000, -0.000000000000000000, -0.000000000000000000 ) ) ;
#16604=CARTESIAN_POINT ( 'NONE',  ( 0.000000000000000000, 0.000000000000000000, 0.000000000000000000 ) ) ;
#16606=DIRECTION ( 'NONE',  ( 0.000000000000000000, 0.6427876096865353661, 0.7660444431189813441 ) ) ;
#16607=DIRECTION ( 'NONE',  ( 1.000000000000000000, -0.000000000000000000, -0.000000000000000000 ) ) ;
#16609=EDGE_CURVE ( 'NONE', #2662, #3420, #4381, .T. ) ;
#16610=EDGE_CURVE ( 'NONE', #10503, #3599, #4417, .T. ) ;
#16615=CYLINDRICAL_SURFACE ( 'NONE', #20808, 92.50100000000000477 ) ;
#16617=AXIS2_PLACEMENT_3D ( 'NONE', #3260, #8464, #9992 ) ;
#16622=EDGE_CURVE ( 'NONE', #12772, #18178, #16421, .T. ) ;
#16623=VERTEX_POINT ( 'NONE', #14211 ) ;
#16624=DIRECTION ( 'NONE',  ( 0.000000000000000000, 0.000000000000000000, 1.000000000000000000 ) ) ;
#16626=ORIENTED_EDGE ( 'NONE', *, *, #4059, .T. ) ;
#16629=LINE ( 'NONE', #20057, #3010 ) ;
#16630=VERTEX_POINT ( 'NONE', #14111 ) ;
#16632=DIRECTION ( 'NONE',  ( 0.000000000000000000, 0.000000000000000000, 1.000000000000000000 ) ) ;
#16633=CARTESIAN_POINT ( 'NONE',  ( 0.000000000000000000, -41.89587599971600440, 77.38692120905457728 ) ) ;
#16634=DIRECTION ( 'NONE',  ( 0.000000000000000000, 0.000000000000000000, 1.000000000000000000 ) ) ;
#16635=CARTESIAN_POINT ( 'NONE',  ( 10.00000000000000000, -81.55207211302094095, 24.17537951050038814 ) ) ;
#16637=DIRECTION ( 'NONE',  ( 1.000000000000000000, 0.000000000000000000, 0.000000000000000000 ) ) ;
#16638=VERTEX_POINT ( 'NONE', #7807 ) ;
#16639=CARTESIAN_POINT ( 'NONE',  ( 10.00000000000000000, -57.47876254627099257, -62.70072803846446163 ) ) ;
#16640=EDGE_CURVE ( 'NONE', #8199, #8870, #2723, .T. ) ;
#16641=CARTESIAN_POINT ( 'NONE',  ( 10.00000000000000000, 8.134922360107273320, -84.67002113262471141 ) ) ;
#16643=FACE_OUTER_BOUND ( 'NONE', #1950, .T. ) ;
#16647=ORIENTED_EDGE ( 'NONE', *, *, #2861, .F. ) ;
#16649=EDGE_LOOP ( 'NONE', ( #1707, #5490, #10302, #11688 ) ) ;
#16650=ORIENTED_EDGE ( 'NONE', *, *, #3710, .T. ) ;
#16654=DIRECTION ( 'NONE',  ( 0.000000000000000000, 0.1391731009600591928, 0.9902680687415711391 ) ) ;
#16657=DIRECTION ( 'NONE',  ( -1.000000000000000000, -0.000000000000000000, -0.000000000000000000 ) ) ;
#16658=EDGE_CURVE ( 'NONE', #797, #6729, #14298, .T. ) ;
#16660=ADVANCED_FACE ( 'NONE', ( #19513 ), #7384, .F. ) ;
#16662=CARTESIAN_POINT ( 'NONE',  ( 0.000000000000000000, -75.27139873020921357, 53.76477968147791131 ) ) ;
#16664=CIRCLE ( 'NONE', #2535, 44.99999999999998579 ) ;
#16669=DIRECTION ( 'NONE',  ( -1.000000000000000000, -0.000000000000000000, 0.000000000000000000 ) ) ;
#16671=ORIENTED_EDGE ( 'NONE', *, *, #14596, .T. ) ;
#16674=ORIENTED_EDGE ( 'NONE', *, *, #56, .F. ) ;
#16675=LINE ( 'NONE', #21648, #2411 ) ;
#16677=DIRECTION ( 'NONE',  ( -1.000000000000000000, -0.000000000000000000, -0.000000000000000000 ) ) ;
#16680=DIRECTION ( 'NONE',  ( -1.000000000000000000, -0.000000000000000000, -0.000000000000000000 ) ) ;
#16682=LINE ( 'NONE', #7965, #11891 ) ;
#16683=DIRECTION ( 'NONE',  ( 0.000000000000000000, -0.6427876096865458022, 0.7660444431189725734 ) ) ;
#16684=CIRCLE ( 'NONE', #3285, 44.99999999999998579 ) ;
#16686=CARTESIAN_POINT ( 'NONE',  ( 10.00000000000000000, -74.74361964203200159, -40.60271866773624083 ) ) ;
#16687=AXIS2_PLACEMENT_3D ( 'NONE', #15132, #15026, #10162 ) ;
#16689=ORIENTED_EDGE ( 'NONE', *, *, #9175, .T. ) ;
#16690=CIRCLE ( 'NONE', #20580, 45.00000000000000711 ) ;
#16693=VERTEX_POINT ( 'NONE', #11331 ) ;
#16694=DIRECTION ( 'NONE',  ( 0.000000000000000000, 0.000000000000000000, -1.000000000000000000 ) ) ;
#16696=ORIENTED_EDGE ( 'NONE', *, *, #20149, .F. ) ;
#16698=AXIS2_PLACEMENT_3D ( 'NONE', #5061, #11798, #16560 ) ;
#16700=EDGE_CURVE ( 'NONE', #12429, #6477, #205, .T. ) ;
#16701=CARTESIAN_POINT ( 'NONE',  ( 0.000000000000000000, -36.60317927562628881, 76.78148674856751654 ) ) ;
#16703=AXIS2_PLACEMENT_3D ( 'NONE', #7025, #8781, #5255 ) ;
#16704=DIRECTION ( 'NONE',  ( 0.000000000000000000, 0.000000000000000000, 1.000000000000000000 ) ) ;
#16708=AXIS2_PLACEMENT_3D ( 'NONE', #19469, #17822, #7773 ) ;
#16709=CARTESIAN_POINT ( 'NONE',  ( 10.00000000000000000, -84.90234713953981327, -5.175025661884713912 ) ) ;
#16710=DIRECTION ( 'NONE',  ( 0.000000000000000000, 0.6946583704589984753, -0.7193398003386500816 ) ) ;
#16711=CYLINDRICAL_SURFACE ( 'NONE', #5942, 92.50100000000000477 ) ;
#16713=AXIS2_PLACEMENT_3D ( 'NONE', #16635, #13426, #4698 ) ;
#16716=AXIS2_PLACEMENT_3D ( 'NONE', #11529, #14838, #11305 ) ;
#16717=CARTESIAN_POINT ( 'NONE',  ( 0.000000000000000000, 0.000000000000000000, 0.000000000000000000 ) ) ;
#16719=CARTESIAN_POINT ( 'NONE',  ( 0.000000000000000000, 67.05625154133539922, -63.71729851637743280 ) ) ;
#16720=VERTEX_POINT ( 'NONE', #21515 ) ;
#16721=CIRCLE ( 'NONE', #9644, 44.99999999999998579 ) ;
#16723=ORIENTED_EDGE ( 'NONE', *, *, #2716, .T. ) ;
#16725=ORIENTED_EDGE ( 'NONE', *, *, #8200, .T. ) ;
#16726=EDGE_CURVE ( 'NONE', #1655, #1066, #11830, .T. ) ;
#16730=ORIENTED_EDGE ( 'NONE', *, *, #8306, .F. ) ;
#16732=CARTESIAN_POINT ( 'NONE',  ( 0.000000000000000000, 56.34908017029559346, 63.71789861856471049 ) ) ;
#16733=CARTESIAN_POINT ( 'NONE',  ( 10.00000000000000000, -68.93609746931124960, -54.69748134696530428 ) ) ;
#16735=DIRECTION ( 'NONE',  ( -1.000000000000000000, 0.000000000000000000, -0.000000000000000000 ) ) ;
#16736=CARTESIAN_POINT ( 'NONE',  ( 0.000000000000000000, 10.41137886060106865, 91.91321010181850681 ) ) ;
#16738=CIRCLE ( 'NONE', #3335, 88.00000000000000000 ) ;
#16739=DIRECTION ( 'NONE',  ( 0.000000000000000000, 0.8987940462991680368, -0.4383711467890751279 ) ) ;
#16741=CARTESIAN_POINT ( 'NONE',  ( 10.00000000000000000, 68.36541360927260769, -50.60987712331631627 ) ) ;
#16742=VERTEX_POINT ( 'NONE', #2836 ) ;
#16743=EDGE_CURVE ( 'NONE', #12032, #15273, #3706, .T. ) ;
#16745=ORIENTED_EDGE ( 'NONE', *, *, #18671, .F. ) ;
#16747=DIRECTION ( 'NONE',  ( 1.000000000000000000, 0.000000000000000000, 0.000000000000000000 ) ) ;
#16748=AXIS2_PLACEMENT_3D ( 'NONE', #9168, #20678, #2329 ) ;
#16752=CARTESIAN_POINT ( 'NONE',  ( 0.000000000000000000, 27.87320266523671819, -88.20158487341731757 ) ) ;
#16753=AXIS2_PLACEMENT_3D ( 'NONE', #1822, #1716, #8558 ) ;
#16755=ADVANCED_FACE ( 'NONE', ( #9663 ), #8144, .F. ) ;
#16757=EDGE_CURVE ( 'NONE', #14363, #16630, #5134, .T. ) ;
#16758=EDGE_LOOP ( 'NONE', ( #2406, #14860, #15390, #8971 ) ) ;
#16759=EDGE_CURVE ( 'NONE', #10503, #5372, #9698, .T. ) ;
#16763=CARTESIAN_POINT ( 'NONE',  ( 5.000000000000000000, -47.19205848891713373, -74.27590198428171675 ) ) ;
#16766=FACE_OUTER_BOUND ( 'NONE', #4533, .T. ) ;
#16767=FACE_OUTER_BOUND ( 'NONE', #13379, .T. ) ;
#16768=DIRECTION ( 'NONE',  ( 1.000000000000000000, 0.000000000000000000, 0.000000000000000000 ) ) ;
#16769=AXIS2_PLACEMENT_3D ( 'NONE', #2503, #11231, #17985 ) ;
#16771=VECTOR ( 'NONE', #15385, 1000.000000000000000 ) ;
#16773=CARTESIAN_POINT ( 'NONE',  ( 10.00000000000000000, 0.000000000000000000, 0.000000000000000000 ) ) ;
#16774=EDGE_CURVE ( 'NONE', #447, #17747, #16049, .T. ) ;
#16775=CIRCLE ( 'NONE', #17127, 92.50100000000000477 ) ;
#16776=DIRECTION ( 'NONE',  ( -1.000000000000000000, -0.000000000000000000, 0.000000000000000000 ) ) ;
#16777=ADVANCED_FACE ( 'NONE', ( #4824 ), #6603, .F. ) ;
#16778=ADVANCED_FACE ( 'NONE', ( #12995 ), #3267, .F. ) ;
#16779=CARTESIAN_POINT ( 'NONE',  ( 0.000000000000000000, 5.479102470011647519, -87.82926298292107958 ) ) ;
#16783=VECTOR ( 'NONE', #16961, 1000.000000000000000 ) ;
#16785=EDGE_CURVE ( 'NONE', #8011, #9734, #14320, .T. ) ;
#16786=VERTEX_POINT ( 'NONE', #6718 ) ;
#16787=VERTEX_POINT ( 'NONE', #1174 ) ;
#16788=VECTOR ( 'NONE', #7242, 1000.000000000000000 ) ;
#16789=AXIS2_PLACEMENT_3D ( 'NONE', #17294, #2144, #8877 ) ;
#16792=DIRECTION ( 'NONE',  ( 0.000000000000000000, -1.079383496163346864E-14, -1.000000000000000000 ) ) ;
#16793=EDGE_CURVE ( 'NONE', #8475, #8452, #11504, .T. ) ;
#16795=DIRECTION ( 'NONE',  ( 0.000000000000000000, 0.06975647374411846069, 0.9975640502598246417 ) ) ;
#16796=LINE ( 'NONE', #107, #9971 ) ;
#16801=DIRECTION ( 'NONE',  ( 0.000000000000000000, 0.000000000000000000, -1.000000000000000000 ) ) ;
#16803=ORIENTED_EDGE ( 'NONE', *, *, #8959, .T. ) ;
#16805=AXIS2_PLACEMENT_3D ( 'NONE', #6355, #9525, #16273 ) ;
#16807=CIRCLE ( 'NONE', #14642, 44.99999999999999289 ) ;
#16808=VERTEX_POINT ( 'NONE', #20177 ) ;
#16809=EDGE_CURVE ( 'NONE', #14602, #20731, #691, .T. ) ;
#16810=ORIENTED_EDGE ( 'NONE', *, *, #18011, .T. ) ;
#16813=DIRECTION ( 'NONE',  ( -1.000000000000000000, 0.000000000000000000, 0.000000000000000000 ) ) ;
#16817=DIRECTION ( 'NONE',  ( -1.000000000000000000, -0.000000000000000000, -0.000000000000000000 ) ) ;
#16818=ORIENTED_EDGE ( 'NONE', *, *, #9760, .F. ) ;
#16820=AXIS2_PLACEMENT_3D ( 'NONE', #9385, #7753, #17589 ) ;
#16822=DIRECTION ( 'NONE',  ( 0.000000000000000000, -0.2756373558169870064, -0.9612616959383222248 ) ) ;
#16823=CARTESIAN_POINT ( 'NONE',  ( 10.00000000000000000, -52.34334029047928993, 76.26670130689468863 ) ) ;
#16825=CARTESIAN_POINT ( 'NONE',  ( 0.000000000000000000, -82.02147376274642454, -42.76579056660944644 ) ) ;
#16826=FACE_OUTER_BOUND ( 'NONE', #18767, .T. ) ;
#16827=CARTESIAN_POINT ( 'NONE',  ( 0.000000000000000000, -43.18649929580243452, 73.28107340219401067 ) ) ;
#16828=EDGE_LOOP ( 'NONE', ( #19695, #6176, #17936, #7774 ) ) ;
#16833=CARTESIAN_POINT ( 'NONE',  ( 5.000000000000000000, 83.89484365856912973, 26.56417150042976161 ) ) ;
#16834=ORIENTED_EDGE ( 'NONE', *, *, #2017, .F. ) ;
#16835=CARTESIAN_POINT ( 'NONE',  ( 5.000000000000000000, -78.80192417387900150, -39.16958956249377621 ) ) ;
#16836=ORIENTED_EDGE ( 'NONE', *, *, #6760, .T. ) ;
#16839=DIRECTION ( 'NONE',  ( 0.000000000000000000, 0.000000000000000000, 1.000000000000000000 ) ) ;
#16840=VERTEX_POINT ( 'NONE', #13762 ) ;
#16841=ORIENTED_EDGE ( 'NONE', *, *, #12151, .F. ) ;
#16842=DIRECTION ( 'NONE',  ( -1.000000000000000000, 0.000000000000000000, -0.000000000000000000 ) ) ;
#16844=ORIENTED_EDGE ( 'NONE', *, *, #581, .T. ) ;
#16845=AXIS2_PLACEMENT_3D ( 'NONE', #9574, #9477, #21419 ) ;
#16846=DIRECTION ( 'NONE',  ( 1.000000000000000000, -0.000000000000000000, -0.000000000000000000 ) ) ;
#16847=CARTESIAN_POINT ( 'NONE',  ( 10.00000000000000000, 39.87723064937119233, 83.46401306393586594 ) ) ;
#16848=AXIS2_PLACEMENT_3D ( 'NONE', #19489, #11094, #4472 ) ;
#16850=DIRECTION ( 'NONE',  ( -1.000000000000000000, -0.000000000000000000, -0.000000000000000000 ) ) ;
#16852=DIRECTION ( 'NONE',  ( 1.000000000000000000, 0.000000000000000000, 0.000000000000000000 ) ) ;
#16854=ORIENTED_EDGE ( 'NONE', *, *, #5813, .F. ) ;
#16860=ORIENTED_EDGE ( 'NONE', *, *, #2482, .T. ) ;
#16863=VECTOR ( 'NONE', #1584, 1000.000000000000000 ) ;
#16864=CIRCLE ( 'NONE', #4167, 92.50100000000000477 ) ;
#16865=FACE_OUTER_BOUND ( 'NONE', #9945, .T. ) ;
#16866=AXIS2_PLACEMENT_3D ( 'NONE', #5003, #9964, #141 ) ;
#16868=EDGE_CURVE ( 'NONE', #5777, #16638, #4090, .T. ) ;
#16870=ORIENTED_EDGE ( 'NONE', *, *, #19732, .F. ) ;
#16871=ORIENTED_EDGE ( 'NONE', *, *, #13503, .T. ) ;
#16874=VERTEX_POINT ( 'NONE', #65 ) ;
#16876=EDGE_CURVE ( 'NONE', #4200, #5362, #13649, .T. ) ;
#16877=DIRECTION ( 'NONE',  ( 1.000000000000000000, 0.000000000000000000, 0.000000000000000000 ) ) ;
#16878=LINE ( 'NONE', #18862, #13556 ) ;
#16880=CARTESIAN_POINT ( 'NONE',  ( 0.000000000000000000, -14.02138820414853448, -83.89630571862299746 ) ) ;
#16881=FACE_OUTER_BOUND ( 'NONE', #672, .T. ) ;
#16882=CIRCLE ( 'NONE', #15105, 44.99999999999999289 ) ;
#16883=AXIS2_PLACEMENT_3D ( 'NONE', #2231, #15929, #10847 ) ;
#16884=CARTESIAN_POINT ( 'NONE',  ( 0.000000000000000000, 0.000000000000000000, 0.000000000000000000 ) ) ;
#16885=DIRECTION ( 'NONE',  ( 0.000000000000000000, 0.000000000000000000, 1.000000000000000000 ) ) ;
#16886=VECTOR ( 'NONE', #21037, 1000.000000000000000 ) ;
#16887=AXIS2_PLACEMENT_3D ( 'NONE', #18374, #3217, #16694 ) ;
#16888=AXIS2_PLACEMENT_3D ( 'NONE', #9275, #16025, #893 ) ;
#16889=CARTESIAN_POINT ( 'NONE',  ( 10.00000000000000000, 0.000000000000000000, 0.000000000000000000 ) ) ;
#16892=EDGE_CURVE ( 'NONE', #16010, #1387, #18218, .T. ) ;
#16897=FACE_OUTER_BOUND ( 'NONE', #21589, .T. ) ;
#16898=ORIENTED_EDGE ( 'NONE', *, *, #19492, .F. ) ;
#16899=DIRECTION ( 'NONE',  ( -1.000000000000000000, 0.000000000000000000, 0.000000000000000000 ) ) ;
#16900=ORIENTED_EDGE ( 'NONE', *, *, #16464, .T. ) ;
#16901=CIRCLE ( 'NONE', #21487, 44.99999999999998579 ) ;
#16902=ORIENTED_EDGE ( 'NONE', *, *, #13836, .T. ) ;
#16903=CIRCLE ( 'NONE', #8083, 92.50100000000000477 ) ;
#16904=AXIS2_PLACEMENT_3D ( 'NONE', #4057, #17546, #2401 ) ;
#16905=AXIS2_PLACEMENT_3D ( 'NONE', #18228, #13232, #12910 ) ;
#16906=ORIENTED_EDGE ( 'NONE', *, *, #11551, .T. ) ;
#16908=CYLINDRICAL_SURFACE ( 'NONE', #20426, 44.99999999999998579 ) ;
#16912=EDGE_CURVE ( 'NONE', #9256, #5435, #7620, .T. ) ;
#16913=DIRECTION ( 'NONE',  ( 0.000000000000000000, 0.7431448254773953543, -0.6691306063588567943 ) ) ;
#16914=CARTESIAN_POINT ( 'NONE',  ( 10.00000000000000000, 0.000000000000000000, 0.000000000000000000 ) ) ;
#16915=DIRECTION ( 'NONE',  ( 0.000000000000000000, 0.5299192642331999048, 0.8480480961564290654 ) ) ;
#16916=DIRECTION ( 'NONE',  ( 0.000000000000000000, 0.4067366430758011520, -0.9135454576426005335 ) ) ;
#16920=CIRCLE ( 'NONE', #8102, 44.99999999999999289 ) ;
#16921=ORIENTED_EDGE ( 'NONE', *, *, #12168, .T. ) ;
#16922=CIRCLE ( 'NONE', #3512, 45.00000000000000000 ) ;
#16925=ORIENTED_EDGE ( 'NONE', *, *, #2190, .T. ) ;
#16926=EDGE_LOOP ( 'NONE', ( #18762, #4769, #18829, #6311 ) ) ;
#16928=VERTEX_POINT ( 'NONE', #18740 ) ;
#16930=ORIENTED_EDGE ( 'NONE', *, *, #6404, .F. ) ;
#16931=VERTEX_POINT ( 'NONE', #5364 ) ;
#16932=CIRCLE ( 'NONE', #10569, 44.99999999999999289 ) ;
#16934=DIRECTION ( 'NONE',  ( 0.000000000000000000, 0.000000000000000000, 1.000000000000000000 ) ) ;
#16935=ORIENTED_EDGE ( 'NONE', *, *, #17211, .F. ) ;
#16939=CARTESIAN_POINT ( 'NONE',  ( 0.000000000000000000, 0.000000000000000000, 0.000000000000000000 ) ) ;
#16940=CARTESIAN_POINT ( 'NONE',  ( 10.00000000000000000, 0.000000000000000000, 0.000000000000000000 ) ) ;
#16942=FACE_OUTER_BOUND ( 'NONE', #14097, .T. ) ;
#16943=EDGE_CURVE ( 'NONE', #21704, #12864, #3997, .T. ) ;
#16944=EDGE_CURVE ( 'NONE', #1536, #13081, #18565, .T. ) ;
#16947=CARTESIAN_POINT ( 'NONE',  ( 0.000000000000000000, 81.55207211302045778, 24.17537951050201883 ) ) ;
#16951=CARTESIAN_POINT ( 'NONE',  ( 0.000000000000000000, 78.01214607583752070, 33.90124636420136994 ) ) ;
#16953=DIRECTION ( 'NONE',  ( 1.000000000000000000, 0.000000000000000000, 0.000000000000000000 ) ) ;
#16957=CARTESIAN_POINT ( 'NONE',  ( 10.00000000000000000, 56.34908017029559346, 63.71789861856471049 ) ) ;
#16958=ORIENTED_EDGE ( 'NONE', *, *, #276, .F. ) ;
#16960=CARTESIAN_POINT ( 'NONE',  ( 10.00000000000000000, 41.87002153499211232, -74.04114219178001122 ) ) ;
#16961=DIRECTION ( 'NONE',  ( 1.000000000000000000, -0.000000000000000000, -0.000000000000000000 ) ) ;
#16962=ORIENTED_EDGE ( 'NONE', *, *, #2818, .F. ) ;
#16967=LINE ( 'NONE', #6918, #2227 ) ;
#16968=DIRECTION ( 'NONE',  ( 0.000000000000000000, 0.000000000000000000, 1.000000000000000000 ) ) ;
#16969=ORIENTED_EDGE ( 'NONE', *, *, #19424, .F. ) ;
#16973=FACE_OUTER_BOUND ( 'NONE', #14935, .T. ) ;
#16974=ORIENTED_EDGE ( 'NONE', *, *, #837, .T. ) ;
#16975=FACE_OUTER_BOUND ( 'NONE', #16926, .T. ) ;
#16976=AXIS2_PLACEMENT_3D ( 'NONE', #18645, #3500, #12102 ) ;
#16979=CARTESIAN_POINT ( 'NONE',  ( 0.000000000000000000, -81.32027326007839463, -44.08455690949136851 ) ) ;
#16982=VERTEX_POINT ( 'NONE', #5886 ) ;
#16983=DIRECTION ( 'NONE',  ( -1.000000000000000000, -0.000000000000000000, -0.000000000000000000 ) ) ;
#16984=ORIENTED_EDGE ( 'NONE', *, *, #14355, .F. ) ;
#16985=CARTESIAN_POINT ( 'NONE',  ( 10.00000000000000000, 36.39558101400249512, -80.12091913260344711 ) ) ;
#16986=DIRECTION ( 'NONE',  ( 0.000000000000000000, 0.000000000000000000, 1.000000000000000000 ) ) ;
#16990=CARTESIAN_POINT ( 'NONE',  ( 10.00000000000000000, -6.797690662954623875, -87.73705831432221203 ) ) ;
#16994=EDGE_CURVE ( 'NONE', #4150, #8155, #11286, .T. ) ;
#16995=DIRECTION ( 'NONE',  ( 0.000000000000000000, 0.000000000000000000, 1.000000000000000000 ) ) ;
#16996=DIRECTION ( 'NONE',  ( 0.000000000000000000, 0.000000000000000000, 1.000000000000000000 ) ) ;
#17000=ORIENTED_EDGE ( 'NONE', *, *, #13888, .T. ) ;
#17004=CIRCLE ( 'NONE', #765, 88.00000000000000000 ) ;
#17006=ORIENTED_EDGE ( 'NONE', *, *, #21794, .T. ) ;
#17007=DIRECTION ( 'NONE',  ( 0.000000000000000000, -0.9271838545667908660, 0.3746065934159032440 ) ) ;
#17008=ORIENTED_EDGE ( 'NONE', *, *, #20850, .T. ) ;
#17009=CARTESIAN_POINT ( 'NONE',  ( 10.00000000000000000, 56.34908017029645322, -63.71789861856395731 ) ) ;
#17011=EDGE_CURVE ( 'NONE', #20811, #13006, #9717, .T. ) ;
#17015=DIRECTION ( 'NONE',  ( -1.000000000000000000, -0.000000000000000000, 0.000000000000000000 ) ) ;
#17016=DIRECTION ( 'NONE',  ( 1.000000000000000000, -0.000000000000000000, -0.000000000000000000 ) ) ;
#17018=DIRECTION ( 'NONE',  ( 0.000000000000000000, -0.06975647374411138302, -0.9975640502598251969 ) ) ;
#17020=DIRECTION ( 'NONE',  ( 1.000000000000000000, 0.000000000000000000, 0.000000000000000000 ) ) ;
#17023=ORIENTED_EDGE ( 'NONE', *, *, #7327, .F. ) ;
#17025=EDGE_CURVE ( 'NONE', #3881, #15140, #15016, .T. ) ;
#17026=LINE ( 'NONE', #5325, #17328 ) ;
#17028=ORIENTED_EDGE ( 'NONE', *, *, #4046, .F. ) ;
#17029=ORIENTED_EDGE ( 'NONE', *, *, #3840, .F. ) ;
#17030=VERTEX_POINT ( 'NONE', #4222 ) ;
#17031=AXIS2_PLACEMENT_3D ( 'NONE', #7827, #4192, #14676 ) ;
#17033=EDGE_CURVE ( 'NONE', #13577, #9520, #14703, .T. ) ;
#17035=ADVANCED_FACE ( 'NONE', ( #21446 ), #10952, .F. ) ;
#17037=EDGE_CURVE ( 'NONE', #2668, #9323, #10074, .T. ) ;
#17039=CARTESIAN_POINT ( 'NONE',  ( 10.00000000000000000, 70.37753541435941429, 60.02863908169658202 ) ) ;
#17040=CARTESIAN_POINT ( 'NONE',  ( 10.00000000000000000, 0.000000000000000000, 0.000000000000000000 ) ) ;
#17042=LINE ( 'NONE', #11965, #19185 ) ;
#17044=FACE_OUTER_BOUND ( 'NONE', #2822, .T. ) ;
#17046=ORIENTED_EDGE ( 'NONE', *, *, #19145, .T. ) ;
#17047=EDGE_CURVE ( 'NONE', #11398, #8996, #16066, .T. ) ;
#17049=CARTESIAN_POINT ( 'NONE',  ( 0.000000000000000000, 1.224646799147353217E-14, -100.0000000000000000 ) ) ;
#17053=DIRECTION ( 'NONE',  ( 1.000000000000000000, 0.000000000000000000, 0.000000000000000000 ) ) ;
#17055=EDGE_CURVE ( 'NONE', #15636, #2214, #6570, .T. ) ;
#17057=ORIENTED_EDGE ( 'NONE', *, *, #5006, .F. ) ;
#17060=VERTEX_POINT ( 'NONE', #19564 ) ;
#17061=ORIENTED_EDGE ( 'NONE', *, *, #16726, .T. ) ;
#17062=CYLINDRICAL_SURFACE ( 'NONE', #13574, 44.99999999999999289 ) ;
#17063=DIRECTION ( 'NONE',  ( 0.000000000000000000, 0.000000000000000000, 1.000000000000000000 ) ) ;
#17064=AXIS2_PLACEMENT_3D ( 'NONE', #20417, #16983, #15312 ) ;
#17065=ADVANCED_FACE ( 'NONE', ( #18140 ), #4439, .F. ) ;
#17067=DIRECTION ( 'NONE',  ( 0.000000000000000000, 0.000000000000000000, 1.000000000000000000 ) ) ;
#17068=DIRECTION ( 'NONE',  ( 0.000000000000000000, -0.9702957262759938084, -0.2419218955996777498 ) ) ;
#17070=LINE ( 'NONE', #3696, #2583 ) ;
#17071=DIRECTION ( 'NONE',  ( -1.000000000000000000, 0.000000000000000000, 0.000000000000000000 ) ) ;
#17073=ORIENTED_EDGE ( 'NONE', *, *, #8090, .F. ) ;
#17075=AXIS2_PLACEMENT_3D ( 'NONE', #21154, #2249, #6025 ) ;
#17077=VERTEX_POINT ( 'NONE', #7857 ) ;
#17082=LINE ( 'NONE', #10654, #13726 ) ;
#17083=ORIENTED_EDGE ( 'NONE', *, *, #17055, .T. ) ;
#17084=ADVANCED_FACE ( 'NONE', ( #14595 ), #12717, .F. ) ;
#17085=DIRECTION ( 'NONE',  ( 1.000000000000000000, 0.000000000000000000, 0.000000000000000000 ) ) ;
#17086=AXIS2_PLACEMENT_3D ( 'NONE', #18946, #20280, #11876 ) ;
#17089=ORIENTED_EDGE ( 'NONE', *, *, #20149, .T. ) ;
#17091=ORIENTED_EDGE ( 'NONE', *, *, #18787, .T. ) ;
#17093=DIRECTION ( 'NONE',  ( 1.000000000000000000, 0.000000000000000000, 0.000000000000000000 ) ) ;
#17094=DIRECTION ( 'NONE',  ( 0.000000000000000000, -0.9510565162951565288, 0.3090169943749382919 ) ) ;
#17095=DIRECTION ( 'NONE',  ( 0.000000000000000000, 0.000000000000000000, 1.000000000000000000 ) ) ;
#17097=LINE ( 'NONE', #3610, #2948 ) ;
#17099=LINE ( 'NONE', #5287, #11525 ) ;
#17102=VERTEX_POINT ( 'NONE', #8189 ) ;
#17103=DIRECTION ( 'NONE',  ( -1.000000000000000000, -0.000000000000000000, -0.000000000000000000 ) ) ;
#17105=AXIS2_PLACEMENT_3D ( 'NONE', #8711, #3945, #12019 ) ;
#17106=EDGE_CURVE ( 'NONE', #20086, #7542, #8088, .T. ) ;
#17111=VERTEX_POINT ( 'NONE', #6763 ) ;
#17112=CARTESIAN_POINT ( 'NONE',  ( 0.000000000000000000, 0.000000000000000000, 0.000000000000000000 ) ) ;
#17113=VECTOR ( 'NONE', #17773, 1000.000000000000000 ) ;
#17114=EDGE_LOOP ( 'NONE', ( #21591, #12869, #10202, #18122 ) ) ;
#17115=ORIENTED_EDGE ( 'NONE', *, *, #15435, .F. ) ;
#17117=EDGE_LOOP ( 'NONE', ( #3647, #14991, #16588, #1627 ) ) ;
#17118=DIRECTION ( 'NONE',  ( -1.000000000000000000, -0.000000000000000000, -0.000000000000000000 ) ) ;
#17119=CIRCLE ( 'NONE', #18180, 44.99999999999998579 ) ;
#17122=CARTESIAN_POINT ( 'NONE',  ( 5.000000000000000000, -47.19205848891816402, 74.27590198428104884 ) ) ;
#17125=VECTOR ( 'NONE', #7909, 1000.000000000000000 ) ;
#17127=AXIS2_PLACEMENT_3D ( 'NONE', #6122, #6568, #16822 ) ;
#17132=DIRECTION ( 'NONE',  ( -1.000000000000000000, 0.000000000000000000, 0.000000000000000000 ) ) ;
#17133=ORIENTED_EDGE ( 'NONE', *, *, #4791, .T. ) ;
#17136=CIRCLE ( 'NONE', #203, 44.99999999999999289 ) ;
#17138=ORIENTED_EDGE ( 'NONE', *, *, #21401, .T. ) ;
#17139=VECTOR ( 'NONE', #8654, 1000.000000000000000 ) ;
#17140=AXIS2_PLACEMENT_3D ( 'NONE', #1490, #8234, #18411 ) ;
#17141=VERTEX_POINT ( 'NONE', #13264 ) ;
#17143=CARTESIAN_POINT ( 'NONE',  ( 0.000000000000000000, 87.17509410653667601, -30.93441398372498341 ) ) ;
#17144=ORIENTED_EDGE ( 'NONE', *, *, #8792, .T. ) ;
#17148=ORIENTED_EDGE ( 'NONE', *, *, #1230, .F. ) ;
#17149=CYLINDRICAL_SURFACE ( 'NONE', #6452, 92.50100000000000477 ) ;
#17150=ADVANCED_FACE ( 'NONE', ( #6867 ), #9838, .F. ) ;
#17151=LINE ( 'NONE', #4895, #8308 ) ;
#17154=LINE ( 'NONE', #2013, #18936 ) ;
#17155=CIRCLE ( 'NONE', #14321, 45.00000000000000711 ) ;
#17156=CIRCLE ( 'NONE', #18921, 45.00000000000000000 ) ;
#17157=LINE ( 'NONE', #8751, #16072 ) ;
#17159=CARTESIAN_POINT ( 'NONE',  ( 10.00000000000000000, 0.000000000000000000, 0.000000000000000000 ) ) ;
#17162=ADVANCED_FACE ( 'NONE', ( #20127 ), #8516, .F. ) ;
#17165=CARTESIAN_POINT ( 'NONE',  ( 10.00000000000000000, 90.63195040374188238, 18.50093422002450083 ) ) ;
#17166=EDGE_CURVE ( 'NONE', #9664, #9397, #16453, .T. ) ;
#17167=DIRECTION ( 'NONE',  ( -1.000000000000000000, 0.000000000000000000, 0.000000000000000000 ) ) ;
#17170=VERTEX_POINT ( 'NONE', #6549 ) ;
#17172=AXIS2_PLACEMENT_3D ( 'NONE', #3099, #9828, #5495 ) ;
#17173=CARTESIAN_POINT ( 'NONE',  ( 10.00000000000000000, 89.12061559554365431, -24.77803214283454736 ) ) ;
#17174=ORIENTED_EDGE ( 'NONE', *, *, #18509, .T. ) ;
#17176=DIRECTION ( 'NONE',  ( 0.000000000000000000, 0.000000000000000000, 1.000000000000000000 ) ) ;
#17177=CARTESIAN_POINT ( 'NONE',  ( 10.00000000000000000, 86.77540292929722909, -14.62974526292624944 ) ) ;
#17178=EDGE_CURVE ( 'NONE', #18403, #9309, #11861, .T. ) ;
#17179=CARTESIAN_POINT ( 'NONE',  ( -10.00000000000000000, 0.000000000000000000, 0.000000000000000000 ) ) ;
#17181=LINE ( 'NONE', #10429, #18568 ) ;
#17182=CARTESIAN_POINT ( 'NONE',  ( 10.00000000000000000, -15.32665449651862843, -91.22241316115434984 ) ) ;
#17184=EDGE_CURVE ( 'NONE', #13006, #6332, #14683, .T. ) ;
#17185=CARTESIAN_POINT ( 'NONE',  ( 10.00000000000000000, 84.90234713953992696, -5.175025661882965089 ) ) ;
#17186=AXIS2_PLACEMENT_3D ( 'NONE', #14151, #19242, #10839 ) ;
#17187=AXIS2_PLACEMENT_3D ( 'NONE', #20062, #4930, #11664 ) ;
#17188=AXIS2_PLACEMENT_3D ( 'NONE', #9579, #2757, #16335 ) ;
#17191=CYLINDRICAL_SURFACE ( 'NONE', #1272, 44.99999999999998579 ) ;
#17193=CARTESIAN_POINT ( 'NONE',  ( 0.000000000000000000, 86.77540292929701593, 14.62974526292747868 ) ) ;
#17195=EDGE_CURVE ( 'NONE', #12538, #10938, #16587, .T. ) ;
#17196=DIRECTION ( 'NONE',  ( 0.000000000000000000, -0.8987940462991619306, -0.4383711467890878399 ) ) ;
#17198=ORIENTED_EDGE ( 'NONE', *, *, #8864, .F. ) ;
#17199=VECTOR ( 'NONE', #14351, 1000.000000000000000 ) ;
#17200=ORIENTED_EDGE ( 'NONE', *, *, #16079, .T. ) ;
#17201=ORIENTED_EDGE ( 'NONE', *, *, #10388, .T. ) ;
#17204=VECTOR ( 'NONE', #4462, 1000.000000000000000 ) ;
#17205=ORIENTED_EDGE ( 'NONE', *, *, #10788, .F. ) ;
#17206=CARTESIAN_POINT ( 'NONE',  ( 0.000000000000000000, -3.728035544475628793, -84.97818067823773447 ) ) ;
#17207=EDGE_CURVE ( 'NONE', #13321, #2883, #14337, .T. ) ;
#17208=DIRECTION ( 'NONE',  ( 0.000000000000000000, 0.000000000000000000, 1.000000000000000000 ) ) ;
#17209=DIRECTION ( 'NONE',  ( -1.000000000000000000, -0.000000000000000000, -0.000000000000000000 ) ) ;
#17210=DIRECTION ( 'NONE',  ( 0.000000000000000000, -0.9271838545667908660, 0.3746065934159032440 ) ) ;
#17211=EDGE_CURVE ( 'NONE', #12634, #17141, #15742, .T. ) ;
#17214=DIRECTION ( 'NONE',  ( 1.000000000000000000, 0.000000000000000000, 0.000000000000000000 ) ) ;
#17215=EDGE_CURVE ( 'NONE', #1305, #4587, #12566, .T. ) ;
#17221=AXIS2_PLACEMENT_3D ( 'NONE', #6932, #2154, #5366 ) ;
#17222=CIRCLE ( 'NONE', #981, 92.50100000000000477 ) ;
#17223=CIRCLE ( 'NONE', #12269, 44.99999999999998579 ) ;
#17227=VERTEX_POINT ( 'NONE', #20350 ) ;
#17228=DIRECTION ( 'NONE',  ( -1.000000000000000000, 0.000000000000000000, 0.000000000000000000 ) ) ;
#17231=VERTEX_POINT ( 'NONE', #11507 ) ;
#17232=FACE_OUTER_BOUND ( 'NONE', #21267, .T. ) ;
#17234=AXIS2_PLACEMENT_3D ( 'NONE', #20818, #2685, #9408 ) ;
#17235=CARTESIAN_POINT ( 'NONE',  ( 10.00000000000000000, 84.79630770241084292, -6.691460262315676033 ) ) ;
#17239=DIRECTION ( 'NONE',  ( 0.000000000000000000, -0.5299192642331944647, -0.8480480961564325071 ) ) ;
#17240=DIRECTION ( 'NONE',  ( 0.000000000000000000, 0.000000000000000000, 1.000000000000000000 ) ) ;
#17242=CYLINDRICAL_SURFACE ( 'NONE', #19923, 92.50100000000000477 ) ;
#17243=DIRECTION ( 'NONE',  ( 0.000000000000000000, 0.000000000000000000, 1.000000000000000000 ) ) ;
#17244=CARTESIAN_POINT ( 'NONE',  ( 10.00000000000000000, 0.000000000000000000, 0.000000000000000000 ) ) ;
#17246=CARTESIAN_POINT ( 'NONE',  ( 0.000000000000000000, -91.70173545986527586, 12.13370160540012499 ) ) ;
#17247=AXIS2_PLACEMENT_3D ( 'NONE', #8722, #2189, #10693 ) ;
#17248=ORIENTED_EDGE ( 'NONE', *, *, #6678, .T. ) ;
#17251=AXIS2_PLACEMENT_3D ( 'NONE', #5892, #17707, #12615 ) ;
#17252=AXIS2_PLACEMENT_3D ( 'NONE', #18948, #2044, #20396 ) ;
#17254=ORIENTED_EDGE ( 'NONE', *, *, #21763, .F. ) ;
#17255=CARTESIAN_POINT ( 'NONE',  ( 5.000000000000002665, -18.94217447942501309, -85.93715160505971085 ) ) ;
#17256=ORIENTED_EDGE ( 'NONE', *, *, #19730, .F. ) ;
#17257=ORIENTED_EDGE ( 'NONE', *, *, #1537, .F. ) ;
#17259=ORIENTED_EDGE ( 'NONE', *, *, #18911, .T. ) ;
#17261=CARTESIAN_POINT ( 'NONE',  ( 0.000000000000000000, -11.59241532900687233, 87.23311244498734141 ) ) ;
#17262=CARTESIAN_POINT ( 'NONE',  ( 10.00000000000000000, 0.000000000000000000, 0.000000000000000000 ) ) ;
#17263=CIRCLE ( 'NONE', #2426, 44.99999999999999289 ) ;
#17265=CARTESIAN_POINT ( 'NONE',  ( 10.00000000000000000, -87.58454185039434492, -8.540961822682595184 ) ) ;
#17266=EDGE_CURVE ( 'NONE', #7559, #5754, #15384, .T. ) ;
#17267=AXIS2_PLACEMENT_3D ( 'NONE', #11453, #5163, #21835 ) ;
#17272=FACE_OUTER_BOUND ( 'NONE', #1861, .T. ) ;
#17274=EDGE_CURVE ( 'NONE', #16592, #8708, #13260, .T. ) ;
#17276=AXIS2_PLACEMENT_3D ( 'NONE', #17206, #2068, #8804 ) ;
#17278=ORIENTED_EDGE ( 'NONE', *, *, #21533, .F. ) ;
#17281=CARTESIAN_POINT ( 'NONE',  ( 0.000000000000000000, 0.000000000000000000, 0.000000000000000000 ) ) ;
#17282=AXIS2_PLACEMENT_3D ( 'NONE', #16889, #1751, #1968 ) ;
#17283=ORIENTED_EDGE ( 'NONE', *, *, #18097, .F. ) ;
#17285=CARTESIAN_POINT ( 'NONE',  ( 10.00000000000000000, 78.83848282823907994, 48.38314403117527718 ) ) ;
#17289=DIRECTION ( 'NONE',  ( -1.000000000000000000, -0.000000000000000000, -0.000000000000000000 ) ) ;
#17293=EDGE_CURVE ( 'NONE', #1439, #9851, #5322, .T. ) ;
#17294=CARTESIAN_POINT ( 'NONE',  ( 0.000000000000000000, -48.19312842678424857, -70.09002648625245513 ) ) ;
#17297=CARTESIAN_POINT ( 'NONE',  ( 5.000000000000000000, 60.65279801375431390, -63.75921967137554702 ) ) ;
#17298=LINE ( 'NONE', #2149, #9929 ) ;
#17299=EDGE_CURVE ( 'NONE', #12008, #5370, #7301, .T. ) ;
#17301=ORIENTED_EDGE ( 'NONE', *, *, #4247, .F. ) ;
#17302=DIRECTION ( 'NONE',  ( 0.000000000000000000, 0.8987940462991651502, 0.4383711467890813451 ) ) ;
#17304=DIRECTION ( 'NONE',  ( 0.000000000000000000, 0.000000000000000000, 1.000000000000000000 ) ) ;
#17305=ADVANCED_FACE ( 'NONE', ( #6981 ), #10380, .F. ) ;
#17306=ORIENTED_EDGE ( 'NONE', *, *, #1379, .T. ) ;
#17308=LINE ( 'NONE', #19068, #1742 ) ;
#17310=EDGE_CURVE ( 'NONE', #14140, #13603, #7990, .T. ) ;
#17311=VERTEX_POINT ( 'NONE', #5423 ) ;
#17312=ORIENTED_EDGE ( 'NONE', *, *, #20574, .F. ) ;
#17313=ORIENTED_EDGE ( 'NONE', *, *, #10714, .T. ) ;
#17314=AXIS2_PLACEMENT_3D ( 'NONE', #11512, #18586, #3442 ) ;
#17315=DIRECTION ( 'NONE',  ( -1.000000000000000000, -0.000000000000000000, 0.000000000000000000 ) ) ;
#17317=DIRECTION ( 'NONE',  ( 1.000000000000000000, 0.000000000000000000, 0.000000000000000000 ) ) ;
#17319=CYLINDRICAL_SURFACE ( 'NONE', #3709, 88.00000000000000000 ) ;
#17320=EDGE_CURVE ( 'NONE', #2139, #14884, #10087, .T. ) ;
#17322=LINE ( 'NONE', #5383, #7478 ) ;
#17324=CARTESIAN_POINT ( 'NONE',  ( 10.00000000000000000, 61.33825423015685629, 69.23910433415966281 ) ) ;
#17325=ORIENTED_EDGE ( 'NONE', *, *, #11893, .F. ) ;
#17327=DIRECTION ( 'NONE',  ( -1.000000000000000000, 0.000000000000000000, -0.000000000000000000 ) ) ;
#17328=VECTOR ( 'NONE', #20561, 1000.000000000000000 ) ;
#17329=DIRECTION ( 'NONE',  ( 0.000000000000000000, 1.680754301168640043E-14, -1.000000000000000000 ) ) ;
#17331=ORIENTED_EDGE ( 'NONE', *, *, #14224, .T. ) ;
#17333=VERTEX_POINT ( 'NONE', #17246 ) ;
#17334=DIRECTION ( 'NONE',  ( -1.000000000000000000, 0.000000000000000000, 0.000000000000000000 ) ) ;
#17337=VERTEX_POINT ( 'NONE', #3759 ) ;
#17339=CARTESIAN_POINT ( 'NONE',  ( 0.000000000000000000, 23.10190250628953379, -89.56973317806578905 ) ) ;
#17341=ORIENTED_EDGE ( 'NONE', *, *, #1587, .T. ) ;
#17343=CARTESIAN_POINT ( 'NONE',  ( 10.00000000000000000, 27.00677879429026618, 80.65868421664441712 ) ) ;
#17344=DIRECTION ( 'NONE',  ( 1.000000000000000000, 0.000000000000000000, 0.000000000000000000 ) ) ;
#17345=DIRECTION ( 'NONE',  ( 0.000000000000000000, 0.000000000000000000, 1.000000000000000000 ) ) ;
#17346=FACE_OUTER_BOUND ( 'NONE', #10915, .T. ) ;
#17348=CARTESIAN_POINT ( 'NONE',  ( 0.000000000000000000, -11.59241532900569993, -87.23311244498751194 ) ) ;
#17349=DIRECTION ( 'NONE',  ( 0.000000000000000000, 0.000000000000000000, 1.000000000000000000 ) ) ;
#17351=DIRECTION ( 'NONE',  ( 1.000000000000000000, 0.000000000000000000, 0.000000000000000000 ) ) ;
#17353=DIRECTION ( 'NONE',  ( 0.000000000000000000, -0.8660254037844432595, 0.4999999999999919509 ) ) ;
#17357=VERTEX_POINT ( 'NONE', #3873 ) ;
#17360=ORIENTED_EDGE ( 'NONE', *, *, #11742, .F. ) ;
#17361=EDGE_CURVE ( 'NONE', #13595, #13159, #4819, .T. ) ;
#17363=ORIENTED_EDGE ( 'NONE', *, *, #19051, .F. ) ;
#17365=CARTESIAN_POINT ( 'NONE',  ( 10.00000000000000000, 0.000000000000000000, 0.000000000000000000 ) ) ;
#17366=DIRECTION ( 'NONE',  ( -1.000000000000000000, 0.000000000000000000, 0.000000000000000000 ) ) ;
#17367=DIRECTION ( 'NONE',  ( -1.000000000000000000, 0.000000000000000000, 0.000000000000000000 ) ) ;
#17368=DIRECTION ( 'NONE',  ( -1.000000000000000000, 0.000000000000000000, -0.000000000000000000 ) ) ;
#17369=DIRECTION ( 'NONE',  ( -1.000000000000000000, -0.000000000000000000, -0.000000000000000000 ) ) ;
#17373=VERTEX_POINT ( 'NONE', #20874 ) ;
#17374=VECTOR ( 'NONE', #7745, 1000.000000000000000 ) ;
#17375=LINE ( 'NONE', #5774, #20072 ) ;
#17377=ORIENTED_EDGE ( 'NONE', *, *, #14328, .F. ) ;
#17378=ADVANCED_FACE ( 'NONE', ( #5747 ), #12472, .F. ) ;
#17379=CARTESIAN_POINT ( 'NONE',  ( 5.000000000000000000, 30.71797041605808687, 82.46457599186561538 ) ) ;
#17380=ORIENTED_EDGE ( 'NONE', *, *, #13640, .F. ) ;
#17383=CIRCLE ( 'NONE', #1514, 88.00000000000000000 ) ;
#17385=EDGE_LOOP ( 'NONE', ( #19298, #5296, #20297, #16338 ) ) ;
#17389=AXIS2_PLACEMENT_3D ( 'NONE', #16018, #7635, #14372 ) ;
#17390=CIRCLE ( 'NONE', #2919, 88.00000000000000000 ) ;
#17391=DIRECTION ( 'NONE',  ( 0.000000000000000000, 0.000000000000000000, 1.000000000000000000 ) ) ;
#17394=DIRECTION ( 'NONE',  ( 1.000000000000000000, 0.000000000000000000, 0.000000000000000000 ) ) ;
#17395=AXIS2_PLACEMENT_3D ( 'NONE', #12117, #15323, #13996 ) ;
#17397=DIRECTION ( 'NONE',  ( -1.000000000000000000, 0.000000000000000000, 0.000000000000000000 ) ) ;
#17399=EDGE_LOOP ( 'NONE', ( #19092, #14706, #17727, #16689 ) ) ;
#17401=CIRCLE ( 'NONE', #7873, 88.00000000000000000 ) ;
#17404=ORIENTED_EDGE ( 'NONE', *, *, #7088, .F. ) ;
#17405=AXIS2_PLACEMENT_3D ( 'NONE', #7236, #9200, #3914 ) ;
#17407=EDGE_CURVE ( 'NONE', #659, #13715, #21042, .T. ) ;
#17409=ORIENTED_EDGE ( 'NONE', *, *, #567, .F. ) ;
#17410=AXIS2_PLACEMENT_3D ( 'NONE', #8453, #15177, #13517 ) ;
#17411=EDGE_LOOP ( 'NONE', ( #6727, #13272, #17028, #10031 ) ) ;
#17415=EDGE_LOOP ( 'NONE', ( #3897, #559, #4365, #9159 ) ) ;
#17417=CARTESIAN_POINT ( 'NONE',  ( 10.00000000000000000, -87.96697768756403946, 2.410567674970269358 ) ) ;
#17418=LINE ( 'NONE', #1846, #14035 ) ;
#17419=DIRECTION ( 'NONE',  ( 1.000000000000000000, 0.000000000000000000, 0.000000000000000000 ) ) ;
#17422=EDGE_CURVE ( 'NONE', #733, #9395, #2639, .T. ) ;
#17423=CIRCLE ( 'NONE', #9639, 44.99999999999999289 ) ;
#17424=FACE_OUTER_BOUND ( 'NONE', #1403, .T. ) ;
#17425=VERTEX_POINT ( 'NONE', #872 ) ;
#17427=EDGE_CURVE ( 'NONE', #20567, #8545, #7637, .T. ) ;
#17430=CARTESIAN_POINT ( 'NONE',  ( 10.00000000000000000, 0.000000000000000000, 0.000000000000000000 ) ) ;
#17431=VERTEX_POINT ( 'NONE', #7732 ) ;
#17435=EDGE_CURVE ( 'NONE', #18093, #6084, #909, .T. ) ;
#17437=EDGE_LOOP ( 'NONE', ( #11136, #3307, #3714, #17089 ) ) ;
#17439=ORIENTED_EDGE ( 'NONE', *, *, #21201, .T. ) ;
#17440=CIRCLE ( 'NONE', #2620, 88.00000000000000000 ) ;
#17442=ORIENTED_EDGE ( 'NONE', *, *, #18164, .F. ) ;
#17444=DIRECTION ( 'NONE',  ( 0.000000000000000000, 0.5877852522924689183, 0.8090169943749504489 ) ) ;
#17445=VECTOR ( 'NONE', #20164, 1000.000000000000000 ) ;
#17447=CARTESIAN_POINT ( 'NONE',  ( 0.000000000000000000, -61.60362715318993310, -62.84101464466307618 ) ) ;
#17449=LINE ( 'NONE', #11020, #871 ) ;
#17450=DIRECTION ( 'NONE',  ( 0.000000000000000000, 0.9510565162951544194, -0.3090169943749450643 ) ) ;
#17451=CARTESIAN_POINT ( 'NONE',  ( 0.000000000000000000, 0.000000000000000000, 0.000000000000000000 ) ) ;
#17452=ADVANCED_FACE ( 'NONE', ( #7507 ), #14566, .F. ) ;
#17453=AXIS2_PLACEMENT_3D ( 'NONE', #5470, #10540, #15616 ) ;
#17458=EDGE_CURVE ( 'NONE', #6503, #21168, #15406, .T. ) ;
#17459=CARTESIAN_POINT ( 'NONE',  ( 10.00000000000000000, 30.71797041605924505, -82.46457599186518905 ) ) ;
#17460=AXIS2_PLACEMENT_3D ( 'NONE', #10747, #15732, #3906 ) ;
#17462=AXIS2_PLACEMENT_3D ( 'NONE', #15610, #12620, #17176 ) ;
#17463=ADVANCED_FACE ( 'NONE', ( #19771 ), #4634, .F. ) ;
#17465=ORIENTED_EDGE ( 'NONE', *, *, #20629, .F. ) ;
#17466=EDGE_LOOP ( 'NONE', ( #19836, #2269, #20269, #16902 ) ) ;
#17467=EDGE_LOOP ( 'NONE', ( #613, #2489, #9057, #16144 ) ) ;
#17468=DIRECTION ( 'NONE',  ( 0.000000000000000000, -0.5299192642331944647, -0.8480480961564325071 ) ) ;
#17469=VECTOR ( 'NONE', #6241, 1000.000000000000000 ) ;
#17470=ADVANCED_FACE ( 'NONE', ( #7618 ), #4197, .F. ) ;
#17471=EDGE_LOOP ( 'NONE', ( #5422, #7060, #12331, #673, #3576, #3035, #21403, #1175, #18650, #2704, #18084, #19271, #18001, #3502, #12355, #13800, #21245, #3194, #1155, #1723, #21698, #21525, #444, #2150, #2530, #16723, #10151, #676, #17655, #19498, #14821, #3280, #11753, #13760, #15223, #3195, #19667, #18456, #10522, #11566, #9427, #21774, #21389, #15207, #1215, #14949, #2866, #12222, #12446, #13646, #11597, #11390, #8579, #8479, #13131, #15081, #8528, #3052, #9816, #12471, #12328, #4639, #17963, #6852, #16073, #4510, #20992, #1568, #2048, #10054, #10828, #5092, #4921, #21807, #13455, #7470, #16512, #7914, #7276, #18020, #2727, #2800, #5349, #2995, #9166, #21051, #20515, #19932, #4162, #12351, #17198, #13921, #8496, #20517, #14664, #12046, #6371, #20068, #19414, #20535, #8365, #20955, #5171, #14524, #1951, #8841, #18613, #21445, #14434, #10123, #19094, #3088, #11285, #4478, #7696, #10181, #2265, #6664, #15218, #6015, #8392, #565, #21732, #9214, #20969, #16236, #11244, #93, #19226, #20186, #20591, #19195, #2546, #3977, #18798, #20469, #768, #8117, #16269, #20862, #15256, #20190, #1954, #3446, #4221, #13046, #7480, #19972, #20083, #19471, #15477, #18802, #21465, #12327, #11809, #7492, #11151, #1277, #8796, #214, #14505, #5696, #14109, #15693, #3162, #9261, #16810, #18708, #12239, #19759, #7715, #4919, #11287, #16238, #18397, #16461, #20501, #4475, #20942, #7918, #11946, #18580, #19822, #9995, #1474, #21696, #11309, #5652, #15980, #11270, #14532, #10906, #13576, #4499, #6291, #12480, #15429, #875, #17986, #1018, #13442, #14744, #12593, #14305, #9494, #21604, #1534, #18, #21839, #349, #7113, #14579, #13034, #4301, #15556, #11972, #16089, #15986, #16836, #4950, #10093, #7372, #10452, #16900, #7368, #11269, #11887, #2920, #507, #15873, #3757, #20159, #17515, #17115, #9454, #10415, #7535, #14641, #17046, #3063, #21039, #11997, #15178, #21139, #10588, #10995, #640, #6753, #18238, #6817, #16402, #18741, #6172, #16870, #12801, #9210, #17380, #20904, #10096, #20590, #6169, #16367, #20411, #16546, #1820, #18682, #13432, #19309, #14748, #6798, #21687, #5161, #3212, #12152, #10761, #14425, #18372, #15250, #10284, #7839, #3571, #16696, #3364, #15797, #6038, #17709, #4796, #9237, #2673, #7016, #5689, #20114, #19580, #10555, #1764, #10854, #5976, #9051, #21261, #21144, #16362, #20016, #11634, #9372, #2784, #7287, #18096, #12947, #10225, #20726, #20239, #1682, #15331, #14568, #3766, #14304, #13351, #13216, #14666, #11683, #19284, #4740, #322, #12731, #17578, #18963, #12193, #12675, #15439, #3995, #6001, #11515, #18585, #1228, #16341, #12506, #2703, #14094, #9158, #14139, #11841, #18990, #5650, #20779, #8278, #19387, #5460, #79, #4453, #12344, #19816, #7393, #10801, #12895, #2407, #4031, #15201, #5755, #18871, #7627, #20132, #20129, #17000 ) ) ;
#17472=ORIENTED_EDGE ( 'NONE', *, *, #20175, .T. ) ;
#17473=AXIS2_PLACEMENT_3D ( 'NONE', #1306, #21622, #17885 ) ;
#17474=ORIENTED_EDGE ( 'NONE', *, *, #4236, .F. ) ;
#17478=CARTESIAN_POINT ( 'NONE',  ( 10.00000000000000000, 61.60362715319035942, 62.84101464466265696 ) ) ;
#17479=CARTESIAN_POINT ( 'NONE',  ( 10.00000000000000000, 91.70173545986517638, 12.13370160540072362 ) ) ;
#17480=CARTESIAN_POINT ( 'NONE',  ( 0.000000000000000000, 90.63195040374188238, 18.50093422002450083 ) ) ;
#17481=DIRECTION ( 'NONE',  ( 0.000000000000000000, 0.000000000000000000, 1.000000000000000000 ) ) ;
#17482=DIRECTION ( 'NONE',  ( 0.000000000000000000, 0.000000000000000000, 1.000000000000000000 ) ) ;
#17483=ADVANCED_FACE ( 'NONE', ( #1095 ), #17677, .F. ) ;
#17484=DIRECTION ( 'NONE',  ( -1.000000000000000000, 0.000000000000000000, -0.000000000000000000 ) ) ;
#17485=DIRECTION ( 'NONE',  ( 0.000000000000000000, 0.4694715627858917495, -0.8829475928589264333 ) ) ;
#17486=LINE ( 'NONE', #17921, #21131 ) ;
#17489=EDGE_CURVE ( 'NONE', #17903, #1766, #7651, .T. ) ;
#17490=VERTEX_POINT ( 'NONE', #16122 ) ;
#17491=CIRCLE ( 'NONE', #4074, 92.50100000000000477 ) ;
#17492=CIRCLE ( 'NONE', #4768, 88.00000000000000000 ) ;
#17496=DIRECTION ( 'NONE',  ( -1.000000000000000000, 0.000000000000000000, -0.000000000000000000 ) ) ;
#17499=LINE ( 'NONE', #2349, #5592 ) ;
#17500=EDGE_LOOP ( 'NONE', ( #16376, #17325, #4549, #21266 ) ) ;
#17501=DIRECTION ( 'NONE',  ( 0.000000000000000000, 0.8987940462991649282, 0.4383711467890815117 ) ) ;
#17502=ORIENTED_EDGE ( 'NONE', *, *, #2972, .T. ) ;
#17503=AXIS2_PLACEMENT_3D ( 'NONE', #18034, #9280, #1341 ) ;
#17504=ORIENTED_EDGE ( 'NONE', *, *, #3423, .F. ) ;
#17505=DIRECTION ( 'NONE',  ( 0.000000000000000000, 0.000000000000000000, 1.000000000000000000 ) ) ;
#17506=CIRCLE ( 'NONE', #7971, 44.99999999999999289 ) ;
#17507=CIRCLE ( 'NONE', #2667, 100.0000000000000000 ) ;
#17508=DIRECTION ( 'NONE',  ( 0.000000000000000000, -0.2756373558169870064, -0.9612616959383222248 ) ) ;
#17510=CARTESIAN_POINT ( 'NONE',  ( 10.00000000000000000, 48.19312842678564834, -70.09002648625148879 ) ) ;
#17511=CARTESIAN_POINT ( 'NONE',  ( 0.000000000000000000, -84.12297548659729785, 12.59025161326973397 ) ) ;
#17512=FACE_OUTER_BOUND ( 'NONE', #16828, .T. ) ;
#17514=DIRECTION ( 'NONE',  ( -1.000000000000000000, -0.000000000000000000, 0.000000000000000000 ) ) ;
#17515=ORIENTED_EDGE ( 'NONE', *, *, #5533, .F. ) ;
#17516=FACE_OUTER_BOUND ( 'NONE', #180, .T. ) ;
#17517=ORIENTED_EDGE ( 'NONE', *, *, #8163, .T. ) ;
#17518=VECTOR ( 'NONE', #18901, 1000.000000000000000 ) ;
#17521=VERTEX_POINT ( 'NONE', #19872 ) ;
#17523=DIRECTION ( 'NONE',  ( -1.000000000000000000, 0.000000000000000000, 0.000000000000000000 ) ) ;
#17524=ORIENTED_EDGE ( 'NONE', *, *, #4869, .F. ) ;
#17526=VERTEX_POINT ( 'NONE', #3412 ) ;
#17527=ORIENTED_EDGE ( 'NONE', *, *, #3518, .F. ) ;
#17528=DIRECTION ( 'NONE',  ( 0.000000000000000000, 0.2756373558169932236, 0.9612616959383206705 ) ) ;
#17529=DIRECTION ( 'NONE',  ( 1.000000000000000000, 0.000000000000000000, 0.000000000000000000 ) ) ;
#17532=CARTESIAN_POINT ( 'NONE',  ( 10.00000000000000000, -61.33825423015638734, -69.23910433416007493 ) ) ;
#17534=AXIS2_PLACEMENT_3D ( 'NONE', #13889, #10468, #15555 ) ;
#17535=LINE ( 'NONE', #2387, #5484 ) ;
#17536=DIRECTION ( 'NONE',  ( -1.000000000000000000, -0.000000000000000000, -0.000000000000000000 ) ) ;
#17540=EDGE_LOOP ( 'NONE', ( #11172, #6564, #6746, #12103 ) ) ;
#17541=CARTESIAN_POINT ( 'NONE',  ( 10.00000000000000000, 46.07110168784925008, -74.97635353408335845 ) ) ;
#17542=LINE ( 'NONE', #9448, #19938 ) ;
#17543=EDGE_CURVE ( 'NONE', #2613, #3811, #6960, .T. ) ;
#17545=ORIENTED_EDGE ( 'NONE', *, *, #17, .F. ) ;
#17546=DIRECTION ( 'NONE',  ( 1.000000000000000000, 0.000000000000000000, 0.000000000000000000 ) ) ;
#17548=ORIENTED_EDGE ( 'NONE', *, *, #8650, .T. ) ;
#17549=DIRECTION ( 'NONE',  ( -1.000000000000000000, -0.000000000000000000, -0.000000000000000000 ) ) ;
#17550=CIRCLE ( 'NONE', #8026, 44.99999999999998579 ) ;
#17552=EDGE_LOOP ( 'NONE', ( #7771, #13862, #2095, #21838 ) ) ;
#17555=ORIENTED_EDGE ( 'NONE', *, *, #12448, .F. ) ;
#17556=CARTESIAN_POINT ( 'NONE',  ( 0.000000000000000000, -87.92084725184950855, 3.731570516142653116 ) ) ;
#17557=LINE ( 'NONE', #12781, #18173 ) ;
#17559=CARTESIAN_POINT ( 'NONE',  ( 10.00000000000000000, 27.00677879429135331, -80.65868421664406185 ) ) ;
#17561=CYLINDRICAL_SURFACE ( 'NONE', #6822, 45.00000000000000000 ) ;
#17562=EDGE_CURVE ( 'NONE', #10277, #6346, #20697, .T. ) ;
#17563=DIRECTION ( 'NONE',  ( 0.000000000000000000, -0.9848077530122062440, -0.1736481776669404620 ) ) ;
#17565=DIRECTION ( 'NONE',  ( 1.000000000000000000, -0.000000000000000000, 0.000000000000000000 ) ) ;
#17568=VECTOR ( 'NONE', #9917, 1000.000000000000000 ) ;
#17569=CARTESIAN_POINT ( 'NONE',  ( 10.00000000000000000, 85.05652083079334602, 0.7600687895874258526 ) ) ;
#17570=DIRECTION ( 'NONE',  ( -1.000000000000000000, 0.000000000000000000, -0.000000000000000000 ) ) ;
#17571=EDGE_CURVE ( 'NONE', #419, #18142, #2695, .T. ) ;
#17572=DIRECTION ( 'NONE',  ( -1.000000000000000000, -0.000000000000000000, -0.000000000000000000 ) ) ;
#17574=ORIENTED_EDGE ( 'NONE', *, *, #14313, .T. ) ;
#17577=AXIS2_PLACEMENT_3D ( 'NONE', #5330, #15697, #5220 ) ;
#17578=ORIENTED_EDGE ( 'NONE', *, *, #4607, .F. ) ;
#17579=VECTOR ( 'NONE', #18492, 1000.000000000000000 ) ;
#17580=CIRCLE ( 'NONE', #11589, 44.99999999999999289 ) ;
#17583=DIRECTION ( 'NONE',  ( 0.000000000000000000, 0.000000000000000000, 1.000000000000000000 ) ) ;
#17584=ORIENTED_EDGE ( 'NONE', *, *, #170, .F. ) ;
#17586=CARTESIAN_POINT ( 'NONE',  ( 10.00000000000000000, 0.000000000000000000, 0.000000000000000000 ) ) ;
#17588=DIRECTION ( 'NONE',  ( -1.000000000000000000, 0.000000000000000000, 0.000000000000000000 ) ) ;
#17589=DIRECTION ( 'NONE',  ( 0.000000000000000000, 0.7431448254773953543, -0.6691306063588569053 ) ) ;
#17590=DIRECTION ( 'NONE',  ( -1.000000000000000000, -0.000000000000000000, 0.000000000000000000 ) ) ;
#17591=CARTESIAN_POINT ( 'NONE',  ( 0.000000000000000000, 0.000000000000000000, 0.000000000000000000 ) ) ;
#17592=CARTESIAN_POINT ( 'NONE',  ( 10.00000000000000000, -65.83713140174687339, -58.39068529131263574 ) ) ;
#17593=AXIS2_PLACEMENT_3D ( 'NONE', #11815, #2, #13036 ) ;
#17595=VECTOR ( 'NONE', #17334, 1000.000000000000000 ) ;
#17596=VECTOR ( 'NONE', #18670, 1000.000000000000000 ) ;
#17597=EDGE_LOOP ( 'NONE', ( #9972, #15869, #15639, #12918 ) ) ;
#17602=DIRECTION ( 'NONE',  ( -1.000000000000000000, -0.000000000000000000, -0.000000000000000000 ) ) ;
#17604=AXIS2_PLACEMENT_3D ( 'NONE', #15763, #627, #14206 ) ;
#17605=CARTESIAN_POINT ( 'NONE',  ( 5.000000000000002665, 46.07110168784925008, -74.97635353408335845 ) ) ;
#17606=EDGE_CURVE ( 'NONE', #9724, #17660, #6249, .T. ) ;
#17607=VERTEX_POINT ( 'NONE', #6844 ) ;
#17608=AXIS2_PLACEMENT_3D ( 'NONE', #10479, #10364, #13578 ) ;
#17611=AXIS2_PLACEMENT_3D ( 'NONE', #21288, #9347, #849 ) ;
#17613=ADVANCED_FACE ( 'NONE', ( #13568 ), #18113, .F. ) ;
#17620=CARTESIAN_POINT ( 'NONE',  ( 10.00000000000000000, -78.04699792498111321, -49.64978465107371619 ) ) ;
#17621=CARTESIAN_POINT ( 'NONE',  ( 10.00000000000000000, -61.71252885873347793, -58.53847642588656441 ) ) ;
#17622=DIRECTION ( 'NONE',  ( -1.000000000000000000, 0.000000000000000000, 0.000000000000000000 ) ) ;
#17623=CARTESIAN_POINT ( 'NONE',  ( 10.00000000000000000, 56.35896156214949571, 73.34918167666329225 ) ) ;
#17624=DIRECTION ( 'NONE',  ( 0.000000000000000000, 0.6946583704589934793, 0.7193398003386547446 ) ) ;
#17626=ORIENTED_EDGE ( 'NONE', *, *, #19340, .F. ) ;
#17627=LINE ( 'NONE', #9105, #12903 ) ;
#17628=CIRCLE ( 'NONE', #16567, 88.00000000000000000 ) ;
#17630=ORIENTED_EDGE ( 'NONE', *, *, #6089, .F. ) ;
#17631=VECTOR ( 'NONE', #1505, 1000.000000000000000 ) ;
#17632=AXIS2_PLACEMENT_3D ( 'NONE', #15550, #6955, #1643 ) ;
#17633=CARTESIAN_POINT ( 'NONE',  ( 0.000000000000000000, -78.01214607583776228, 33.90124636420084414 ) ) ;
#17634=ORIENTED_EDGE ( 'NONE', *, *, #21501, .T. ) ;
#17637=VERTEX_POINT ( 'NONE', #16779 ) ;
#17638=ORIENTED_EDGE ( 'NONE', *, *, #1699, .F. ) ;
#17639=ORIENTED_EDGE ( 'NONE', *, *, #10450, .T. ) ;
#17641=CARTESIAN_POINT ( 'NONE',  ( 10.00000000000000000, 61.71252885873465033, -58.53847642588533517 ) ) ;
#17642=DIRECTION ( 'NONE',  ( 1.000000000000000000, 0.000000000000000000, 0.000000000000000000 ) ) ;
#17643=ORIENTED_EDGE ( 'NONE', *, *, #7594, .T. ) ;
#17644=DIRECTION ( 'NONE',  ( -1.000000000000000000, 0.000000000000000000, -0.000000000000000000 ) ) ;
#17646=CARTESIAN_POINT ( 'NONE',  ( 5.000000000000002665, 40.72878876293147954, 78.00747250042462611 ) ) ;
#17647=AXIS2_PLACEMENT_3D ( 'NONE', #7218, #3676, #13949 ) ;
#17649=CARTESIAN_POINT ( 'NONE',  ( 0.000000000000000000, -90.32141448704669529, -19.96189084378313794 ) ) ;
#17650=DIRECTION ( 'NONE',  ( -1.000000000000000000, -0.000000000000000000, -0.000000000000000000 ) ) ;
#17651=ORIENTED_EDGE ( 'NONE', *, *, #13788, .T. ) ;
#17652=LINE ( 'NONE', #12232, #18696 ) ;
#17655=ORIENTED_EDGE ( 'NONE', *, *, #4759, .T. ) ;
#17656=CARTESIAN_POINT ( 'NONE',  ( 10.00000000000000000, -81.97107881582211064, 22.71412948308539370 ) ) ;
#17657=ORIENTED_EDGE ( 'NONE', *, *, #13414, .T. ) ;
#17658=CIRCLE ( 'NONE', #13775, 88.00000000000000000 ) ;
#17660=VERTEX_POINT ( 'NONE', #11592 ) ;
#17667=DIRECTION ( 'NONE',  ( 1.000000000000000000, -0.000000000000000000, -0.000000000000000000 ) ) ;
#17669=CARTESIAN_POINT ( 'NONE',  ( 5.000000000000000000, -69.74988376404053270, 53.65588238863315240 ) ) ;
#17670=ADVANCED_FACE ( 'NONE', ( #14800 ), #13454, .F. ) ;
#17671=DIRECTION ( 'NONE',  ( 1.000000000000000000, 0.000000000000000000, 0.000000000000000000 ) ) ;
#17672=CARTESIAN_POINT ( 'NONE',  ( 10.00000000000000000, -72.58367602204218372, 49.75550195834843237 ) ) ;
#17674=VECTOR ( 'NONE', #11455, 1000.000000000000000 ) ;
#17676=CARTESIAN_POINT ( 'NONE',  ( 10.00000000000000000, 46.93287725819779155, 70.94007663282461351 ) ) ;
#17677=CYLINDRICAL_SURFACE ( 'NONE', #2008, 44.99999999999998579 ) ;
#17678=EDGE_LOOP ( 'NONE', ( #12570, #12474, #15339, #25 ) ) ;
#17679=ORIENTED_EDGE ( 'NONE', *, *, #10165, .F. ) ;
#17681=ORIENTED_EDGE ( 'NONE', *, *, #10816, .F. ) ;
#17682=EDGE_CURVE ( 'NONE', #15531, #5375, #9048, .T. ) ;
#17686=CARTESIAN_POINT ( 'NONE',  ( 0.000000000000000000, 0.000000000000000000, 0.000000000000000000 ) ) ;
#17687=EDGE_LOOP ( 'NONE', ( #15932, #19551, #20111, #19548 ) ) ;
#17688=FACE_OUTER_BOUND ( 'NONE', #11186, .T. ) ;
#17689=CARTESIAN_POINT ( 'NONE',  ( 0.000000000000000000, -56.34908017029516714, -63.71789861856507997 ) ) ;
#17690=DIRECTION ( 'NONE',  ( -1.000000000000000000, -0.000000000000000000, -0.000000000000000000 ) ) ;
#17692=CARTESIAN_POINT ( 'NONE',  ( 10.00000000000000000, -77.39385041987173963, 35.28996114464576550 ) ) ;
#17693=CARTESIAN_POINT ( 'NONE',  ( 10.00000000000000000, 0.000000000000000000, 0.000000000000000000 ) ) ;
#17695=EDGE_CURVE ( 'NONE', #16928, #11100, #16120, .T. ) ;
#17696=CARTESIAN_POINT ( 'NONE',  ( 0.000000000000000000, 41.87002153499110335, 74.04114219178059386 ) ) ;
#17698=ORIENTED_EDGE ( 'NONE', *, *, #19569, .T. ) ;
#17701=FACE_OUTER_BOUND ( 'NONE', #3700, .T. ) ;
#17702=CARTESIAN_POINT ( 'NONE',  ( 0.000000000000000000, 81.83745710415318797, -32.35167097270070258 ) ) ;
#17703=EDGE_CURVE ( 'NONE', #4590, #827, #3847, .T. ) ;
#17704=VERTEX_POINT ( 'NONE', #15328 ) ;
#17705=EDGE_CURVE ( 'NONE', #10994, #6894, #2348, .T. ) ;
#17706=EDGE_CURVE ( 'NONE', #21543, #7099, #418, .T. ) ;
#17707=DIRECTION ( 'NONE',  ( -1.000000000000000000, -0.000000000000000000, -0.000000000000000000 ) ) ;
#17709=ORIENTED_EDGE ( 'NONE', *, *, #2421, .F. ) ;
#17711=FACE_OUTER_BOUND ( 'NONE', #14911, .T. ) ;
#17712=EDGE_CURVE ( 'NONE', #75, #1096, #4120, .T. ) ;
#17713=ORIENTED_EDGE ( 'NONE', *, *, #20581, .T. ) ;
#17715=CARTESIAN_POINT ( 'NONE',  ( 10.00000000000000000, -29.29369617358407041, -87.74003855418429509 ) ) ;
#17716=DIRECTION ( 'NONE',  ( -1.000000000000000000, 0.000000000000000000, 0.000000000000000000 ) ) ;
#17718=DIRECTION ( 'NONE',  ( -1.000000000000000000, -0.000000000000000000, 0.000000000000000000 ) ) ;
#17719=LINE ( 'NONE', #19265, #13340 ) ;
#17721=FACE_OUTER_BOUND ( 'NONE', #8418, .T. ) ;
#17723=DIRECTION ( 'NONE',  ( -1.000000000000000000, 0.000000000000000000, 0.000000000000000000 ) ) ;
#17724=EDGE_CURVE ( 'NONE', #4269, #923, #21060, .T. ) ;
#17725=DIRECTION ( 'NONE',  ( -1.000000000000000000, 0.000000000000000000, -0.000000000000000000 ) ) ;
#17726=AXIS2_PLACEMENT_3D ( 'NONE', #20593, #484, #7227 ) ;
#17727=ORIENTED_EDGE ( 'NONE', *, *, #9320, .F. ) ;
#17730=LINE ( 'NONE', #21158, #20332 ) ;
#17732=EDGE_CURVE ( 'NONE', #8340, #8524, #1664, .T. ) ;
#17735=CARTESIAN_POINT ( 'NONE',  ( 10.00000000000000000, -8.134922360106683570, 84.67002113262478247 ) ) ;
#17737=EDGE_LOOP ( 'NONE', ( #17363, #6728, #16854, #12798 ) ) ;
#17740=AXIS2_PLACEMENT_3D ( 'NONE', #20338, #8290, #15023 ) ;
#17743=VERTEX_POINT ( 'NONE', #12124 ) ;
#17744=DIRECTION ( 'NONE',  ( 1.000000000000000000, 0.000000000000000000, 0.000000000000000000 ) ) ;
#17747=VERTEX_POINT ( 'NONE', #15767 ) ;
#17749=CARTESIAN_POINT ( 'NONE',  ( 10.00000000000000000, 61.33825423015685629, 69.23910433415966281 ) ) ;
#17751=DIRECTION ( 'NONE',  ( 0.000000000000000000, 0.6946583704589935904, 0.7193398003386546335 ) ) ;
#17752=CARTESIAN_POINT ( 'NONE',  ( 0.000000000000000000, 0.000000000000000000, 0.000000000000000000 ) ) ;
#17753=AXIS2_PLACEMENT_3D ( 'NONE', #17689, #12708, #14483 ) ;
#17754=ORIENTED_EDGE ( 'NONE', *, *, #1119, .T. ) ;
#17755=EDGE_CURVE ( 'NONE', #7932, #10994, #18876, .T. ) ;
#17757=DIRECTION ( 'NONE',  ( 0.000000000000000000, 0.1391731009600657709, -0.9902680687415702510 ) ) ;
#17758=AXIS2_PLACEMENT_3D ( 'NONE', #1813, #11755, #14854 ) ;
#17761=EDGE_LOOP ( 'NONE', ( #8455, #10883, #1353, #10710 ) ) ;
#17762=CARTESIAN_POINT ( 'NONE',  ( 5.000000000000002665, -46.07110168784872428, 74.97635353408365688 ) ) ;
#17768=ORIENTED_EDGE ( 'NONE', *, *, #5305, .T. ) ;
#17771=DIRECTION ( 'NONE',  ( 0.000000000000000000, 0.000000000000000000, 1.000000000000000000 ) ) ;
#17772=CIRCLE ( 'NONE', #7186, 92.50100000000003320 ) ;
#17773=DIRECTION ( 'NONE',  ( -1.000000000000000000, 0.000000000000000000, 0.000000000000000000 ) ) ;
#17774=DIRECTION ( 'NONE',  ( 0.000000000000000000, 0.000000000000000000, 1.000000000000000000 ) ) ;
#17775=DIRECTION ( 'NONE',  ( 1.000000000000000000, 0.000000000000000000, 0.000000000000000000 ) ) ;
#17776=AXIS2_PLACEMENT_3D ( 'NONE', #8481, #3503, #3395 ) ;
#17777=AXIS2_PLACEMENT_3D ( 'NONE', #9959, #20034, #3015 ) ;
#17778=DIRECTION ( 'NONE',  ( 1.000000000000000000, 0.000000000000000000, 0.000000000000000000 ) ) ;
#17779=CARTESIAN_POINT ( 'NONE',  ( 0.000000000000000000, 0.000000000000000000, 0.000000000000000000 ) ) ;
#17780=ADVANCED_FACE ( 'NONE', ( #15445 ), #10354, .F. ) ;
#17781=CARTESIAN_POINT ( 'NONE',  ( 5.000000000000000000, 87.92084725184948013, 3.731570516143270400 ) ) ;
#17783=AXIS2_PLACEMENT_3D ( 'NONE', #7910, #4599, #6712 ) ;
#17784=DIRECTION ( 'NONE',  ( 1.000000000000000000, 0.000000000000000000, 0.000000000000000000 ) ) ;
#17785=ORIENTED_EDGE ( 'NONE', *, *, #2034, .T. ) ;
#17786=EDGE_LOOP ( 'NONE', ( #19073, #8937, #10615, #18125 ) ) ;
#17788=ORIENTED_EDGE ( 'NONE', *, *, #7235, .T. ) ;
#17789=ORIENTED_EDGE ( 'NONE', *, *, #6217, .F. ) ;
#17791=CARTESIAN_POINT ( 'NONE',  ( 0.000000000000000000, 0.000000000000000000, 0.000000000000000000 ) ) ;
#17792=CIRCLE ( 'NONE', #16012, 92.50100000000000477 ) ;
#17794=DIRECTION ( 'NONE',  ( 0.000000000000000000, -0.4067366430758070917, 0.9135454576425978690 ) ) ;
#17795=DIRECTION ( 'NONE',  ( 0.000000000000000000, 0.000000000000000000, 1.000000000000000000 ) ) ;
#17796=CARTESIAN_POINT ( 'NONE',  ( 10.00000000000000000, 91.49386717542222414, 13.61276130277023810 ) ) ;
#17797=AXIS2_PLACEMENT_3D ( 'NONE', #6152, #11110, #1166 ) ;
#17798=DIRECTION ( 'NONE',  ( 0.000000000000000000, 0.000000000000000000, 1.000000000000000000 ) ) ;
#17799=DIRECTION ( 'NONE',  ( 1.000000000000000000, 0.000000000000000000, 0.000000000000000000 ) ) ;
#17800=DIRECTION ( 'NONE',  ( 1.000000000000000000, 0.000000000000000000, 0.000000000000000000 ) ) ;
#17802=DIRECTION ( 'NONE',  ( 0.000000000000000000, 0.9510565162951544194, -0.3090169943749450643 ) ) ;
#17803=DIRECTION ( 'NONE',  ( -1.000000000000000000, 0.000000000000000000, 0.000000000000000000 ) ) ;
#17805=EDGE_CURVE ( 'NONE', #17876, #7364, #256, .T. ) ;
#17806=VERTEX_POINT ( 'NONE', #2286 ) ;
#17807=DIRECTION ( 'NONE',  ( -1.000000000000000000, -0.000000000000000000, -0.000000000000000000 ) ) ;
#17808=AXIS2_PLACEMENT_3D ( 'NONE', #15467, #2310, #6976 ) ;
#17810=ORIENTED_EDGE ( 'NONE', *, *, #3159, .T. ) ;
#17811=ADVANCED_FACE ( 'NONE', ( #9021 ), #12024, .F. ) ;
#17812=VECTOR ( 'NONE', #13225, 1000.000000000000000 ) ;
#17813=DIRECTION ( 'NONE',  ( 0.000000000000000000, -0.06975647374411146628, -0.9975640502598251969 ) ) ;
#17816=CYLINDRICAL_SURFACE ( 'NONE', #16539, 44.99999999999999289 ) ;
#17821=EDGE_CURVE ( 'NONE', #3424, #12605, #20373, .T. ) ;
#17822=DIRECTION ( 'NONE',  ( -1.000000000000000000, -0.000000000000000000, -0.000000000000000000 ) ) ;
#17823=ORIENTED_EDGE ( 'NONE', *, *, #7461, .F. ) ;
#17824=ORIENTED_EDGE ( 'NONE', *, *, #14156, .F. ) ;
#17826=DIRECTION ( 'NONE',  ( -1.000000000000000000, 0.000000000000000000, 0.000000000000000000 ) ) ;
#17827=DIRECTION ( 'NONE',  ( -1.000000000000000000, -0.000000000000000000, -0.000000000000000000 ) ) ;
#17828=CARTESIAN_POINT ( 'NONE',  ( 0.000000000000000000, -65.64563793391867819, 54.09103124042793098 ) ) ;
#17829=AXIS2_PLACEMENT_3D ( 'NONE', #12440, #9229, #741 ) ;
#17830=DIRECTION ( 'NONE',  ( 0.000000000000000000, -0.9510565162951565288, 0.3090169943749382919 ) ) ;
#17831=FACE_OUTER_BOUND ( 'NONE', #17552, .T. ) ;
#17835=CARTESIAN_POINT ( 'NONE',  ( 10.00000000000000000, 33.95793648385932784, -86.04239391577952745 ) ) ;
#17836=VECTOR ( 'NONE', #3561, 1000.000000000000000 ) ;
#17838=EDGE_CURVE ( 'NONE', #12967, #5617, #8366, .T. ) ;
#17840=EDGE_LOOP ( 'NONE', ( #13927, #15144, #17360, #1858 ) ) ;
#17843=EDGE_LOOP ( 'NONE', ( #6193, #20785, #1910, #18771 ) ) ;
#17846=AXIS2_PLACEMENT_3D ( 'NONE', #11174, #1118, #7763 ) ;
#17847=FACE_OUTER_BOUND ( 'NONE', #12329, .T. ) ;
#17848=AXIS2_PLACEMENT_3D ( 'NONE', #20698, #373, #7220 ) ;
#17849=VERTEX_POINT ( 'NONE', #2506 ) ;
#17851=EDGE_CURVE ( 'NONE', #17170, #6729, #6267, .T. ) ;
#17852=AXIS2_PLACEMENT_3D ( 'NONE', #10838, #17590, #2450 ) ;
#17853=ORIENTED_EDGE ( 'NONE', *, *, #17025, .F. ) ;
#17855=ORIENTED_EDGE ( 'NONE', *, *, #16389, .F. ) ;
#17856=DIRECTION ( 'NONE',  ( 0.000000000000000000, 0.000000000000000000, 1.000000000000000000 ) ) ;
#17857=CARTESIAN_POINT ( 'NONE',  ( 10.00000000000000000, 92.49798535263880694, -0.7467976319023919007 ) ) ;
#17858=ORIENTED_EDGE ( 'NONE', *, *, #15795, .T. ) ;
#17859=EDGE_CURVE ( 'NONE', #1594, #19677, #12594, .T. ) ;
#17861=CARTESIAN_POINT ( 'NONE',  ( 10.00000000000000000, -5.479102470009884485, -87.82926298292120748 ) ) ;
#17862=DIRECTION ( 'NONE',  ( -1.000000000000000000, -0.000000000000000000, -0.000000000000000000 ) ) ;
#17864=AXIS2_PLACEMENT_3D ( 'NONE', #9963, #6783, #14943 ) ;
#17865=CARTESIAN_POINT ( 'NONE',  ( 10.00000000000000000, 0.000000000000000000, 0.000000000000000000 ) ) ;
#17871=AXIS2_PLACEMENT_3D ( 'NONE', #643, #2187, #6064 ) ;
#17872=EDGE_CURVE ( 'NONE', #923, #13383, #15771, .T. ) ;
#17876=VERTEX_POINT ( 'NONE', #2399 ) ;
#17880=FACE_OUTER_BOUND ( 'NONE', #9373, .T. ) ;
#17881=ADVANCED_FACE ( 'NONE', ( #1177 ), #17988, .F. ) ;
#17882=ORIENTED_EDGE ( 'NONE', *, *, #14682, .T. ) ;
#17885=DIRECTION ( 'NONE',  ( 0.000000000000000000, 0.000000000000000000, 1.000000000000000000 ) ) ;
#17886=EDGE_CURVE ( 'NONE', #8737, #4066, #15424, .T. ) ;
#17889=DIRECTION ( 'NONE',  ( 0.000000000000000000, 0.000000000000000000, 1.000000000000000000 ) ) ;
#17890=CARTESIAN_POINT ( 'NONE',  ( 10.00000000000000000, -83.35585896458628952, 16.94078559807922346 ) ) ;
#17893=CARTESIAN_POINT ( 'NONE',  ( 10.00000000000000000, -91.49386717542229519, 13.61276130276963414 ) ) ;
#17897=CARTESIAN_POINT ( 'NONE',  ( 5.000000000000002665, 12.90135963484081216, 87.04915231966650424 ) ) ;
#17899=AXIS2_PLACEMENT_3D ( 'NONE', #10274, #20345, #2104 ) ;
#17901=AXIS2_PLACEMENT_3D ( 'NONE', #14129, #10809, #17563 ) ;
#17902=DIRECTION ( 'NONE',  ( -1.000000000000000000, 0.000000000000000000, 0.000000000000000000 ) ) ;
#17903=VERTEX_POINT ( 'NONE', #2612 ) ;
#17904=VERTEX_POINT ( 'NONE', #16308 ) ;
#17906=EDGE_LOOP ( 'NONE', ( #9643, #5526, #13078, #18311 ) ) ;
#17908=DIRECTION ( 'NONE',  ( -1.000000000000000000, -0.000000000000000000, -0.000000000000000000 ) ) ;
#17909=CIRCLE ( 'NONE', #8738, 88.00000000000000000 ) ;
#17910=ORIENTED_EDGE ( 'NONE', *, *, #7337, .F. ) ;
#17912=AXIS2_PLACEMENT_3D ( 'NONE', #5266, #12320, #8884 ) ;
#17914=CYLINDRICAL_SURFACE ( 'NONE', #85, 44.99999999999999289 ) ;
#17917=DIRECTION ( 'NONE',  ( -1.000000000000000000, 0.000000000000000000, -0.000000000000000000 ) ) ;
#17919=CARTESIAN_POINT ( 'NONE',  ( 0.000000000000000000, 84.12297548659721258, 32.40974838672968872 ) ) ;
#17920=CARTESIAN_POINT ( 'NONE',  ( 10.00000000000000000, -84.12297548659712731, -12.59025161327086906 ) ) ;
#17921=CARTESIAN_POINT ( 'NONE',  ( 10.00000000000000000, -51.10509369859486384, 77.10190917907182495 ) ) ;
#17922=ORIENTED_EDGE ( 'NONE', *, *, #15653, .F. ) ;
#17923=DIRECTION ( 'NONE',  ( 0.000000000000000000, 0.3420201433256630508, 0.9396926207859104263 ) ) ;
#17924=CIRCLE ( 'NONE', #20745, 92.50100000000000477 ) ;
#17925=AXIS2_PLACEMENT_3D ( 'NONE', #14202, #20949, #21059 ) ;
#17926=ORIENTED_EDGE ( 'NONE', *, *, #5940, .T. ) ;
#17928=CARTESIAN_POINT ( 'NONE',  ( 0.000000000000000000, -70.37753541435900217, -60.02863908169706519 ) ) ;
#17929=ORIENTED_EDGE ( 'NONE', *, *, #15652, .T. ) ;
#17930=DIRECTION ( 'NONE',  ( -1.000000000000000000, 0.000000000000000000, -0.000000000000000000 ) ) ;
#17931=EDGE_LOOP ( 'NONE', ( #15659, #5071, #8814, #14888 ) ) ;
#17932=VERTEX_POINT ( 'NONE', #19191 ) ;
#17934=AXIS2_PLACEMENT_3D ( 'NONE', #17040, #136, #1689 ) ;
#17935=CARTESIAN_POINT ( 'NONE',  ( 5.000000000000000000, 61.60362715319122628, -62.84101464466179721 ) ) ;
#17936=ORIENTED_EDGE ( 'NONE', *, *, #2313, .T. ) ;
#17937=EDGE_CURVE ( 'NONE', #19614, #4068, #12238, .T. ) ;
#17938=VERTEX_POINT ( 'NONE', #7703 ) ;
#17939=CARTESIAN_POINT ( 'NONE',  ( 5.000000000000000000, -51.18896083639317851, 71.57995730992162464 ) ) ;
#17941=CIRCLE ( 'NONE', #8765, 88.00000000000000000 ) ;
#17942=DIRECTION ( 'NONE',  ( -1.000000000000000000, -0.000000000000000000, -0.000000000000000000 ) ) ;
#17943=CARTESIAN_POINT ( 'NONE',  ( 0.000000000000000000, 11.59241532900744787, -87.23311244498727035 ) ) ;
#17946=AXIS2_PLACEMENT_3D ( 'NONE', #20136, #18264, #3114 ) ;
#17947=DIRECTION ( 'NONE',  ( 0.000000000000000000, 0.2756373558169932791, 0.9612616959383205595 ) ) ;
#17948=VECTOR ( 'NONE', #13370, 1000.000000000000000 ) ;
#17950=DIRECTION ( 'NONE',  ( 1.000000000000000000, 0.000000000000000000, 0.000000000000000000 ) ) ;
#17951=DIRECTION ( 'NONE',  ( -1.000000000000000000, 0.000000000000000000, 0.000000000000000000 ) ) ;
#17952=CARTESIAN_POINT ( 'NONE',  ( 10.00000000000000000, -72.53479564998815476, 44.42851404693331574 ) ) ;
#17954=DIRECTION ( 'NONE',  ( 0.000000000000000000, 0.000000000000000000, 1.000000000000000000 ) ) ;
#17956=CYLINDRICAL_SURFACE ( 'NONE', #3820, 44.99999999999998579 ) ;
#17957=AXIS2_PLACEMENT_3D ( 'NONE', #8923, #15563, #8503 ) ;
#17961=CARTESIAN_POINT ( 'NONE',  ( 0.000000000000000000, 0.000000000000000000, 0.000000000000000000 ) ) ;
#17962=VECTOR ( 'NONE', #554, 1000.000000000000000 ) ;
#17963=ORIENTED_EDGE ( 'NONE', *, *, #3559, .F. ) ;
#17967=EDGE_CURVE ( 'NONE', #2155, #15044, #18604, .T. ) ;
#17968=ADVANCED_FACE ( 'NONE', ( #6720 ), #18085, .F. ) ;
#17969=ORIENTED_EDGE ( 'NONE', *, *, #12289, .T. ) ;
#17970=ADVANCED_FACE ( 'NONE', ( #16643 ), #21402, .F. ) ;
#17974=ADVANCED_FACE ( 'NONE', ( #12999 ), #1409, .F. ) ;
#17975=CARTESIAN_POINT ( 'NONE',  ( 0.000000000000000000, -81.32027326007897727, 44.08455690949027428 ) ) ;
#17976=LINE ( 'NONE', #9547, #5941 ) ;
#17977=DIRECTION ( 'NONE',  ( 0.000000000000000000, 0.000000000000000000, 1.000000000000000000 ) ) ;
#17978=CARTESIAN_POINT ( 'NONE',  ( 0.000000000000000000, 86.54587337002898551, -15.93147207946920396 ) ) ;
#17979=LINE ( 'NONE', #16086, #9079 ) ;
#17980=VECTOR ( 'NONE', #3605, 1000.000000000000000 ) ;
#17983=CARTESIAN_POINT ( 'NONE',  ( 10.00000000000000000, -52.96496548042809138, -66.55750800669412115 ) ) ;
#17985=DIRECTION ( 'NONE',  ( 0.000000000000000000, 0.000000000000000000, 1.000000000000000000 ) ) ;
#17986=ORIENTED_EDGE ( 'NONE', *, *, #2299, .T. ) ;
#17987=ADVANCED_FACE ( 'NONE', ( #4608 ), #11448, .F. ) ;
#17988=CYLINDRICAL_SURFACE ( 'NONE', #10829, 44.99999999999999289 ) ;
#17989=ORIENTED_EDGE ( 'NONE', *, *, #12409, .T. ) ;
#17990=PLANE ( 'NONE',  #6331 ) ;
#17991=CARTESIAN_POINT ( 'NONE',  ( 10.00000000000000000, 0.000000000000000000, 0.000000000000000000 ) ) ;
#17994=AXIS2_PLACEMENT_3D ( 'NONE', #9622, #17716, #19807 ) ;
#17997=EDGE_CURVE ( 'NONE', #8941, #18330, #16542, .T. ) ;
#17998=VECTOR ( 'NONE', #43, 1000.000000000000000 ) ;
#18001=ORIENTED_EDGE ( 'NONE', *, *, #16622, .T. ) ;
#18003=ADVANCED_FACE ( 'NONE', ( #8247 ), #10113, .F. ) ;
#18004=DIRECTION ( 'NONE',  ( 0.000000000000000000, -8.943463253924873884E-15, -1.000000000000000000 ) ) ;
#18005=CARTESIAN_POINT ( 'NONE',  ( 10.00000000000000000, -86.77540292929691645, -14.62974526292806843 ) ) ;
#18006=DIRECTION ( 'NONE',  ( 0.000000000000000000, -0.3420201433256569445, -0.9396926207859125357 ) ) ;
#18008=CARTESIAN_POINT ( 'NONE',  ( 5.000000000000000000, 56.05743251323954013, -67.83483072893743326 ) ) ;
#18009=CARTESIAN_POINT ( 'NONE',  ( 10.00000000000000000, -39.87723064937059547, -83.46401306393613595 ) ) ;
#18010=CARTESIAN_POINT ( 'NONE',  ( -10.00000000000000000, 0.000000000000000000, 0.000000000000000000 ) ) ;
#18011=EDGE_CURVE ( 'NONE', #16010, #6503, #10486, .T. ) ;
#18020=ORIENTED_EDGE ( 'NONE', *, *, #2317, .F. ) ;
#18022=FACE_OUTER_BOUND ( 'NONE', #18559, .T. ) ;
#18023=EDGE_CURVE ( 'NONE', #9734, #19710, #8036, .T. ) ;
#18025=CARTESIAN_POINT ( 'NONE',  ( 0.000000000000000000, 0.000000000000000000, 0.000000000000000000 ) ) ;
#18026=AXIS2_PLACEMENT_3D ( 'NONE', #7096, #11952, #8846 ) ;
#18028=DIRECTION ( 'NONE',  ( 0.000000000000000000, 0.000000000000000000, 1.000000000000000000 ) ) ;
#18030=LINE ( 'NONE', #14698, #21043 ) ;
#18031=CARTESIAN_POINT ( 'NONE',  ( 0.000000000000000000, -83.35585896458628952, 16.94078559807922346 ) ) ;
#18032=CARTESIAN_POINT ( 'NONE',  ( 10.00000000000000000, 0.000000000000000000, 0.000000000000000000 ) ) ;
#18033=ORIENTED_EDGE ( 'NONE', *, *, #9183, .T. ) ;
#18034=CARTESIAN_POINT ( 'NONE',  ( 0.000000000000000000, 0.000000000000000000, 0.000000000000000000 ) ) ;
#18036=ORIENTED_EDGE ( 'NONE', *, *, #8428, .F. ) ;
#18037=EDGE_CURVE ( 'NONE', #14060, #15149, #18524, .T. ) ;
#18038=DIRECTION ( 'NONE',  ( -1.000000000000000000, -0.000000000000000000, 0.000000000000000000 ) ) ;
#18039=CARTESIAN_POINT ( 'NONE',  ( 0.000000000000000000, 21.31452625070926743, 82.34610137166127686 ) ) ;
#18042=ORIENTED_EDGE ( 'NONE', *, *, #182, .F. ) ;
#18043=VERTEX_POINT ( 'NONE', #9899 ) ;
#18046=ORIENTED_EDGE ( 'NONE', *, *, #549, .T. ) ;
#18047=ORIENTED_EDGE ( 'NONE', *, *, #14737, .T. ) ;
#18049=FACE_OUTER_BOUND ( 'NONE', #19365, .T. ) ;
#18050=CARTESIAN_POINT ( 'NONE',  ( 10.00000000000000000, 0.000000000000000000, 0.000000000000000000 ) ) ;
#18051=DIRECTION ( 'NONE',  ( 0.000000000000000000, 0.000000000000000000, 1.000000000000000000 ) ) ;
#18052=DIRECTION ( 'NONE',  ( 1.000000000000000000, 0.000000000000000000, 0.000000000000000000 ) ) ;
#18053=AXIS2_PLACEMENT_3D ( 'NONE', #5273, #73, #10235 ) ;
#18054=DIRECTION ( 'NONE',  ( -1.000000000000000000, -0.000000000000000000, -0.000000000000000000 ) ) ;
#18055=CARTESIAN_POINT ( 'NONE',  ( 10.00000000000000000, -66.01871308925419157, -64.79170103523090063 ) ) ;
#18056=CARTESIAN_POINT ( 'NONE',  ( 0.000000000000000000, 0.000000000000000000, 0.000000000000000000 ) ) ;
#18057=CARTESIAN_POINT ( 'NONE',  ( 10.00000000000000000, 0.000000000000000000, 0.000000000000000000 ) ) ;
#18059=EDGE_CURVE ( 'NONE', #13595, #10604, #5921, .T. ) ;
#18061=FACE_OUTER_BOUND ( 'NONE', #20873, .T. ) ;
#18062=VECTOR ( 'NONE', #19084, 1000.000000000000000 ) ;
#18063=CARTESIAN_POINT ( 'NONE',  ( 5.000000000000000000, 75.87763420127832603, 44.57111876559750385 ) ) ;
#18064=ORIENTED_EDGE ( 'NONE', *, *, #15837, .F. ) ;
#18065=VERTEX_POINT ( 'NONE', #11679 ) ;
#18069=FACE_OUTER_BOUND ( 'NONE', #11030, .T. ) ;
#18070=ORIENTED_EDGE ( 'NONE', *, *, #3893, .F. ) ;
#18072=CARTESIAN_POINT ( 'NONE',  ( 0.000000000000000000, 12.90135963484197212, -87.04915231966633371 ) ) ;
#18073=CARTESIAN_POINT ( 'NONE',  ( 0.000000000000000000, 87.92084725184953697, -3.731570516142035387 ) ) ;
#18074=LINE ( 'NONE', #14865, #2306 ) ;
#18076=DIRECTION ( 'NONE',  ( 1.000000000000000000, 0.000000000000000000, 0.000000000000000000 ) ) ;
#18078=UNCERTAINTY_MEASURE_WITH_UNIT (LENGTH_MEASURE( 1.000000000000000082E-05 ), #18440, 'distance_accuracy_value', 'NONE');
#18079=ORIENTED_EDGE ( 'NONE', *, *, #21240, .F. ) ;
#18082=DIRECTION ( 'NONE',  ( 0.000000000000000000, 0.000000000000000000, 1.000000000000000000 ) ) ;
#18084=ORIENTED_EDGE ( 'NONE', *, *, #13518, .F. ) ;
#18085=CYLINDRICAL_SURFACE ( 'NONE', #9771, 88.00000000000000000 ) ;
#18087=AXIS2_PLACEMENT_3D ( 'NONE', #10266, #16677, #10043 ) ;
#18088=FACE_BOUND ( 'NONE', #17471, .T. ) ;
#18091=EDGE_CURVE ( 'NONE', #15149, #6824, #13679, .T. ) ;
#18093=VERTEX_POINT ( 'NONE', #11996 ) ;
#18094=ORIENTED_EDGE ( 'NONE', *, *, #3532, .F. ) ;
#18095=CARTESIAN_POINT ( 'NONE',  ( 0.000000000000000000, 70.37753541435941429, 60.02863908169658202 ) ) ;
#18096=ORIENTED_EDGE ( 'NONE', *, *, #17011, .T. ) ;
#18097=EDGE_CURVE ( 'NONE', #15334, #4606, #11199, .T. ) ;
#18098=LINE ( 'NONE', #16320, #3507 ) ;
#18099=VECTOR ( 'NONE', #9038, 1000.000000000000000 ) ;
#18100=DIRECTION ( 'NONE',  ( 1.000000000000000000, 0.000000000000000000, 0.000000000000000000 ) ) ;
#18101=CYLINDRICAL_SURFACE ( 'NONE', #5063, 44.99999999999999289 ) ;
#18103=AXIS2_PLACEMENT_3D ( 'NONE', #21765, #16579, #4978 ) ;
#18104=CYLINDRICAL_SURFACE ( 'NONE', #18282, 44.99999999999999289 ) ;
#18106=CIRCLE ( 'NONE', #15633, 44.99999999999998579 ) ;
#18107=DIRECTION ( 'NONE',  ( 1.000000000000000000, 0.000000000000000000, 0.000000000000000000 ) ) ;
#18108=DIRECTION ( 'NONE',  ( 0.000000000000000000, -0.9702957262759939194, -0.2419218955996776110 ) ) ;
#18109=ADVANCED_FACE ( 'NONE', ( #16973 ), #12095, .F. ) ;
#18111=ADVANCED_FACE ( 'NONE', ( #18848 ), #8791, .F. ) ;
#18112=ADVANCED_FACE ( 'NONE', ( #8569 ), #20506, .F. ) ;
#18113=CYLINDRICAL_SURFACE ( 'NONE', #4470, 88.00000000000000000 ) ;
#18114=ORIENTED_EDGE ( 'NONE', *, *, #21246, .F. ) ;
#18115=ADVANCED_FACE ( 'NONE', ( #19065 ), #20291, .F. ) ;
#18117=ORIENTED_EDGE ( 'NONE', *, *, #17178, .F. ) ;
#18118=ORIENTED_EDGE ( 'NONE', *, *, #17851, .T. ) ;
#18120=AXIS2_PLACEMENT_3D ( 'NONE', #9681, #6834, #18654 ) ;
#18121=ORIENTED_EDGE ( 'NONE', *, *, #13637, .F. ) ;
#18122=ORIENTED_EDGE ( 'NONE', *, *, #4441, .T. ) ;
#18125=ORIENTED_EDGE ( 'NONE', *, *, #18958, .T. ) ;
#18126=DIRECTION ( 'NONE',  ( 0.000000000000000000, 0.000000000000000000, 1.000000000000000000 ) ) ;
#18127=CARTESIAN_POINT ( 'NONE',  ( 0.000000000000000000, 86.66425444033919234, 32.33793443156426406 ) ) ;
#18129=CIRCLE ( 'NONE', #2598, 92.50099999999999056 ) ;
#18130=DIRECTION ( 'NONE',  ( 1.000000000000000000, 0.000000000000000000, 0.000000000000000000 ) ) ;
#18132=DIRECTION ( 'NONE',  ( 0.000000000000000000, 0.000000000000000000, 1.000000000000000000 ) ) ;
#18133=EDGE_CURVE ( 'NONE', #14602, #1536, #2730, .T. ) ;
#18134=CARTESIAN_POINT ( 'NONE',  ( 10.00000000000000000, 0.000000000000000000, 0.000000000000000000 ) ) ;
#18135=CARTESIAN_POINT ( 'NONE',  ( 10.00000000000000000, 0.000000000000000000, 0.000000000000000000 ) ) ;
#18136=CIRCLE ( 'NONE', #15298, 44.99999999999999289 ) ;
#18140=FACE_OUTER_BOUND ( 'NONE', #744, .T. ) ;
#18141=EDGE_CURVE ( 'NONE', #9877, #20418, #1332, .T. ) ;
#18142=VERTEX_POINT ( 'NONE', #13977 ) ;
#18148=CARTESIAN_POINT ( 'NONE',  ( 10.00000000000000000, 87.17509410653623547, 30.93441398372612738 ) ) ;
#18149=ORIENTED_EDGE ( 'NONE', *, *, #3159, .F. ) ;
#18154=ORIENTED_EDGE ( 'NONE', *, *, #16785, .T. ) ;
#18155=DIRECTION ( 'NONE',  ( -1.000000000000000000, 0.000000000000000000, 0.000000000000000000 ) ) ;
#18156=ADVANCED_FACE ( 'NONE', ( #7035 ), #15195, .F. ) ;
#18159=CARTESIAN_POINT ( 'NONE',  ( -10.00000000000000000, 0.000000000000000000, 0.000000000000000000 ) ) ;
#18160=EDGE_CURVE ( 'NONE', #15532, #18176, #8384, .T. ) ;
#18162=EDGE_CURVE ( 'NONE', #2483, #11838, #18635, .T. ) ;
#18164=EDGE_CURVE ( 'NONE', #13661, #8013, #19322, .T. ) ;
#18166=DIRECTION ( 'NONE',  ( -1.000000000000000000, -0.000000000000000000, 0.000000000000000000 ) ) ;
#18168=AXIS2_PLACEMENT_3D ( 'NONE', #16280, #1149, #6247 ) ;
#18169=CIRCLE ( 'NONE', #12667, 44.99999999999998579 ) ;
#18170=VERTEX_POINT ( 'NONE', #15414 ) ;
#18172=ORIENTED_EDGE ( 'NONE', *, *, #4616, .F. ) ;
#18173=VECTOR ( 'NONE', #5631, 1000.000000000000000 ) ;
#18176=VERTEX_POINT ( 'NONE', #10443 ) ;
#18177=DIRECTION ( 'NONE',  ( 0.000000000000000000, 0.000000000000000000, 1.000000000000000000 ) ) ;
#18178=VERTEX_POINT ( 'NONE', #17193 ) ;
#18180=AXIS2_PLACEMENT_3D ( 'NONE', #6302, #980, #2633 ) ;
#18181=VERTEX_POINT ( 'NONE', #12211 ) ;
#18182=ORIENTED_EDGE ( 'NONE', *, *, #17821, .F. ) ;
#18183=ORIENTED_EDGE ( 'NONE', *, *, #6640, .F. ) ;
#18185=VERTEX_POINT ( 'NONE', #18959 ) ;
#18187=CIRCLE ( 'NONE', #12520, 88.00000000000000000 ) ;
#18189=DIRECTION ( 'NONE',  ( -1.000000000000000000, 0.000000000000000000, 0.000000000000000000 ) ) ;
#18191=CARTESIAN_POINT ( 'NONE',  ( 0.000000000000000000, -24.89070495400792637, 84.40647372620493627 ) ) ;
#18193=CARTESIAN_POINT ( 'NONE',  ( 10.00000000000000000, 8.925965667930086056, -92.06933331948771126 ) ) ;
#18196=VERTEX_POINT ( 'NONE', #19162 ) ;
#18198=CARTESIAN_POINT ( 'NONE',  ( 10.00000000000000000, 0.000000000000000000, 0.000000000000000000 ) ) ;
#18199=AXIS2_PLACEMENT_3D ( 'NONE', #9633, #18277, #1692 ) ;
#18203=AXIS2_PLACEMENT_3D ( 'NONE', #20598, #10219, #3482 ) ;
#18205=ORIENTED_EDGE ( 'NONE', *, *, #18430, .F. ) ;
#18206=CARTESIAN_POINT ( 'NONE',  ( 10.00000000000000000, 0.000000000000000000, 0.000000000000000000 ) ) ;
#18208=ORIENTED_EDGE ( 'NONE', *, *, #7876, .F. ) ;
#18209=CARTESIAN_POINT ( 'NONE',  ( 10.00000000000000000, -37.96946988134122591, -76.11510229470897571 ) ) ;
#18217=ADVANCED_FACE ( 'NONE', ( #6136 ), #9421, .F. ) ;
#18218=CIRCLE ( 'NONE', #9360, 44.99999999999999289 ) ;
#18219=DIRECTION ( 'NONE',  ( 0.000000000000000000, 4.433182216385175439E-15, -1.000000000000000000 ) ) ;
#18221=DIRECTION ( 'NONE',  ( 0.000000000000000000, 0.9702957262759971391, -0.2419218955996649545 ) ) ;
#18222=CIRCLE ( 'NONE', #3036, 44.99999999999999289 ) ;
#18224=CARTESIAN_POINT ( 'NONE',  ( 0.000000000000000000, 0.000000000000000000, 0.000000000000000000 ) ) ;
#18227=CARTESIAN_POINT ( 'NONE',  ( 0.000000000000000000, 0.000000000000000000, 0.000000000000000000 ) ) ;
#18228=CARTESIAN_POINT ( 'NONE',  ( 10.00000000000000000, -71.72924546249915068, -45.71766382684744201 ) ) ;
#18234=CIRCLE ( 'NONE', #5894, 44.99999999999998579 ) ;
#18235=ORIENTED_EDGE ( 'NONE', *, *, #1119, .F. ) ;
#18236=CIRCLE ( 'NONE', #17172, 44.99999999999998579 ) ;
#18238=ORIENTED_EDGE ( 'NONE', *, *, #2307, .F. ) ;
#18242=EDGE_CURVE ( 'NONE', #13893, #15534, #12609, .T. ) ;
#18243=EDGE_CURVE ( 'NONE', #19663, #6192, #6285, .T. ) ;
#18244=EDGE_CURVE ( 'NONE', #1355, #21597, #9107, .T. ) ;
#18245=DIRECTION ( 'NONE',  ( 0.000000000000000000, 0.000000000000000000, 1.000000000000000000 ) ) ;
#18247=EDGE_CURVE ( 'NONE', #9731, #6423, #4864, .T. ) ;
#18250=AXIS2_PLACEMENT_3D ( 'NONE', #20206, #21749, #6418 ) ;
#18254=FACE_OUTER_BOUND ( 'NONE', #14135, .T. ) ;
#18255=VERTEX_POINT ( 'NONE', #4023 ) ;
#18256=CARTESIAN_POINT ( 'NONE',  ( 0.000000000000000000, -43.18649929580143976, -73.28107340219457910 ) ) ;
#18260=ADVANCED_FACE ( 'NONE', ( #2369 ), #12526, .F. ) ;
#18262=VERTEX_POINT ( 'NONE', #15744 ) ;
#18264=DIRECTION ( 'NONE',  ( -1.000000000000000000, 0.000000000000000000, 0.000000000000000000 ) ) ;
#18265=ORIENTED_EDGE ( 'NONE', *, *, #21120, .F. ) ;
#18266=ORIENTED_EDGE ( 'NONE', *, *, #9993, .T. ) ;
#18268=DIRECTION ( 'NONE',  ( -1.000000000000000000, 0.000000000000000000, -0.000000000000000000 ) ) ;
#18269=ORIENTED_EDGE ( 'NONE', *, *, #16020, .F. ) ;
#18273=CARTESIAN_POINT ( 'NONE',  ( 10.00000000000000000, 84.33453774737657227, 11.08490790852157559 ) ) ;
#18275=CARTESIAN_POINT ( 'NONE',  ( 10.00000000000000000, -43.18649929580243452, 73.28107340219401067 ) ) ;
#18277=DIRECTION ( 'NONE',  ( -1.000000000000000000, -0.000000000000000000, 0.000000000000000000 ) ) ;
#18280=AXIS2_PLACEMENT_3D ( 'NONE', #1832, #500, #17304 ) ;
#18281=ORIENTED_EDGE ( 'NONE', *, *, #1784, .T. ) ;
#18282=AXIS2_PLACEMENT_3D ( 'NONE', #19983, #2960, #9685 ) ;
#18286=CARTESIAN_POINT ( 'NONE',  ( 10.00000000000000000, 52.34334029047981574, -76.26670130689429072 ) ) ;
#18291=VERTEX_POINT ( 'NONE', #5912 ) ;
#18293=AXIS2_PLACEMENT_3D ( 'NONE', #11958, #15588, #8744 ) ;
#18294=VECTOR ( 'NONE', #13399, 1000.000000000000000 ) ;
#18298=AXIS2_PLACEMENT_3D ( 'NONE', #3136, #11538, #6577 ) ;
#18299=ORIENTED_EDGE ( 'NONE', *, *, #13124, .T. ) ;
#18303=ADVANCED_FACE ( 'NONE', ( #929 ), #7674, .F. ) ;
#18305=DIRECTION ( 'NONE',  ( 1.000000000000000000, 0.000000000000000000, 0.000000000000000000 ) ) ;
#18306=DIRECTION ( 'NONE',  ( -1.000000000000000000, -0.000000000000000000, 0.000000000000000000 ) ) ;
#18308=CARTESIAN_POINT ( 'NONE',  ( 10.00000000000000000, 87.17509410653667601, -30.93441398372498341 ) ) ;
#18309=FACE_OUTER_BOUND ( 'NONE', #18699, .T. ) ;
#18311=ORIENTED_EDGE ( 'NONE', *, *, #4161, .T. ) ;
#18313=AXIS2_PLACEMENT_3D ( 'NONE', #4538, #14248, #19341 ) ;
#18317=CIRCLE ( 'NONE', #21126, 92.50100000000000477 ) ;
#18319=AXIS2_PLACEMENT_3D ( 'NONE', #21556, #16254, #9940 ) ;
#18324=ORIENTED_EDGE ( 'NONE', *, *, #15783, .F. ) ;
#18326=ORIENTED_EDGE ( 'NONE', *, *, #11572, .F. ) ;
#18327=VERTEX_POINT ( 'NONE', #4355 ) ;
#18328=CIRCLE ( 'NONE', #12965, 92.50100000000000477 ) ;
#18329=DIRECTION ( 'NONE',  ( 1.000000000000000000, 0.000000000000000000, 0.000000000000000000 ) ) ;
#18330=VERTEX_POINT ( 'NONE', #14520 ) ;
#18331=CYLINDRICAL_SURFACE ( 'NONE', #13027, 88.00000000000000000 ) ;
#18332=DIRECTION ( 'NONE',  ( -1.000000000000000000, -0.000000000000000000, -0.000000000000000000 ) ) ;
#18334=CIRCLE ( 'NONE', #14069, 44.99999999999998579 ) ;
#18336=VECTOR ( 'NONE', #10792, 1000.000000000000000 ) ;
#18337=CIRCLE ( 'NONE', #8087, 92.50100000000000477 ) ;
#18338=CARTESIAN_POINT ( 'NONE',  ( 0.000000000000000000, 23.10190250628833297, 89.56973317806607326 ) ) ;
#18339=DIRECTION ( 'NONE',  ( 0.000000000000000000, 0.000000000000000000, -1.000000000000000000 ) ) ;
#18343=DIRECTION ( 'NONE',  ( -1.000000000000000000, -0.000000000000000000, 0.000000000000000000 ) ) ;
#18344=ORIENTED_EDGE ( 'NONE', *, *, #13363, .T. ) ;
#18345=CARTESIAN_POINT ( 'NONE',  ( 10.00000000000000000, 41.21966518006070146, -82.80926399530243032 ) ) ;
#18347=CIRCLE ( 'NONE', #14448, 44.99999999999999289 ) ;
#18348=VERTEX_POINT ( 'NONE', #16282 ) ;
#18349=AXIS2_PLACEMENT_3D ( 'NONE', #292, #9110, #18961 ) ;
#18350=AXIS2_PLACEMENT_3D ( 'NONE', #13676, #20542, #13452 ) ;
#18352=VERTEX_POINT ( 'NONE', #6461 ) ;
#18354=ORIENTED_EDGE ( 'NONE', *, *, #21225, .F. ) ;
#18355=DIRECTION ( 'NONE',  ( 1.000000000000000000, 0.000000000000000000, 0.000000000000000000 ) ) ;
#18357=DIRECTION ( 'NONE',  ( -1.000000000000000000, -0.000000000000000000, -0.000000000000000000 ) ) ;
#18358=CARTESIAN_POINT ( 'NONE',  ( 0.000000000000000000, 75.27139873020885830, 53.76477968147837316 ) ) ;
#18359=FACE_OUTER_BOUND ( 'NONE', #8574, .T. ) ;
#18360=DIRECTION ( 'NONE',  ( 0.000000000000000000, 0.000000000000000000, 1.000000000000000000 ) ) ;
#18363=AXIS2_PLACEMENT_3D ( 'NONE', #15297, #8676, #16739 ) ;
#18364=FACE_OUTER_BOUND ( 'NONE', #5054, .T. ) ;
#18365=DIRECTION ( 'NONE',  ( 0.000000000000000000, 0.000000000000000000, 1.000000000000000000 ) ) ;
#18366=VERTEX_POINT ( 'NONE', #11311 ) ;
#18367=DIRECTION ( 'NONE',  ( 1.000000000000000000, 0.000000000000000000, 0.000000000000000000 ) ) ;
#18369=VERTEX_POINT ( 'NONE', #13075 ) ;
#18372=ORIENTED_EDGE ( 'NONE', *, *, #16541, .F. ) ;
#18373=CIRCLE ( 'NONE', #21540, 44.99999999999999289 ) ;
#18374=CARTESIAN_POINT ( 'NONE',  ( 0.000000000000000000, -84.79630770241078608, -6.691460262316255125 ) ) ;
#18375=ORIENTED_EDGE ( 'NONE', *, *, #7863, .F. ) ;
#18378=DIRECTION ( 'NONE',  ( 0.000000000000000000, -0.4067366430758069806, 0.9135454576425978690 ) ) ;
#18379=VERTEX_POINT ( 'NONE', #9534 ) ;
#18380=DIRECTION ( 'NONE',  ( 0.000000000000000000, 0.000000000000000000, 1.000000000000000000 ) ) ;
#18381=LINE ( 'NONE', #9956, #1137 ) ;
#18382=EDGE_CURVE ( 'NONE', #11418, #16010, #6252, .T. ) ;
#18384=DIRECTION ( 'NONE',  ( 0.000000000000000000, 0.000000000000000000, 1.000000000000000000 ) ) ;
#18386=DIRECTION ( 'NONE',  ( 1.000000000000000000, -0.000000000000000000, -0.000000000000000000 ) ) ;
#18387=ADVANCED_FACE ( 'NONE', ( #18394 ), #9871, .F. ) ;
#18388=DIRECTION ( 'NONE',  ( 0.000000000000000000, -0.3420201433256568890, -0.9396926207859125357 ) ) ;
#18389=CARTESIAN_POINT ( 'NONE',  ( 5.000000000000000000, 81.34229909304724515, -33.57723005635285318 ) ) ;
#18391=ADVANCED_FACE ( 'NONE', ( #18061 ), #17956, .F. ) ;
#18393=EDGE_CURVE ( 'NONE', #3473, #13081, #8755, .T. ) ;
#18394=FACE_OUTER_BOUND ( 'NONE', #1023, .T. ) ;
#18395=EDGE_CURVE ( 'NONE', #10561, #17030, #7893, .T. ) ;
#18396=CARTESIAN_POINT ( 'NONE',  ( 0.000000000000000000, 0.000000000000000000, 0.000000000000000000 ) ) ;
#18397=ORIENTED_EDGE ( 'NONE', *, *, #20980, .T. ) ;
#18398=CARTESIAN_POINT ( 'NONE',  ( 10.00000000000000000, 64.95266917914399585, -59.37298010462904330 ) ) ;
#18399=ORIENTED_EDGE ( 'NONE', *, *, #4618, .T. ) ;
#18403=VERTEX_POINT ( 'NONE', #2913 ) ;
#18405=CARTESIAN_POINT ( 'NONE',  ( 10.00000000000000000, 3.974475837766159980, -92.41557521768187655 ) ) ;
#18406=DIRECTION ( 'NONE',  ( -1.000000000000000000, 0.000000000000000000, 0.000000000000000000 ) ) ;
#18407=ORIENTED_EDGE ( 'NONE', *, *, #7869, .F. ) ;
#18410=DIRECTION ( 'NONE',  ( 0.000000000000000000, -1.680754301168640043E-14, -1.000000000000000000 ) ) ;
#18411=DIRECTION ( 'NONE',  ( 0.000000000000000000, 0.000000000000000000, 1.000000000000000000 ) ) ;
#18413=CARTESIAN_POINT ( 'NONE',  ( 10.00000000000000000, 88.70892494636740366, 26.21376805916615282 ) ) ;
#18414=CARTESIAN_POINT ( 'NONE',  ( 10.00000000000000000, -14.02138820414853448, -83.89630571862299746 ) ) ;
#18418=EDGE_CURVE ( 'NONE', #4497, #13650, #10158, .T. ) ;
#18419=FACE_OUTER_BOUND ( 'NONE', #8866, .T. ) ;
#18424=VERTEX_POINT ( 'NONE', #16393 ) ;
#18428=ORIENTED_EDGE ( 'NONE', *, *, #12834, .F. ) ;
#18429=CARTESIAN_POINT ( 'NONE',  ( 5.000000000000002665, -86.54587337002867287, -15.93147207947093236 ) ) ;
#18430=EDGE_CURVE ( 'NONE', #12429, #18327, #20153, .T. ) ;
#18433=DIRECTION ( 'NONE',  ( 0.000000000000000000, -0.4067366430758069806, 0.9135454576425978690 ) ) ;
#18434=EDGE_LOOP ( 'NONE', ( #3027, #19139, #6821, #4278 ) ) ;
#18436=CARTESIAN_POINT ( 'NONE',  ( 10.00000000000000000, 72.53479564998846740, -44.42851404693280415 ) ) ;
#18437=DIRECTION ( 'NONE',  ( 1.000000000000000000, -0.000000000000000000, -0.000000000000000000 ) ) ;
#18439=EDGE_CURVE ( 'NONE', #3876, #7736, #11213, .T. ) ;
#18440=( LENGTH_UNIT ( ) NAMED_UNIT ( * ) SI_UNIT ( .MILLI., .METRE. ) );
#18441=DIRECTION ( 'NONE',  ( -1.000000000000000000, -0.000000000000000000, -0.000000000000000000 ) ) ;
#18442=CARTESIAN_POINT ( 'NONE',  ( 10.00000000000000000, 85.05652083079334602, 0.7600687895874258526 ) ) ;
#18443=ADVANCED_FACE ( 'NONE', ( #14845 ), #14740, .F. ) ;
#18444=CARTESIAN_POINT ( 'NONE',  ( 10.00000000000000000, -61.33825423015729683, 69.23910433415923649 ) ) ;
#18445=CARTESIAN_POINT ( 'NONE',  ( 10.00000000000000000, -66.01871308925505843, 64.79170103522997692 ) ) ;
#18447=ORIENTED_EDGE ( 'NONE', *, *, #17706, .F. ) ;
#18449=ORIENTED_EDGE ( 'NONE', *, *, #1192, .T. ) ;
#18450=ORIENTED_EDGE ( 'NONE', *, *, #13241, .F. ) ;
#18451=AXIS2_PLACEMENT_3D ( 'NONE', #15814, #11276, #773 ) ;
#18452=ORIENTED_EDGE ( 'NONE', *, *, #20181, .T. ) ;
#18454=CARTESIAN_POINT ( 'NONE',  ( 10.00000000000000000, -84.33453774737664332, 11.08490790852103380 ) ) ;
#18456=ORIENTED_EDGE ( 'NONE', *, *, #18141, .T. ) ;
#18457=DIRECTION ( 'NONE',  ( -1.000000000000000000, 0.000000000000000000, -0.000000000000000000 ) ) ;
#18458=DIRECTION ( 'NONE',  ( 1.000000000000000000, 0.000000000000000000, 0.000000000000000000 ) ) ;
#18460=AXIS2_PLACEMENT_3D ( 'NONE', #4628, #21095, #11354 ) ;
#18465=ORIENTED_EDGE ( 'NONE', *, *, #2325, .T. ) ;
#18468=AXIS2_PLACEMENT_3D ( 'NONE', #19423, #975, #16226 ) ;
#18473=EDGE_LOOP ( 'NONE', ( #3614, #18046, #12376, #12478 ) ) ;
#18477=CARTESIAN_POINT ( 'NONE',  ( 10.00000000000000000, 45.60224695560570041, 80.47900393021744492 ) ) ;
#18480=CARTESIAN_POINT ( 'NONE',  ( 0.000000000000000000, 81.34229909304679040, 33.57723005635394742 ) ) ;
#18481=DIRECTION ( 'NONE',  ( 1.000000000000000000, -0.000000000000000000, -0.000000000000000000 ) ) ;
#18482=CARTESIAN_POINT ( 'NONE',  ( 10.00000000000000000, -27.00677879428973682, -80.65868421664460186 ) ) ;
#18483=EDGE_CURVE ( 'NONE', #6607, #10149, #6300, .T. ) ;
#18488=FACE_OUTER_BOUND ( 'NONE', #21819, .T. ) ;
#18492=DIRECTION ( 'NONE',  ( -1.000000000000000000, 0.000000000000000000, 0.000000000000000000 ) ) ;
#18493=EDGE_CURVE ( 'NONE', #14806, #9696, #1695, .T. ) ;
#18494=AXIS2_PLACEMENT_3D ( 'NONE', #14618, #17950, #2689 ) ;
#18497=DIRECTION ( 'NONE',  ( -1.000000000000000000, 0.000000000000000000, 0.000000000000000000 ) ) ;
#18499=EDGE_LOOP ( 'NONE', ( #77, #3305, #2067, #13551 ) ) ;
#18500=AXIS2_PLACEMENT_3D ( 'NONE', #13986, #18971, #17528 ) ;
#18501=ORIENTED_EDGE ( 'NONE', *, *, #13784, .T. ) ;
#18504=VERTEX_POINT ( 'NONE', #17049 ) ;
#18506=DIRECTION ( 'NONE',  ( 0.000000000000000000, -0.9702957262759938084, -0.2419218955996777498 ) ) ;
#18507=ORIENTED_EDGE ( 'NONE', *, *, #10970, .T. ) ;
#18508=CIRCLE ( 'NONE', #3672, 44.99999999999999289 ) ;
#18509=EDGE_CURVE ( 'NONE', #6423, #12565, #21109, .T. ) ;
#18510=LINE ( 'NONE', #15287, #4039 ) ;
#18512=EDGE_CURVE ( 'NONE', #16592, #4702, #10410, .T. ) ;
#18513=CARTESIAN_POINT ( 'NONE',  ( 10.00000000000000000, 0.000000000000000000, 0.000000000000000000 ) ) ;
#18514=EDGE_CURVE ( 'NONE', #5375, #21588, #15271, .T. ) ;
#18516=CARTESIAN_POINT ( 'NONE',  ( 5.000000000000000000, 68.93609746931237225, -54.69748134696388320 ) ) ;
#18517=LINE ( 'NONE', #8237, #4623 ) ;
#18519=ORIENTED_EDGE ( 'NONE', *, *, #18512, .T. ) ;
#18521=CYLINDRICAL_SURFACE ( 'NONE', #18710, 44.99999999999999289 ) ;
#18523=EDGE_LOOP ( 'NONE', ( #7141, #11863, #12090, #18118 ) ) ;
#18524=LINE ( 'NONE', #6392, #605 ) ;
#18525=EDGE_CURVE ( 'NONE', #11272, #15501, #10520, .T. ) ;
#18526=ORIENTED_EDGE ( 'NONE', *, *, #10310, .T. ) ;
#18528=CIRCLE ( 'NONE', #20995, 88.00000000000000000 ) ;
#18532=CARTESIAN_POINT ( 'NONE',  ( -10.00000000000000000, 0.000000000000000000, 88.00000000000000000 ) ) ;
#18534=VECTOR ( 'NONE', #20387, 1000.000000000000000 ) ;
#18536=ORIENTED_EDGE ( 'NONE', *, *, #11551, .F. ) ;
#18538=CYLINDRICAL_SURFACE ( 'NONE', #17776, 44.99999999999999289 ) ;
#18539=VERTEX_POINT ( 'NONE', #17165 ) ;
#18540=DIRECTION ( 'NONE',  ( 0.000000000000000000, 0.000000000000000000, 1.000000000000000000 ) ) ;
#18541=DIRECTION ( 'NONE',  ( 0.000000000000000000, 0.000000000000000000, 1.000000000000000000 ) ) ;
#18542=CARTESIAN_POINT ( 'NONE',  ( 5.000000000000000000, 83.48638250753266732, -27.82128566055030916 ) ) ;
#18544=DIRECTION ( 'NONE',  ( -1.000000000000000000, -0.000000000000000000, 0.000000000000000000 ) ) ;
#18545=EDGE_CURVE ( 'NONE', #14663, #17231, #14749, .T. ) ;
#18546=VECTOR ( 'NONE', #10079, 1000.000000000000000 ) ;
#18547=CARTESIAN_POINT ( 'NONE',  ( 5.000000000000000000, 68.93609746931163329, 54.69748134696484954 ) ) ;
#18549=CARTESIAN_POINT ( 'NONE',  ( 5.000000000000000000, -52.25832601289046409, -70.80301803122840454 ) ) ;
#18552=CARTESIAN_POINT ( 'NONE',  ( 10.00000000000000000, 35.34277389771654043, -85.48288328206348297 ) ) ;
#18553=CIRCLE ( 'NONE', #12178, 44.99999999999999289 ) ;
#18557=VERTEX_POINT ( 'NONE', #3674 ) ;
#18559=EDGE_LOOP ( 'NONE', ( #16178, #18745, #2002, #8049 ) ) ;
#18561=LINE ( 'NONE', #3416, #649 ) ;
#18562=EDGE_CURVE ( 'NONE', #535, #6588, #1700, .T. ) ;
#18563=VERTEX_POINT ( 'NONE', #18606 ) ;
#18565=CIRCLE ( 'NONE', #10421, 44.99999999999999289 ) ;
#18567=VECTOR ( 'NONE', #3487, 1000.000000000000000 ) ;
#18568=VECTOR ( 'NONE', #2039, 1000.000000000000000 ) ;
#18569=ADVANCED_FACE ( 'NONE', ( #18720 ), #10300, .F. ) ;
#18571=DIRECTION ( 'NONE',  ( 0.000000000000000000, -0.06975647374413235235, 0.9975640502598237536 ) ) ;
#18574=DIRECTION ( 'NONE',  ( 0.000000000000000000, -8.943463253924875462E-15, -1.000000000000000000 ) ) ;
#18575=CARTESIAN_POINT ( 'NONE',  ( -10.00000000000000000, 0.000000000000000000, 0.000000000000000000 ) ) ;
#18576=LINE ( 'NONE', #3430, #21063 ) ;
#18577=DIRECTION ( 'NONE',  ( 1.000000000000000000, 0.000000000000000000, 0.000000000000000000 ) ) ;
#18578=CYLINDRICAL_SURFACE ( 'NONE', #13307, 44.99999999999999289 ) ;
#18579=CARTESIAN_POINT ( 'NONE',  ( 10.00000000000000000, 0.000000000000000000, 0.000000000000000000 ) ) ;
#18580=ORIENTED_EDGE ( 'NONE', *, *, #8143, .F. ) ;
#18581=VECTOR ( 'NONE', #11528, 1000.000000000000000 ) ;
#18582=CARTESIAN_POINT ( 'NONE',  ( 10.00000000000000000, -75.27139873020921357, 53.76477968147791131 ) ) ;
#18584=ORIENTED_EDGE ( 'NONE', *, *, #14877, .T. ) ;
#18585=ORIENTED_EDGE ( 'NONE', *, *, #19302, .F. ) ;
#18586=DIRECTION ( 'NONE',  ( -1.000000000000000000, -0.000000000000000000, -0.000000000000000000 ) ) ;
#18588=CARTESIAN_POINT ( 'NONE',  ( 0.000000000000000000, 0.000000000000000000, 0.000000000000000000 ) ) ;
#18589=ORIENTED_EDGE ( 'NONE', *, *, #14796, .T. ) ;
#18590=ORIENTED_EDGE ( 'NONE', *, *, #785, .F. ) ;
#18591=FACE_OUTER_BOUND ( 'NONE', #16317, .T. ) ;
#18592=VECTOR ( 'NONE', #7690, 1000.000000000000000 ) ;
#18593=ORIENTED_EDGE ( 'NONE', *, *, #3297, .F. ) ;
#18594=AXIS2_PLACEMENT_3D ( 'NONE', #16003, #17902, #10929 ) ;
#18595=FACE_OUTER_BOUND ( 'NONE', #16649, .T. ) ;
#18596=CARTESIAN_POINT ( 'NONE',  ( 10.00000000000000000, -35.34277389771592226, 85.48288328206373876 ) ) ;
#18598=LINE ( 'NONE', #20250, #7993 ) ;
#18604=CIRCLE ( 'NONE', #13662, 88.00000000000000000 ) ;
#18605=CIRCLE ( 'NONE', #1319, 88.00000000000000000 ) ;
#18606=CARTESIAN_POINT ( 'NONE',  ( 0.000000000000000000, -78.80192417387952730, 39.16958956249271040 ) ) ;
#18607=DIRECTION ( 'NONE',  ( 0.000000000000000000, 0.000000000000000000, 1.000000000000000000 ) ) ;
#18608=VERTEX_POINT ( 'NONE', #13734 ) ;
#18610=CYLINDRICAL_SURFACE ( 'NONE', #7250, 44.99999999999999289 ) ;
#18613=ORIENTED_EDGE ( 'NONE', *, *, #6102, .T. ) ;
#18614=LINE ( 'NONE', #20270, #14575 ) ;
#18617=LINE ( 'NONE', #18405, #2257 ) ;
#18618=CARTESIAN_POINT ( 'NONE',  ( 0.000000000000000000, 0.000000000000000000, 0.000000000000000000 ) ) ;
#18619=ADVANCED_FACE ( 'NONE', ( #12496 ), #7330, .F. ) ;
#18625=DIRECTION ( 'NONE',  ( 0.000000000000000000, -7.093091546216279124E-15, 1.000000000000000000 ) ) ;
#18627=VECTOR ( 'NONE', #15108, 1000.000000000000000 ) ;
#18629=CARTESIAN_POINT ( 'NONE',  ( 10.00000000000000000, 46.93287725819874368, -70.94007663282398823 ) ) ;
#18632=CARTESIAN_POINT ( 'NONE',  ( 10.00000000000000000, -92.32475887865419395, -5.707354816231494432 ) ) ;
#18634=ORIENTED_EDGE ( 'NONE', *, *, #2337, .F. ) ;
#18635=LINE ( 'NONE', #287, #21799 ) ;
#18636=ORIENTED_EDGE ( 'NONE', *, *, #4059, .F. ) ;
#18641=ADVANCED_FACE ( 'NONE', ( #17701 ), #5887, .F. ) ;
#18645=CARTESIAN_POINT ( 'NONE',  ( 0.000000000000000000, -81.55207211302094095, 24.17537951050038814 ) ) ;
#18647=EDGE_LOOP ( 'NONE', ( #14574, #19339, #20660, #8259 ) ) ;
#18648=ORIENTED_EDGE ( 'NONE', *, *, #8749, .T. ) ;
#18650=ORIENTED_EDGE ( 'NONE', *, *, #9866, .T. ) ;
#18651=VECTOR ( 'NONE', #16139, 1000.000000000000000 ) ;
#18652=DIRECTION ( 'NONE',  ( 0.000000000000000000, 0.000000000000000000, 1.000000000000000000 ) ) ;
#18653=LINE ( 'NONE', #20310, #11090 ) ;
#18654=DIRECTION ( 'NONE',  ( 0.000000000000000000, 0.8987940462991680368, -0.4383711467890751279 ) ) ;
#18656=DIRECTION ( 'NONE',  ( 1.000000000000000000, 0.000000000000000000, 0.000000000000000000 ) ) ;
#18657=EDGE_CURVE ( 'NONE', #15964, #16742, #997, .T. ) ;
#18658=AXIS2_PLACEMENT_3D ( 'NONE', #14577, #21318, #6201 ) ;
#18659=AXIS2_PLACEMENT_3D ( 'NONE', #2292, #17549, #7279 ) ;
#18660=DIRECTION ( 'NONE',  ( 1.000000000000000000, 0.000000000000000000, 0.000000000000000000 ) ) ;
#18663=AXIS2_PLACEMENT_3D ( 'NONE', #6545, #16473, #11614 ) ;
#18664=ADVANCED_FACE ( 'NONE', ( #16032 ), #10955, .F. ) ;
#18665=DIRECTION ( 'NONE',  ( -1.000000000000000000, -0.000000000000000000, -0.000000000000000000 ) ) ;
#18667=DIRECTION ( 'NONE',  ( 1.000000000000000000, 0.000000000000000000, 0.000000000000000000 ) ) ;
#18668=ORIENTED_EDGE ( 'NONE', *, *, #13462, .F. ) ;
#18669=EDGE_CURVE ( 'NONE', #9349, #18403, #9181, .T. ) ;
#18670=DIRECTION ( 'NONE',  ( -1.000000000000000000, 0.000000000000000000, -0.000000000000000000 ) ) ;
#18671=EDGE_CURVE ( 'NONE', #2869, #15286, #9097, .T. ) ;
#18672=ORIENTED_EDGE ( 'NONE', *, *, #6950, .F. ) ;
#18673=FACE_OUTER_BOUND ( 'NONE', #16285, .T. ) ;
#18674=ORIENTED_EDGE ( 'NONE', *, *, #9163, .T. ) ;
#18675=AXIS2_PLACEMENT_3D ( 'NONE', #20545, #19102, #8606 ) ;
#18676=EDGE_CURVE ( 'NONE', #20112, #8941, #17924, .T. ) ;
#18677=ORIENTED_EDGE ( 'NONE', *, *, #12834, .T. ) ;
#18678=AXIS2_PLACEMENT_3D ( 'NONE', #14779, #10005, #1413 ) ;
#18680=ORIENTED_EDGE ( 'NONE', *, *, #15535, .F. ) ;
#18681=DIRECTION ( 'NONE',  ( 1.000000000000000000, 0.000000000000000000, 0.000000000000000000 ) ) ;
#18682=ORIENTED_EDGE ( 'NONE', *, *, #16757, .F. ) ;
#18685=EDGE_CURVE ( 'NONE', #4587, #13603, #17375, .T. ) ;
#18689=EDGE_CURVE ( 'NONE', #6588, #16623, #9817, .T. ) ;
#18690=CARTESIAN_POINT ( 'NONE',  ( 10.00000000000000000, 92.32475887865426500, 5.707354816230855832 ) ) ;
#18691=DIRECTION ( 'NONE',  ( -1.000000000000000000, -0.000000000000000000, -0.000000000000000000 ) ) ;
#18693=CIRCLE ( 'NONE', #20107, 88.00000000000000000 ) ;
#18694=AXIS2_PLACEMENT_3D ( 'NONE', #183, #6934, #13654 ) ;
#18695=ORIENTED_EDGE ( 'NONE', *, *, #14861, .F. ) ;
#18696=VECTOR ( 'NONE', #10675, 1000.000000000000000 ) ;
#18698=DIRECTION ( 'NONE',  ( -1.000000000000000000, 0.000000000000000000, 0.000000000000000000 ) ) ;
#18699=EDGE_LOOP ( 'NONE', ( #14681, #7340, #644, #14702 ) ) ;
#18700=EDGE_LOOP ( 'NONE', ( #4953, #7282, #20471, #401 ) ) ;
#18701=DIRECTION ( 'NONE',  ( -1.000000000000000000, -0.000000000000000000, 0.000000000000000000 ) ) ;
#18702=EDGE_CURVE ( 'NONE', #6010, #15453, #7532, .T. ) ;
#18704=DIRECTION ( 'NONE',  ( -1.000000000000000000, -0.000000000000000000, -0.000000000000000000 ) ) ;
#18705=ORIENTED_EDGE ( 'NONE', *, *, #395, .T. ) ;
#18708=ORIENTED_EDGE ( 'NONE', *, *, #17458, .T. ) ;
#18709=AXIS2_PLACEMENT_3D ( 'NONE', #8651, #370, #7437 ) ;
#18710=AXIS2_PLACEMENT_3D ( 'NONE', #1828, #5035, #11992 ) ;
#18712=DIRECTION ( 'NONE',  ( 1.000000000000000000, 0.000000000000000000, 0.000000000000000000 ) ) ;
#18714=CARTESIAN_POINT ( 'NONE',  ( 0.000000000000000000, -69.74988376404053270, 53.65588238863315240 ) ) ;
#18715=DIRECTION ( 'NONE',  ( -1.000000000000000000, -0.000000000000000000, 0.000000000000000000 ) ) ;
#18716=DIRECTION ( 'NONE',  ( 0.000000000000000000, -0.9271838545667832054, -0.3746065934159226729 ) ) ;
#18717=CARTESIAN_POINT ( 'NONE',  ( 10.00000000000000000, -74.74361964203200159, -40.60271866773624083 ) ) ;
#18718=ORIENTED_EDGE ( 'NONE', *, *, #21534, .F. ) ;
#18720=FACE_OUTER_BOUND ( 'NONE', #11154, .T. ) ;
#18721=DIRECTION ( 'NONE',  ( 0.000000000000000000, 0.000000000000000000, -1.000000000000000000 ) ) ;
#18722=ORIENTED_EDGE ( 'NONE', *, *, #1192, .F. ) ;
#18723=CARTESIAN_POINT ( 'NONE',  ( 10.00000000000000000, -23.10190250628773967, -89.56973317806621537 ) ) ;
#18729=DIRECTION ( 'NONE',  ( 1.000000000000000000, 0.000000000000000000, 0.000000000000000000 ) ) ;
#18730=DIRECTION ( 'NONE',  ( 0.000000000000000000, -0.5299192642331944647, -0.8480480961564325071 ) ) ;
#18731=CYLINDRICAL_SURFACE ( 'NONE', #10515, 44.99999999999998579 ) ;
#18735=CARTESIAN_POINT ( 'NONE',  ( 0.000000000000000000, -46.93287725819829603, 70.94007663282431508 ) ) ;
#18736=DIRECTION ( 'NONE',  ( -1.000000000000000000, -0.000000000000000000, 0.000000000000000000 ) ) ;
#18739=VECTOR ( 'NONE', #14764, 1000.000000000000000 ) ;
#18740=CARTESIAN_POINT ( 'NONE',  ( 0.000000000000000000, 74.39348546125125949, -54.97312363261338675 ) ) ;
#18741=ORIENTED_EDGE ( 'NONE', *, *, #7436, .T. ) ;
#18745=ORIENTED_EDGE ( 'NONE', *, *, #20412, .T. ) ;
#18747=ORIENTED_EDGE ( 'NONE', *, *, #48, .T. ) ;
#18750=ORIENTED_EDGE ( 'NONE', *, *, #562, .T. ) ;
#18751=CARTESIAN_POINT ( 'NONE',  ( 10.00000000000000000, 0.000000000000000000, 0.000000000000000000 ) ) ;
#18752=DIRECTION ( 'NONE',  ( 0.000000000000000000, 8.866364432770347722E-15, -1.000000000000000000 ) ) ;
#18753=DIRECTION ( 'NONE',  ( -1.000000000000000000, 0.000000000000000000, 0.000000000000000000 ) ) ;
#18754=CYLINDRICAL_SURFACE ( 'NONE', #13945, 44.99999999999999289 ) ;
#18758=EDGE_CURVE ( 'NONE', #16476, #21231, #19702, .T. ) ;
#18760=CARTESIAN_POINT ( 'NONE',  ( 0.000000000000000000, 0.000000000000000000, 0.000000000000000000 ) ) ;
#18762=ORIENTED_EDGE ( 'NONE', *, *, #18395, .T. ) ;
#18763=CARTESIAN_POINT ( 'NONE',  ( 10.00000000000000000, 62.44821182181184582, -68.23969402963440700 ) ) ;
#18767=EDGE_LOOP ( 'NONE', ( #8678, #9767, #7075, #15528 ) ) ;
#18768=CARTESIAN_POINT ( 'NONE',  ( 10.00000000000000000, 0.000000000000000000, 0.000000000000000000 ) ) ;
#18769=ORIENTED_EDGE ( 'NONE', *, *, #21649, .F. ) ;
#18770=DIRECTION ( 'NONE',  ( -1.000000000000000000, 0.000000000000000000, -0.000000000000000000 ) ) ;
#18771=ORIENTED_EDGE ( 'NONE', *, *, #7548, .F. ) ;
#18772=EDGE_CURVE ( 'NONE', #2240, #15531, #15221, .T. ) ;
#18774=AXIS2_PLACEMENT_3D ( 'NONE', #15547, #8899, #3836 ) ;
#18775=ORIENTED_EDGE ( 'NONE', *, *, #12935, .T. ) ;
#18776=FACE_OUTER_BOUND ( 'NONE', #6293, .T. ) ;
#18780=CYLINDRICAL_SURFACE ( 'NONE', #3626, 92.50100000000000477 ) ;
#18782=AXIS2_PLACEMENT_3D ( 'NONE', #18025, #2872, #1216 ) ;
#18783=CARTESIAN_POINT ( 'NONE',  ( 10.00000000000000000, 57.06999622551897033, -66.98518889142023625 ) ) ;
#18784=ADVANCED_FACE ( 'NONE', ( #97 ), #9510, .F. ) ;
#18785=LINE ( 'NONE', #13810, #11900 ) ;
#18787=EDGE_CURVE ( 'NONE', #13543, #13174, #16363, .T. ) ;
#18788=LINE ( 'NONE', #20657, #11177 ) ;
#18789=CARTESIAN_POINT ( 'NONE',  ( 10.00000000000000000, 31.15801000616942673, -79.14775961996359399 ) ) ;
#18790=EDGE_CURVE ( 'NONE', #1972, #16720, #12936, .T. ) ;
#18791=ORIENTED_EDGE ( 'NONE', *, *, #6465, .F. ) ;
#18792=DIRECTION ( 'NONE',  ( 0.000000000000000000, 0.9702957262759972501, -0.2419218955996647880 ) ) ;
#18793=ORIENTED_EDGE ( 'NONE', *, *, #41, .F. ) ;
#18794=VERTEX_POINT ( 'NONE', #19796 ) ;
#18796=CARTESIAN_POINT ( 'NONE',  ( 10.00000000000000000, 75.27139873020885830, 53.76477968147838027 ) ) ;
#18797=ORIENTED_EDGE ( 'NONE', *, *, #7043, .T. ) ;
#18798=ORIENTED_EDGE ( 'NONE', *, *, #2160, .T. ) ;
#18799=CIRCLE ( 'NONE', #17031, 44.99999999999999289 ) ;
#18802=ORIENTED_EDGE ( 'NONE', *, *, #18949, .F. ) ;
#18804=ADVANCED_FACE ( 'NONE', ( #18673 ), #4442, .F. ) ;
#18806=CARTESIAN_POINT ( 'NONE',  ( 0.000000000000000000, 0.000000000000000000, 0.000000000000000000 ) ) ;
#18807=CARTESIAN_POINT ( 'NONE',  ( 0.000000000000000000, -21.65267340503309512, 89.93106657554424999 ) ) ;
#18808=CYLINDRICAL_SURFACE ( 'NONE', #15050, 45.00000000000000000 ) ;
#18809=CYLINDRICAL_SURFACE ( 'NONE', #21659, 44.99999999999999289 ) ;
#18811=DIRECTION ( 'NONE',  ( -1.000000000000000000, -0.000000000000000000, -0.000000000000000000 ) ) ;
#18812=AXIS2_PLACEMENT_3D ( 'NONE', #12041, #3637, #20654 ) ;
#18813=CIRCLE ( 'NONE', #20914, 92.50100000000000477 ) ;
#18815=ORIENTED_EDGE ( 'NONE', *, *, #5639, .T. ) ;
#18817=CARTESIAN_POINT ( 'NONE',  ( 10.00000000000000000, 0.000000000000000000, 0.000000000000000000 ) ) ;
#18821=VERTEX_POINT ( 'NONE', #20327 ) ;
#18822=FACE_OUTER_BOUND ( 'NONE', #19644, .T. ) ;
#18823=ADVANCED_FACE ( 'NONE', ( #14598 ), #13459, .F. ) ;
#18826=AXIS2_PLACEMENT_3D ( 'NONE', #18735, #16852, #3589 ) ;
#18828=ORIENTED_EDGE ( 'NONE', *, *, #13658, .F. ) ;
#18829=ORIENTED_EDGE ( 'NONE', *, *, #17033, .T. ) ;
#18840=DIRECTION ( 'NONE',  ( -1.000000000000000000, 0.000000000000000000, -0.000000000000000000 ) ) ;
#18846=ORIENTED_EDGE ( 'NONE', *, *, #7599, .F. ) ;
#18848=FACE_OUTER_BOUND ( 'NONE', #8919, .T. ) ;
#18849=ORIENTED_EDGE ( 'NONE', *, *, #2998, .F. ) ;
#18852=ORIENTED_EDGE ( 'NONE', *, *, #2313, .F. ) ;
#18853=CARTESIAN_POINT ( 'NONE',  ( 5.000000000000000000, 81.83745710415276164, 32.35167097270178260 ) ) ;
#18860=CARTESIAN_POINT ( 'NONE',  ( 10.00000000000000000, -57.47876254627184522, 62.70072803846370135 ) ) ;
#18862=CARTESIAN_POINT ( 'NONE',  ( 10.00000000000000000, 52.34334029047875703, 76.26670130689501548 ) ) ;
#18864=CARTESIAN_POINT ( 'NONE',  ( 10.00000000000000000, 75.45728100697598961, 39.26051685139091063 ) ) ;
#18867=AXIS2_PLACEMENT_3D ( 'NONE', #15512, #10745, #17505 ) ;
#18868=DIRECTION ( 'NONE',  ( 0.000000000000000000, 2.844946500601964266E-14, -1.000000000000000000 ) ) ;
#18870=DIRECTION ( 'NONE',  ( 0.000000000000000000, -0.2079116908177468526, -0.9781476007338083534 ) ) ;
#18871=ORIENTED_EDGE ( 'NONE', *, *, #9462, .T. ) ;
#18872=DIRECTION ( 'NONE',  ( -1.000000000000000000, -0.000000000000000000, -0.000000000000000000 ) ) ;
#18873=AXIS2_PLACEMENT_3D ( 'NONE', #10810, #5742, #5314 ) ;
#18874=DIRECTION ( 'NONE',  ( 0.000000000000000000, -0.5877852522924797984, 0.8090169943749425663 ) ) ;
#18876=LINE ( 'NONE', #7275, #16483 ) ;
#18880=CARTESIAN_POINT ( 'NONE',  ( 10.00000000000000000, -84.12297548659729785, 12.59025161326973397 ) ) ;
#18884=EDGE_CURVE ( 'NONE', #21244, #11867, #18561, .T. ) ;
#18887=DIRECTION ( 'NONE',  ( -1.000000000000000000, -0.000000000000000000, -0.000000000000000000 ) ) ;
#18890=CARTESIAN_POINT ( 'NONE',  ( 5.000000000000002665, 73.32282170386913833, -48.65967342042704757 ) ) ;
#18891=EDGE_CURVE ( 'NONE', #6765, #9927, #20763, .T. ) ;
#18894=CARTESIAN_POINT ( 'NONE',  ( 10.00000000000000000, 0.000000000000000000, 0.000000000000000000 ) ) ;
#18895=DIRECTION ( 'NONE',  ( -1.000000000000000000, -0.000000000000000000, -0.000000000000000000 ) ) ;
#18896=CYLINDRICAL_SURFACE ( 'NONE', #13208, 92.50100000000000477 ) ;
#18897=AXIS2_PLACEMENT_3D ( 'NONE', #18436, #6408, #6508 ) ;
#18898=DIRECTION ( 'NONE',  ( 0.000000000000000000, -2.929755203871941151E-14, -1.000000000000000000 ) ) ;
#18899=CARTESIAN_POINT ( 'NONE',  ( 10.00000000000000000, 3.974475837766159980, -92.41557521768187655 ) ) ;
#18900=ORIENTED_EDGE ( 'NONE', *, *, #9430, .T. ) ;
#18901=DIRECTION ( 'NONE',  ( -1.000000000000000000, -0.000000000000000000, 0.000000000000000000 ) ) ;
#18902=VECTOR ( 'NONE', #15829, 1000.000000000000000 ) ;
#18904=AXIS2_PLACEMENT_3D ( 'NONE', #3792, #11862, #12073 ) ;
#18905=AXIS2_PLACEMENT_3D ( 'NONE', #18513, #10103, #6380 ) ;
#18907=AXIS2_PLACEMENT_3D ( 'NONE', #4311, #21226, #17802 ) ;
#18909=ORIENTED_EDGE ( 'NONE', *, *, #2961, .T. ) ;
#18910=EDGE_CURVE ( 'NONE', #13052, #19662, #7389, .T. ) ;
#18911=EDGE_CURVE ( 'NONE', #21331, #16982, #15107, .T. ) ;
#18912=EDGE_CURVE ( 'NONE', #19254, #2288, #11945, .T. ) ;
#18913=EDGE_LOOP ( 'NONE', ( #7571, #6966, #6290, #18182 ) ) ;
#18917=CARTESIAN_POINT ( 'NONE',  ( 0.000000000000000000, 0.000000000000000000, 0.000000000000000000 ) ) ;
#18918=CARTESIAN_POINT ( 'NONE',  ( 10.00000000000000000, -46.89573839703219704, -79.73220629831536144 ) ) ;
#18920=DIRECTION ( 'NONE',  ( 1.000000000000000000, -0.000000000000000000, -0.000000000000000000 ) ) ;
#18921=AXIS2_PLACEMENT_3D ( 'NONE', #17621, #600, #17830 ) ;
#18922=DIRECTION ( 'NONE',  ( 0.000000000000000000, 0.000000000000000000, 1.000000000000000000 ) ) ;
#18924=ADVANCED_FACE ( 'NONE', ( #9025 ), #5302, .F. ) ;
#18925=DIRECTION ( 'NONE',  ( -1.000000000000000000, 0.000000000000000000, -0.000000000000000000 ) ) ;
#18927=VERTEX_POINT ( 'NONE', #12129 ) ;
#18930=DIRECTION ( 'NONE',  ( 1.000000000000000000, 0.000000000000000000, 0.000000000000000000 ) ) ;
#18931=EDGE_LOOP ( 'NONE', ( #19044, #10935, #10366, #15383 ) ) ;
#18933=ADVANCED_FACE ( 'NONE', ( #20639 ), #2184, .F. ) ;
#18936=VECTOR ( 'NONE', #8750, 1000.000000000000000 ) ;
#18938=ADVANCED_FACE ( 'NONE', ( #15332 ), #638, .F. ) ;
#18942=DIRECTION ( 'NONE',  ( 1.000000000000000000, 0.000000000000000000, 0.000000000000000000 ) ) ;
#18943=FACE_OUTER_BOUND ( 'NONE', #7565, .T. ) ;
#18944=DIRECTION ( 'NONE',  ( -1.000000000000000000, 0.000000000000000000, 0.000000000000000000 ) ) ;
#18945=CARTESIAN_POINT ( 'NONE',  ( 10.00000000000000000, 3.728035544476225649, 84.97818067823770605 ) ) ;
#18946=CARTESIAN_POINT ( 'NONE',  ( 10.00000000000000000, 8.134922360107273320, -84.67002113262471141 ) ) ;
#18948=CARTESIAN_POINT ( 'NONE',  ( -10.00000000000000000, 0.000000000000000000, 0.000000000000000000 ) ) ;
#18949=EDGE_CURVE ( 'NONE', #9371, #6615, #4534, .T. ) ;
#18950=AXIS2_PLACEMENT_3D ( 'NONE', #17591, #2451, #9174 ) ;
#18951=AXIS2_PLACEMENT_3D ( 'NONE', #21069, #12887, #9453 ) ;
#18952=VERTEX_POINT ( 'NONE', #14006 ) ;
#18953=EDGE_CURVE ( 'NONE', #7736, #18563, #18991, .T. ) ;
#18954=CIRCLE ( 'NONE', #6977, 44.99999999999999289 ) ;
#18956=VERTEX_POINT ( 'NONE', #13799 ) ;
#18957=EDGE_CURVE ( 'NONE', #16416, #5617, #216, .T. ) ;
#18958=EDGE_CURVE ( 'NONE', #5049, #19254, #15449, .T. ) ;
#18959=CARTESIAN_POINT ( 'NONE',  ( 0.000000000000000000, 39.87723064937119233, 83.46401306393586594 ) ) ;
#18960=ORIENTED_EDGE ( 'NONE', *, *, #8812, .T. ) ;
#18961=DIRECTION ( 'NONE',  ( 0.000000000000000000, 0.000000000000000000, 1.000000000000000000 ) ) ;
#18963=ORIENTED_EDGE ( 'NONE', *, *, #1396, .F. ) ;
#18964=( NAMED_UNIT ( * ) PLANE_ANGLE_UNIT ( ) SI_UNIT ( $, .RADIAN. ) );
#18965=CIRCLE ( 'NONE', #8380, 44.99999999999999289 ) ;
#18971=DIRECTION ( 'NONE',  ( 1.000000000000000000, 0.000000000000000000, 0.000000000000000000 ) ) ;
#18972=AXIS2_PLACEMENT_3D ( 'NONE', #7554, #19270, #5795 ) ;
#18974=DIRECTION ( 'NONE',  ( 0.000000000000000000, 0.000000000000000000, 1.000000000000000000 ) ) ;
#18975=CARTESIAN_POINT ( 'NONE',  ( 10.00000000000000000, 0.000000000000000000, 0.000000000000000000 ) ) ;
#18976=CARTESIAN_POINT ( 'NONE',  ( 10.00000000000000000, 0.000000000000000000, 0.000000000000000000 ) ) ;
#18978=LINE ( 'NONE', #10780, #21044 ) ;
#18979=CARTESIAN_POINT ( 'NONE',  ( 10.00000000000000000, 64.66851233300799606, -55.25552418572899427 ) ) ;
#18982=AXIS2_PLACEMENT_3D ( 'NONE', #4778, #10185, #16934 ) ;
#18983=CARTESIAN_POINT ( 'NONE',  ( 10.00000000000000000, 51.76708072107978609, -67.49339815138442589 ) ) ;
#18986=AXIS2_PLACEMENT_3D ( 'NONE', #11414, #1371, #8111 ) ;
#18988=ORIENTED_EDGE ( 'NONE', *, *, #13338, .T. ) ;
#18990=ORIENTED_EDGE ( 'NONE', *, *, #12702, .F. ) ;
#18991=LINE ( 'NONE', #10475, #14771 ) ;
#18992=ORIENTED_EDGE ( 'NONE', *, *, #21528, .T. ) ;
#18997=AXIS2_PLACEMENT_3D ( 'NONE', #21000, #2534, #6085 ) ;
#18998=AXIS2_PLACEMENT_3D ( 'NONE', #17828, #5901, #14171 ) ;
#18999=CARTESIAN_POINT ( 'NONE',  ( 0.000000000000000000, 57.53593069156472239, -72.42963261300903355 ) ) ;
#19000=CARTESIAN_POINT ( 'NONE',  ( 10.00000000000000000, 37.96946988134172329, 76.11510229470873412 ) ) ;
#19002=AXIS2_PLACEMENT_3D ( 'NONE', #6634, #20537, #8497 ) ;
#19003=AXIS2_PLACEMENT_3D ( 'NONE', #4433, #10731, #2340 ) ;
#19005=DIRECTION ( 'NONE',  ( -1.000000000000000000, 0.000000000000000000, 0.000000000000000000 ) ) ;
#19006=DIRECTION ( 'NONE',  ( 0.000000000000000000, 0.000000000000000000, 1.000000000000000000 ) ) ;
#19009=FACE_OUTER_BOUND ( 'NONE', #12153, .T. ) ;
#19010=EDGE_CURVE ( 'NONE', #16638, #18504, #5723, .T. ) ;
#19011=ORIENTED_EDGE ( 'NONE', *, *, #6995, .F. ) ;
#19013=VERTEX_POINT ( 'NONE', #3851 ) ;
#19016=AXIS2_PLACEMENT_3D ( 'NONE', #421, #10684, #12558 ) ;
#19017=CIRCLE ( 'NONE', #8438, 92.50100000000000477 ) ;
#19019=ORIENTED_EDGE ( 'NONE', *, *, #1699, .T. ) ;
#19023=CARTESIAN_POINT ( 'NONE',  ( 10.00000000000000000, -81.34229909304701778, 33.57723005635337898 ) ) ;
#19025=DIRECTION ( 'NONE',  ( 0.000000000000000000, 0.000000000000000000, 1.000000000000000000 ) ) ;
#19026=CARTESIAN_POINT ( 'NONE',  ( 10.00000000000000000, 56.34908017029645322, -63.71789861856395731 ) ) ;
#19027=AXIS2_PLACEMENT_3D ( 'NONE', #18860, #9194, #6944 ) ;
#19028=CARTESIAN_POINT ( 'NONE',  ( -10.00000000000000000, 0.000000000000000000, 0.000000000000000000 ) ) ;
#19029=AXIS2_PLACEMENT_3D ( 'NONE', #13326, #5044, #16427 ) ;
#19030=CARTESIAN_POINT ( 'NONE',  ( 0.000000000000000000, 0.000000000000000000, 0.000000000000000000 ) ) ;
#19032=CIRCLE ( 'NONE', #4939, 44.99999999999998579 ) ;
#19035=DIRECTION ( 'NONE',  ( 0.000000000000000000, 0.000000000000000000, 1.000000000000000000 ) ) ;
#19036=EDGE_CURVE ( 'NONE', #4200, #21244, #19354, .T. ) ;
#19037=EDGE_LOOP ( 'NONE', ( #7817, #13944, #11247, #9718 ) ) ;
#19038=DIRECTION ( 'NONE',  ( 1.000000000000000000, 0.000000000000000000, 0.000000000000000000 ) ) ;
#19040=CARTESIAN_POINT ( 'NONE',  ( 0.000000000000000000, 74.74361964203228581, -40.60271866773572214 ) ) ;
#19041=ORIENTED_EDGE ( 'NONE', *, *, #3844, .T. ) ;
#19042=FACE_OUTER_BOUND ( 'NONE', #1937, .T. ) ;
#19043=CIRCLE ( 'NONE', #16222, 44.99999999999999289 ) ;
#19044=ORIENTED_EDGE ( 'NONE', *, *, #5829, .F. ) ;
#19046=CYLINDRICAL_SURFACE ( 'NONE', #108, 45.00000000000000000 ) ;
#19047=EDGE_LOOP ( 'NONE', ( #14909, #9951, #11204, #21700 ) ) ;
#19049=DIRECTION ( 'NONE',  ( -1.000000000000000000, -0.000000000000000000, 0.000000000000000000 ) ) ;
#19051=EDGE_CURVE ( 'NONE', #11509, #18379, #20964, .T. ) ;
#19054=CARTESIAN_POINT ( 'NONE',  ( 10.00000000000000000, 75.87763420127832603, 44.57111876559751096 ) ) ;
#19055=DIRECTION ( 'NONE',  ( 0.000000000000000000, 0.000000000000000000, 1.000000000000000000 ) ) ;
#19062=CYLINDRICAL_SURFACE ( 'NONE', #5866, 45.00000000000000000 ) ;
#19063=EDGE_CURVE ( 'NONE', #15534, #21383, #13372, .T. ) ;
#19065=FACE_OUTER_BOUND ( 'NONE', #7184, .T. ) ;
#19067=DIRECTION ( 'NONE',  ( -1.000000000000000000, -0.000000000000000000, -0.000000000000000000 ) ) ;
#19068=CARTESIAN_POINT ( 'NONE',  ( 5.000000000000000000, 36.39558101400249512, -80.12091913260344711 ) ) ;
#19069=ORIENTED_EDGE ( 'NONE', *, *, #15795, .F. ) ;
#19071=ADVANCED_FACE ( 'NONE', ( #9559 ), #19415, .F. ) ;
#19072=EDGE_LOOP ( 'NONE', ( #12991, #8217, #16098, #10237 ) ) ;
#19073=ORIENTED_EDGE ( 'NONE', *, *, #7160, .F. ) ;
#19074=ORIENTED_EDGE ( 'NONE', *, *, #17361, .T. ) ;
#19078=EDGE_CURVE ( 'NONE', #1865, #13181, #4913, .T. ) ;
#19079=CARTESIAN_POINT ( 'NONE',  ( 0.000000000000000000, -86.77540292929711541, 14.62974526292689426 ) ) ;
#19081=FACE_OUTER_BOUND ( 'NONE', #47, .T. ) ;
#19082=DIRECTION ( 'NONE',  ( -1.000000000000000000, -0.000000000000000000, 0.000000000000000000 ) ) ;
#19083=EDGE_CURVE ( 'NONE', #5617, #11894, #18334, .T. ) ;
#19084=DIRECTION ( 'NONE',  ( -1.000000000000000000, 0.000000000000000000, 0.000000000000000000 ) ) ;
#19085=FACE_OUTER_BOUND ( 'NONE', #13429, .T. ) ;
#19086=VERTEX_POINT ( 'NONE', #11012 ) ;
#19089=CYLINDRICAL_SURFACE ( 'NONE', #3017, 44.99999999999999289 ) ;
#19090=AXIS2_PLACEMENT_3D ( 'NONE', #564, #7307, #5648 ) ;
#19091=CARTESIAN_POINT ( 'NONE',  ( 0.000000000000000000, 84.90234713953992696, -5.175025661882965089 ) ) ;
#19092=ORIENTED_EDGE ( 'NONE', *, *, #2255, .T. ) ;
#19093=LINE ( 'NONE', #2290, #14072 ) ;
#19094=ORIENTED_EDGE ( 'NONE', *, *, #21225, .T. ) ;
#19096=ORIENTED_EDGE ( 'NONE', *, *, #9884, .F. ) ;
#19098=VERTEX_POINT ( 'NONE', #2845 ) ;
#19099=CARTESIAN_POINT ( 'NONE',  ( 10.00000000000000000, -88.70892494636720471, -26.21376805916674613 ) ) ;
#19101=ORIENTED_EDGE ( 'NONE', *, *, #10704, .F. ) ;
#19102=DIRECTION ( 'NONE',  ( -1.000000000000000000, 0.000000000000000000, 0.000000000000000000 ) ) ;
#19103=CARTESIAN_POINT ( 'NONE',  ( 10.00000000000000000, 92.22057093985031884, 7.197311757040840696 ) ) ;
#19107=ADVANCED_FACE ( 'NONE', ( #4612 ), #7813, .F. ) ;
#19108=DIRECTION ( 'NONE',  ( -1.000000000000000000, 0.000000000000000000, 0.000000000000000000 ) ) ;
#19109=CARTESIAN_POINT ( 'NONE',  ( 10.00000000000000000, -76.53853822673953289, -43.42639941457193231 ) ) ;
#19110=CARTESIAN_POINT ( 'NONE',  ( 10.00000000000000000, -79.66702613806754130, -29.80527447819517661 ) ) ;
#19111=DIRECTION ( 'NONE',  ( -1.000000000000000000, 0.000000000000000000, -0.000000000000000000 ) ) ;
#19112=CYLINDRICAL_SURFACE ( 'NONE', #6333, 44.99999999999999289 ) ;
#19113=ORIENTED_EDGE ( 'NONE', *, *, #13544, .T. ) ;
#19114=CARTESIAN_POINT ( 'NONE',  ( 10.00000000000000000, 0.000000000000000000, 0.000000000000000000 ) ) ;
#19115=EDGE_LOOP ( 'NONE', ( #6751, #7243, #12831, #18815 ) ) ;
#19119=ORIENTED_EDGE ( 'NONE', *, *, #19332, .F. ) ;
#19121=EDGE_CURVE ( 'NONE', #6765, #14822, #3854, .T. ) ;
#19126=DIRECTION ( 'NONE',  ( 0.000000000000000000, 0.000000000000000000, 1.000000000000000000 ) ) ;
#19127=DIRECTION ( 'NONE',  ( 0.000000000000000000, 0.000000000000000000, 1.000000000000000000 ) ) ;
#19128=CARTESIAN_POINT ( 'NONE',  ( 10.00000000000000000, 16.79755869217770936, -90.96305306542237190 ) ) ;
#19129=CYLINDRICAL_SURFACE ( 'NONE', #5502, 92.50100000000000477 ) ;
#19134=CARTESIAN_POINT ( 'NONE',  ( 10.00000000000000000, -75.27139873020847460, -53.76477968147890607 ) ) ;
#19135=AXIS2_PLACEMENT_3D ( 'NONE', #11982, #15395, #6801 ) ;
#19136=CIRCLE ( 'NONE', #18460, 44.99999999999999289 ) ;
#19137=CARTESIAN_POINT ( 'NONE',  ( -10.00000000000000000, 0.000000000000000000, 0.000000000000000000 ) ) ;
#19139=ORIENTED_EDGE ( 'NONE', *, *, #14017, .T. ) ;
#19141=ORIENTED_EDGE ( 'NONE', *, *, #12863, .F. ) ;
#19142=CARTESIAN_POINT ( 'NONE',  ( 5.000000000000002665, -87.96697768756403946, 2.410567674970269358 ) ) ;
#19144=VERTEX_POINT ( 'NONE', #12891 ) ;
#19145=EDGE_CURVE ( 'NONE', #11314, #8172, #16903, .T. ) ;
#19146=EDGE_LOOP ( 'NONE', ( #12444, #10210, #18695, #14545 ) ) ;
#19147=DIRECTION ( 'NONE',  ( 1.000000000000000000, -0.000000000000000000, -0.000000000000000000 ) ) ;
#19148=CIRCLE ( 'NONE', #16687, 44.99999999999999289 ) ;
#19149=VECTOR ( 'NONE', #1986, 1000.000000000000000 ) ;
#19150=DIRECTION ( 'NONE',  ( 0.000000000000000000, 0.000000000000000000, 1.000000000000000000 ) ) ;
#19151=CARTESIAN_POINT ( 'NONE',  ( 10.00000000000000000, 67.05625154133539922, -63.71729851637743280 ) ) ;
#19152=DIRECTION ( 'NONE',  ( 0.000000000000000000, -0.8660254037844432595, 0.4999999999999919509 ) ) ;
#19153=DIRECTION ( 'NONE',  ( 0.000000000000000000, 0.9271838545667884235, -0.3746065934159096278 ) ) ;
#19154=EDGE_CURVE ( 'NONE', #10029, #11398, #13015, .T. ) ;
#19155=AXIS2_PLACEMENT_3D ( 'NONE', #3683, #19255, #9087 ) ;
#19156=LINE ( 'NONE', #12407, #4006 ) ;
#19158=ORIENTED_EDGE ( 'NONE', *, *, #9960, .F. ) ;
#19159=CARTESIAN_POINT ( 'NONE',  ( 5.000000000000002665, 79.38136668499790005, -37.98155635597233726 ) ) ;
#19162=CARTESIAN_POINT ( 'NONE',  ( 0.000000000000000000, 33.95793648385814123, 86.04239391578002483 ) ) ;
#19163=ORIENTED_EDGE ( 'NONE', *, *, #4655, .F. ) ;
#19164=CIRCLE ( 'NONE', #2568, 92.50100000000000477 ) ;
#19165=DIRECTION ( 'NONE',  ( 0.000000000000000000, 0.000000000000000000, 1.000000000000000000 ) ) ;
#19168=CIRCLE ( 'NONE', #1195, 88.00000000000000000 ) ;
#19170=ORIENTED_EDGE ( 'NONE', *, *, #5400, .T. ) ;
#19173=ORIENTED_EDGE ( 'NONE', *, *, #145, .F. ) ;
#19174=ADVANCED_FACE ( 'NONE', ( #15092 ), #13106, .T. ) ;
#19175=DIRECTION ( 'NONE',  ( 0.000000000000000000, 0.9945218953682729568, 0.1045284632676569958 ) ) ;
#19176=CARTESIAN_POINT ( 'NONE',  ( 10.00000000000000000, -86.66425444033897918, -32.33793443156484670 ) ) ;
#19177=EDGE_LOOP ( 'NONE', ( #2120, #5814, #21496, #21586 ) ) ;
#19178=ADVANCED_FACE ( 'NONE', ( #11682 ), #8474, .F. ) ;
#19179=VECTOR ( 'NONE', #19406, 1000.000000000000000 ) ;
#19180=CARTESIAN_POINT ( 'NONE',  ( 10.00000000000000000, -60.65279801375385915, 63.75921967137595914 ) ) ;
#19182=CARTESIAN_POINT ( 'NONE',  ( 10.00000000000000000, 0.000000000000000000, 0.000000000000000000 ) ) ;
#19183=CARTESIAN_POINT ( 'NONE',  ( 10.00000000000000000, -2.481790431838652111, -92.46770094066596357 ) ) ;
#19184=CARTESIAN_POINT ( 'NONE',  ( 0.000000000000000000, -21.31452625070983231, 82.34610137166113475 ) ) ;
#19185=VECTOR ( 'NONE', #18386, 1000.000000000000000 ) ;
#19186=ORIENTED_EDGE ( 'NONE', *, *, #12168, .F. ) ;
#19187=DIRECTION ( 'NONE',  ( 0.000000000000000000, 0.9271838545667858700, 0.3746065934159160116 ) ) ;
#19188=EDGE_CURVE ( 'NONE', #10476, #5352, #7379, .T. ) ;
#19189=CARTESIAN_POINT ( 'NONE',  ( 0.000000000000000000, 79.66702613806774025, -29.80527447819464371 ) ) ;
#19191=CARTESIAN_POINT ( 'NONE',  ( 0.000000000000000000, -2.481790431839888011, 92.46770094066590673 ) ) ;
#19192=ORIENTED_EDGE ( 'NONE', *, *, #19442, .F. ) ;
#19193=AXIS2_PLACEMENT_3D ( 'NONE', #5680, #12629, #8981 ) ;
#19194=DIRECTION ( 'NONE',  ( -1.000000000000000000, -0.000000000000000000, -0.000000000000000000 ) ) ;
#19195=ORIENTED_EDGE ( 'NONE', *, *, #16380, .F. ) ;
#19197=ORIENTED_EDGE ( 'NONE', *, *, #1661, .T. ) ;
#19198=AXIS2_PLACEMENT_3D ( 'NONE', #4264, #9331, #946 ) ;
#19199=ORIENTED_EDGE ( 'NONE', *, *, #12557, .F. ) ;
#19200=EDGE_LOOP ( 'NONE', ( #10966, #17006, #20560, #11519 ) ) ;
#19201=DIRECTION ( 'NONE',  ( 1.000000000000000000, 0.000000000000000000, 0.000000000000000000 ) ) ;
#19203=ORIENTED_EDGE ( 'NONE', *, *, #15699, .F. ) ;
#19204=DIRECTION ( 'NONE',  ( -1.000000000000000000, 0.000000000000000000, 0.000000000000000000 ) ) ;
#19205=EDGE_CURVE ( 'NONE', #12050, #8996, #15841, .T. ) ;
#19207=DIRECTION ( 'NONE',  ( -1.000000000000000000, -0.000000000000000000, -0.000000000000000000 ) ) ;
#19209=CIRCLE ( 'NONE', #11099, 88.00000000000000000 ) ;
#19211=CARTESIAN_POINT ( 'NONE',  ( 0.000000000000000000, 83.89484365856945658, -26.56417150042864961 ) ) ;
#19212=AXIS2_PLACEMENT_3D ( 'NONE', #4306, #21002, #12483 ) ;
#19221=CARTESIAN_POINT ( 'NONE',  ( -10.00000000000000000, 0.000000000000000000, 0.000000000000000000 ) ) ;
#19224=ADVANCED_FACE ( 'NONE', ( #20185 ), #6497, .F. ) ;
#19226=ORIENTED_EDGE ( 'NONE', *, *, #10037, .F. ) ;
#19228=EDGE_LOOP ( 'NONE', ( #7929, #12314, #10126, #18988 ) ) ;
#19229=ORIENTED_EDGE ( 'NONE', *, *, #21090, .F. ) ;
#19231=VERTEX_POINT ( 'NONE', #2945 ) ;
#19233=CYLINDRICAL_SURFACE ( 'NONE', #7698, 92.50100000000000477 ) ;
#19235=CARTESIAN_POINT ( 'NONE',  ( 10.00000000000000000, 0.000000000000000000, 0.000000000000000000 ) ) ;
#19237=DIRECTION ( 'NONE',  ( 0.000000000000000000, 0.6427876096865403621, -0.7660444431189772363 ) ) ;
#19238=CARTESIAN_POINT ( 'NONE',  ( 10.00000000000000000, 46.93287725819779155, 70.94007663282461351 ) ) ;
#19239=DIRECTION ( 'NONE',  ( -1.000000000000000000, -0.000000000000000000, -0.000000000000000000 ) ) ;
#19242=DIRECTION ( 'NONE',  ( 1.000000000000000000, 0.000000000000000000, 0.000000000000000000 ) ) ;
#19243=DIRECTION ( 'NONE',  ( 0.000000000000000000, 1.603655480014115143E-14, -1.000000000000000000 ) ) ;
#19244=VECTOR ( 'NONE', #14542, 1000.000000000000000 ) ;
#19245=EDGE_LOOP ( 'NONE', ( #2846, #21669, #10524, #16078 ) ) ;
#19246=AXIS2_PLACEMENT_3D ( 'NONE', #3898, #5453, #8970 ) ;
#19247=CIRCLE ( 'NONE', #15343, 44.99999999999999289 ) ;
#19249=AXIS2_PLACEMENT_3D ( 'NONE', #887, #19450, #17798 ) ;
#19252=ORIENTED_EDGE ( 'NONE', *, *, #6863, .T. ) ;
#19253=DIRECTION ( 'NONE',  ( -1.000000000000000000, 0.000000000000000000, -0.000000000000000000 ) ) ;
#19254=VERTEX_POINT ( 'NONE', #15199 ) ;
#19255=DIRECTION ( 'NONE',  ( 1.000000000000000000, 0.000000000000000000, 0.000000000000000000 ) ) ;
#19261=CIRCLE ( 'NONE', #13247, 45.00000000000000000 ) ;
#19262=CARTESIAN_POINT ( 'NONE',  ( -10.00000000000000000, 0.000000000000000000, 0.000000000000000000 ) ) ;
#19264=CARTESIAN_POINT ( 'NONE',  ( 0.000000000000000000, 86.66425444033963288, -32.33793443156311298 ) ) ;
#19265=CARTESIAN_POINT ( 'NONE',  ( 5.000000000000000000, -41.89587599971600440, 77.38692120905457728 ) ) ;
#19266=LINE ( 'NONE', #6124, #12534 ) ;
#19267=CYLINDRICAL_SURFACE ( 'NONE', #14978, 45.00000000000000000 ) ;
#19270=DIRECTION ( 'NONE',  ( -1.000000000000000000, -0.000000000000000000, 0.000000000000000000 ) ) ;
#19271=ORIENTED_EDGE ( 'NONE', *, *, #4247, .T. ) ;
#19273=EDGE_CURVE ( 'NONE', #10208, #1972, #10191, .T. ) ;
#19278=VERTEX_POINT ( 'NONE', #11781 ) ;
#19282=EDGE_CURVE ( 'NONE', #1766, #155, #14984, .T. ) ;
#19283=( NAMED_UNIT ( * ) SI_UNIT ( $, .STERADIAN. ) SOLID_ANGLE_UNIT ( ) );
#19284=ORIENTED_EDGE ( 'NONE', *, *, #5385, .F. ) ;
#19287=DIRECTION ( 'NONE',  ( 1.000000000000000000, 0.000000000000000000, 0.000000000000000000 ) ) ;
#19288=CARTESIAN_POINT ( 'NONE',  ( 5.000000000000000000, 87.96697768756401103, 2.410567674970879981 ) ) ;
#19289=EDGE_LOOP ( 'NONE', ( #7764, #13461, #8471, #55 ) ) ;
#19291=CARTESIAN_POINT ( 'NONE',  ( 5.000000000000000000, 64.95266917914399585, -59.37298010462904330 ) ) ;
#19293=AXIS2_PLACEMENT_3D ( 'NONE', #13348, #8387, #21638 ) ;
#19295=CARTESIAN_POINT ( 'NONE',  ( 0.000000000000000000, 0.000000000000000000, 0.000000000000000000 ) ) ;
#19296=CIRCLE ( 'NONE', #1307, 92.50100000000000477 ) ;
#19297=CARTESIAN_POINT ( 'NONE',  ( 10.00000000000000000, 0.000000000000000000, 0.000000000000000000 ) ) ;
#19298=ORIENTED_EDGE ( 'NONE', *, *, #2736, .T. ) ;
#19299=DIRECTION ( 'NONE',  ( -1.000000000000000000, -0.000000000000000000, -0.000000000000000000 ) ) ;
#19301=ADVANCED_FACE ( 'NONE', ( #16865 ), #13546, .F. ) ;
#19302=EDGE_CURVE ( 'NONE', #8524, #20998, #6330, .T. ) ;
#19306=ORIENTED_EDGE ( 'NONE', *, *, #12692, .T. ) ;
#19308=CIRCLE ( 'NONE', #5908, 88.00000000000000000 ) ;
#19309=ORIENTED_EDGE ( 'NONE', *, *, #14471, .T. ) ;
#19311=EDGE_LOOP ( 'NONE', ( #13773, #7386, #12561, #14632 ) ) ;
#19312=CARTESIAN_POINT ( 'NONE',  ( 10.00000000000000000, 0.000000000000000000, 0.000000000000000000 ) ) ;
#19313=VERTEX_POINT ( 'NONE', #8150 ) ;
#19316=CARTESIAN_POINT ( 'NONE',  ( 10.00000000000000000, 0.000000000000000000, 0.000000000000000000 ) ) ;
#19318=CARTESIAN_POINT ( 'NONE',  ( 10.00000000000000000, 87.96697768756401103, 2.410567674970879981 ) ) ;
#19319=EDGE_CURVE ( 'NONE', #9608, #16623, #14790, .T. ) ;
#19320=AXIS2_PLACEMENT_3D ( 'NONE', #4367, #21270, #7797 ) ;
#19321=CARTESIAN_POINT ( 'NONE',  ( 10.00000000000000000, -57.53593069156421791, 72.42963261300944566 ) ) ;
#19322=CIRCLE ( 'NONE', #15787, 45.00000000000000000 ) ;
#19327=CARTESIAN_POINT ( 'NONE',  ( 10.00000000000000000, -83.48638250753248258, 27.82128566055087049 ) ) ;
#19328=ADVANCED_FACE ( 'NONE', ( #3598 ), #2058, .F. ) ;
#19329=ADVANCED_FACE ( 'NONE', ( #185 ), #15417, .F. ) ;
#19332=EDGE_CURVE ( 'NONE', #16339, #20116, #8573, .T. ) ;
#19334=ORIENTED_EDGE ( 'NONE', *, *, #7854, .T. ) ;
#19335=VECTOR ( 'NONE', #2494, 1000.000000000000000 ) ;
#19337=AXIS2_PLACEMENT_3D ( 'NONE', #5008, #1471, #20044 ) ;
#19338=AXIS2_PLACEMENT_3D ( 'NONE', #20578, #15598, #12066 ) ;
#19339=ORIENTED_EDGE ( 'NONE', *, *, #18912, .F. ) ;
#19340=EDGE_CURVE ( 'NONE', #17373, #11314, #17082, .T. ) ;
#19341=DIRECTION ( 'NONE',  ( 0.000000000000000000, 0.000000000000000000, 1.000000000000000000 ) ) ;
#19342=ORIENTED_EDGE ( 'NONE', *, *, #15358, .F. ) ;
#19344=CYLINDRICAL_SURFACE ( 'NONE', #13262, 92.50100000000000477 ) ;
#19345=CARTESIAN_POINT ( 'NONE',  ( 10.00000000000000000, 83.35585896458643163, -16.94078559807864792 ) ) ;
#19346=CARTESIAN_POINT ( 'NONE',  ( 10.00000000000000000, 84.12297548659721258, -12.59025161327029529 ) ) ;
#19347=CARTESIAN_POINT ( 'NONE',  ( 0.000000000000000000, 0.000000000000000000, 0.000000000000000000 ) ) ;
#19354=CIRCLE ( 'NONE', #312, 92.50100000000000477 ) ;
#19355=CIRCLE ( 'NONE', #3476, 44.99999999999998579 ) ;
#19356=ORIENTED_EDGE ( 'NONE', *, *, #2255, .F. ) ;
#19357=CIRCLE ( 'NONE', #5978, 45.00000000000000711 ) ;
#19358=DIRECTION ( 'NONE',  ( 1.000000000000000000, 0.000000000000000000, 0.000000000000000000 ) ) ;
#19360=DIRECTION ( 'NONE',  ( 1.000000000000000000, 0.000000000000000000, 0.000000000000000000 ) ) ;
#19361=DIRECTION ( 'NONE',  ( 0.000000000000000000, 0.9271838545667884235, -0.3746065934159096278 ) ) ;
#19365=EDGE_LOOP ( 'NONE', ( #11332, #13552, #4098, #21110 ) ) ;
#19371=VERTEX_POINT ( 'NONE', #5482 ) ;
#19375=CARTESIAN_POINT ( 'NONE',  ( 10.00000000000000000, -61.71252885873428085, 58.53847642588571887 ) ) ;
#19376=CARTESIAN_POINT ( 'NONE',  ( 10.00000000000000000, -0.6609040254605957898, -87.99751818016876825 ) ) ;
#19378=DIRECTION ( 'NONE',  ( -1.000000000000000000, 0.000000000000000000, -0.000000000000000000 ) ) ;
#19379=DIRECTION ( 'NONE',  ( 0.000000000000000000, 0.06975647374412555224, -0.9975640502598241977 ) ) ;
#19380=ADVANCED_FACE ( 'NONE', ( #612 ), #8687, .F. ) ;
#19382=LINE ( 'NONE', #9413, #16419 ) ;
#19384=ORIENTED_EDGE ( 'NONE', *, *, #14082, .F. ) ;
#19385=DIRECTION ( 'NONE',  ( -1.000000000000000000, 0.000000000000000000, -0.000000000000000000 ) ) ;
#19387=ORIENTED_EDGE ( 'NONE', *, *, #3673, .F. ) ;
#19388=CIRCLE ( 'NONE', #348, 44.99999999999998579 ) ;
#19389=VECTOR ( 'NONE', #13346, 1000.000000000000000 ) ;
#19391=EDGE_LOOP ( 'NONE', ( #17257, #19119, #14818, #13606 ) ) ;
#19393=CARTESIAN_POINT ( 'NONE',  ( 0.000000000000000000, -23.62010150527279961, 84.77081340225898032 ) ) ;
#19394=ORIENTED_EDGE ( 'NONE', *, *, #7196, .T. ) ;
#19395=ORIENTED_EDGE ( 'NONE', *, *, #581, .F. ) ;
#19396=EDGE_LOOP ( 'NONE', ( #19199, #6150, #20328, #2113 ) ) ;
#19397=ORIENTED_EDGE ( 'NONE', *, *, #1230, .T. ) ;
#19398=LINE ( 'NONE', #12426, #8943 ) ;
#19401=CARTESIAN_POINT ( 'NONE',  ( 5.000000000000002665, 86.77540292929722909, -14.62974526292624944 ) ) ;
#19402=CARTESIAN_POINT ( 'NONE',  ( 10.00000000000000000, -9.646732466565913100, 84.51112348751846071 ) ) ;
#19404=CIRCLE ( 'NONE', #15521, 44.99999999999999289 ) ;
#19405=AXIS2_PLACEMENT_3D ( 'NONE', #16303, #1172, #13097 ) ;
#19406=DIRECTION ( 'NONE',  ( -1.000000000000000000, 0.000000000000000000, 0.000000000000000000 ) ) ;
#19407=CARTESIAN_POINT ( 'NONE',  ( 0.000000000000000000, 52.96496548042942010, -66.55750800669305534 ) ) ;
#19410=CARTESIAN_POINT ( 'NONE',  ( 10.00000000000000000, -91.49386717542212466, -13.61276130277086693 ) ) ;
#19411=CARTESIAN_POINT ( 'NONE',  ( 10.00000000000000000, 0.000000000000000000, 0.000000000000000000 ) ) ;
#19414=ORIENTED_EDGE ( 'NONE', *, *, #17543, .T. ) ;
#19415=CYLINDRICAL_SURFACE ( 'NONE', #9128, 92.50100000000000477 ) ;
#19416=VERTEX_POINT ( 'NONE', #8995 ) ;
#19420=ORIENTED_EDGE ( 'NONE', *, *, #14846, .F. ) ;
#19421=CARTESIAN_POINT ( 'NONE',  ( 10.00000000000000000, -82.02147376274642454, -42.76579056660944644 ) ) ;
#19422=DIRECTION ( 'NONE',  ( -1.000000000000000000, 0.000000000000000000, -0.000000000000000000 ) ) ;
#19423=CARTESIAN_POINT ( 'NONE',  ( 0.000000000000000000, 36.60317927562682883, -76.78148674856727496 ) ) ;
#19424=EDGE_CURVE ( 'NONE', #9177, #535, #15857, .T. ) ;
#19425=DIRECTION ( 'NONE',  ( 1.000000000000000000, 0.000000000000000000, 0.000000000000000000 ) ) ;
#19427=LINE ( 'NONE', #4290, #3772 ) ;
#19428=CARTESIAN_POINT ( 'NONE',  ( 0.000000000000000000, 0.000000000000000000, 0.000000000000000000 ) ) ;
#19432=CARTESIAN_POINT ( 'NONE',  ( 10.00000000000000000, -61.33825423015638734, -69.23910433416007493 ) ) ;
#19433=DIRECTION ( 'NONE',  ( 0.000000000000000000, 0.000000000000000000, 1.000000000000000000 ) ) ;
#19436=ORIENTED_EDGE ( 'NONE', *, *, #11228, .T. ) ;
#19437=VERTEX_POINT ( 'NONE', #12324 ) ;
#19441=DIRECTION ( 'NONE',  ( -1.000000000000000000, 0.000000000000000000, -0.000000000000000000 ) ) ;
#19442=EDGE_CURVE ( 'NONE', #1794, #5152, #17308, .T. ) ;
#19444=FACE_OUTER_BOUND ( 'NONE', #13155, .T. ) ;
#19445=EDGE_CURVE ( 'NONE', #21566, #589, #18693, .T. ) ;
#19447=FACE_OUTER_BOUND ( 'NONE', #8915, .T. ) ;
#19450=DIRECTION ( 'NONE',  ( -1.000000000000000000, 0.000000000000000000, 0.000000000000000000 ) ) ;
#19451=CARTESIAN_POINT ( 'NONE',  ( 10.00000000000000000, 56.35896156215049047, -73.34918167666251065 ) ) ;
#19453=DIRECTION ( 'NONE',  ( 1.000000000000000000, 0.000000000000000000, 0.000000000000000000 ) ) ;
#19454=CARTESIAN_POINT ( 'NONE',  ( 10.00000000000000000, 0.000000000000000000, 0.000000000000000000 ) ) ;
#19456=VECTOR ( 'NONE', #13758, 1000.000000000000000 ) ;
#19457=ORIENTED_EDGE ( 'NONE', *, *, #7824, .F. ) ;
#19459=EDGE_CURVE ( 'NONE', #2267, #17431, #347, .T. ) ;
#19460=ORIENTED_EDGE ( 'NONE', *, *, #15492, .T. ) ;
#19462=ADVANCED_FACE ( 'NONE', ( #5805 ), #16067, .F. ) ;
#19464=ORIENTED_EDGE ( 'NONE', *, *, #12443, .F. ) ;
#19466=VERTEX_POINT ( 'NONE', #19393 ) ;
#19467=ORIENTED_EDGE ( 'NONE', *, *, #9462, .F. ) ;
#19469=CARTESIAN_POINT ( 'NONE',  ( 0.000000000000000000, 0.000000000000000000, 0.000000000000000000 ) ) ;
#19471=ORIENTED_EDGE ( 'NONE', *, *, #21065, .T. ) ;
#19473=DIRECTION ( 'NONE',  ( -1.000000000000000000, -0.000000000000000000, 0.000000000000000000 ) ) ;
#19474=DIRECTION ( 'NONE',  ( 0.000000000000000000, 0.000000000000000000, 1.000000000000000000 ) ) ;
#19477=CARTESIAN_POINT ( 'NONE',  ( 5.000000000000000000, 41.89587599971653731, -77.38692120905427885 ) ) ;
#19478=DIRECTION ( 'NONE',  ( -1.000000000000000000, 0.000000000000000000, 0.000000000000000000 ) ) ;
#19479=CARTESIAN_POINT ( 'NONE',  ( 10.00000000000000000, 71.72924546249947753, 45.71766382684695884 ) ) ;
#19480=CARTESIAN_POINT ( 'NONE',  ( 10.00000000000000000, 75.45728100697654384, -39.26051685138985903 ) ) ;
#19481=LINE ( 'NONE', #16055, #16886 ) ;
#19482=DIRECTION ( 'NONE',  ( 0.000000000000000000, 0.000000000000000000, 1.000000000000000000 ) ) ;
#19483=AXIS2_PLACEMENT_3D ( 'NONE', #20707, #16014, #21434 ) ;
#19484=VERTEX_POINT ( 'NONE', #19493 ) ;
#19485=CARTESIAN_POINT ( 'NONE',  ( 10.00000000000000000, 48.19312842678472464, 70.09002648625214249 ) ) ;
#19486=EDGE_CURVE ( 'NONE', #5395, #15764, #14084, .T. ) ;
#19487=ORIENTED_EDGE ( 'NONE', *, *, #8082, .F. ) ;
#19488=EDGE_CURVE ( 'NONE', #1594, #8339, #4564, .T. ) ;
#19489=CARTESIAN_POINT ( 'NONE',  ( 10.00000000000000000, -2.208823992043557283, -85.03123271466938604 ) ) ;
#19490=FACE_OUTER_BOUND ( 'NONE', #9788, .T. ) ;
#19491=AXIS2_PLACEMENT_3D ( 'NONE', #10396, #7318, #12484 ) ;
#19492=EDGE_CURVE ( 'NONE', #4876, #2112, #1154, .T. ) ;
#19493=CARTESIAN_POINT ( 'NONE',  ( 10.00000000000000000, -51.18896083639317851, 71.57995730992162464 ) ) ;
#19494=ORIENTED_EDGE ( 'NONE', *, *, #5031, .T. ) ;
#19498=ORIENTED_EDGE ( 'NONE', *, *, #6496, .T. ) ;
#19499=ORIENTED_EDGE ( 'NONE', *, *, #7365, .T. ) ;
#19500=DIRECTION ( 'NONE',  ( 0.000000000000000000, -0.4694715627858798146, -0.8829475928589327616 ) ) ;
#19508=LINE ( 'NONE', #7911, #10892 ) ;
#19510=ORIENTED_EDGE ( 'NONE', *, *, #18884, .T. ) ;
#19513=FACE_OUTER_BOUND ( 'NONE', #18913, .T. ) ;
#19514=AXIS2_PLACEMENT_3D ( 'NONE', #7012, #10742, #20703 ) ;
#19515=CARTESIAN_POINT ( 'NONE',  ( 0.000000000000000000, 0.000000000000000000, 0.000000000000000000 ) ) ;
#19516=VERTEX_POINT ( 'NONE', #21264 ) ;
#19519=CARTESIAN_POINT ( 'NONE',  ( 5.000000000000002665, -12.90135963484139658, 87.04915231966639055 ) ) ;
#19521=DIRECTION ( 'NONE',  ( -1.000000000000000000, 0.000000000000000000, -0.000000000000000000 ) ) ;
#19522=AXIS2_PLACEMENT_3D ( 'NONE', #21416, #11022, #2520 ) ;
#19524=ORIENTED_EDGE ( 'NONE', *, *, #372, .F. ) ;
#19525=CARTESIAN_POINT ( 'NONE',  ( 10.00000000000000000, -16.79755869217711250, 90.96305306542248559 ) ) ;
#19527=CYLINDRICAL_SURFACE ( 'NONE', #3488, 45.00000000000000000 ) ;
#19531=LINE ( 'NONE', #17893, #1877 ) ;
#19533=AXIS2_PLACEMENT_3D ( 'NONE', #5111, #13725, #20365 ) ;
#19534=DIRECTION ( 'NONE',  ( 0.000000000000000000, 0.000000000000000000, -1.000000000000000000 ) ) ;
#19535=DIRECTION ( 'NONE',  ( 1.000000000000000000, 0.000000000000000000, 0.000000000000000000 ) ) ;
#19537=CARTESIAN_POINT ( 'NONE',  ( 0.000000000000000000, 0.000000000000000000, 0.000000000000000000 ) ) ;
#19538=CIRCLE ( 'NONE', #7906, 45.00000000000000711 ) ;
#19541=EDGE_LOOP ( 'NONE', ( #19069, #1790, #5427, #12700 ) ) ;
#19547=ADVANCED_FACE ( 'NONE', ( #17847 ), #4255, .F. ) ;
#19548=ORIENTED_EDGE ( 'NONE', *, *, #1112, .F. ) ;
#19549=FACE_OUTER_BOUND ( 'NONE', #15885, .T. ) ;
#19550=VECTOR ( 'NONE', #15735, 1000.000000000000000 ) ;
#19551=ORIENTED_EDGE ( 'NONE', *, *, #9486, .T. ) ;
#19552=LINE ( 'NONE', #12304, #20550 ) ;
#19554=CARTESIAN_POINT ( 'NONE',  ( 10.00000000000000000, 0.000000000000000000, 0.000000000000000000 ) ) ;
#19557=LINE ( 'NONE', #9499, #1364 ) ;
#19560=FACE_OUTER_BOUND ( 'NONE', #19311, .T. ) ;
#19561=DIRECTION ( 'NONE',  ( -1.000000000000000000, 0.000000000000000000, -0.000000000000000000 ) ) ;
#19562=CARTESIAN_POINT ( 'NONE',  ( 10.00000000000000000, 0.000000000000000000, 0.000000000000000000 ) ) ;
#19563=ORIENTED_EDGE ( 'NONE', *, *, #18790, .T. ) ;
#19564=CARTESIAN_POINT ( 'NONE',  ( 0.000000000000000000, 51.18896083639367589, -71.57995730992126937 ) ) ;
#19569=EDGE_CURVE ( 'NONE', #2662, #733, #10910, .T. ) ;
#19570=VERTEX_POINT ( 'NONE', #21164 ) ;
#19571=CIRCLE ( 'NONE', #6584, 88.00000000000000000 ) ;
#19574=AXIS2_PLACEMENT_3D ( 'NONE', #13731, #3668, #20478 ) ;
#19575=ADVANCED_FACE ( 'NONE', ( #6034 ), #7790, .F. ) ;
#19576=DIRECTION ( 'NONE',  ( 0.000000000000000000, 0.000000000000000000, 1.000000000000000000 ) ) ;
#19577=ORIENTED_EDGE ( 'NONE', *, *, #18562, .F. ) ;
#19578=CARTESIAN_POINT ( 'NONE',  ( 0.000000000000000000, 29.47587714451147534, -82.91666097089093057 ) ) ;
#19580=ORIENTED_EDGE ( 'NONE', *, *, #6381, .F. ) ;
#19581=CIRCLE ( 'NONE', #3348, 44.99999999999998579 ) ;
#19586=DIRECTION ( 'NONE',  ( 0.000000000000000000, 0.8290375725550390706, 0.5591929034707506796 ) ) ;
#19587=DIRECTION ( 'NONE',  ( 0.000000000000000000, 0.000000000000000000, 1.000000000000000000 ) ) ;
#19588=EDGE_CURVE ( 'NONE', #4269, #15626, #13739, .T. ) ;
#19589=DIRECTION ( 'NONE',  ( 0.000000000000000000, 0.000000000000000000, 1.000000000000000000 ) ) ;
#19591=AXIS2_PLACEMENT_3D ( 'NONE', #10869, #7783, #17624 ) ;
#19594=VECTOR ( 'NONE', #9973, 1000.000000000000000 ) ;
#19595=FACE_OUTER_BOUND ( 'NONE', #3119, .T. ) ;
#19596=AXIS2_PLACEMENT_3D ( 'NONE', #8135, #3155, #11665 ) ;
#19597=DIRECTION ( 'NONE',  ( 0.000000000000000000, 2.127927463864883580E-14, -1.000000000000000000 ) ) ;
#19598=EDGE_CURVE ( 'NONE', #3682, #12932, #8450, .T. ) ;
#19599=CARTESIAN_POINT ( 'NONE',  ( 10.00000000000000000, -92.22057093985034726, 7.197311757040196767 ) ) ;
#19600=CYLINDRICAL_SURFACE ( 'NONE', #15076, 88.00000000000000000 ) ;
#19601=AXIS2_PLACEMENT_3D ( 'NONE', #21680, #3337, #11846 ) ;
#19603=DIRECTION ( 'NONE',  ( -1.000000000000000000, 0.000000000000000000, 0.000000000000000000 ) ) ;
#19605=EDGE_CURVE ( 'NONE', #21544, #12774, #12969, .T. ) ;
#19606=DIRECTION ( 'NONE',  ( 0.000000000000000000, -1.954455116267202870E-14, -1.000000000000000000 ) ) ;
#19607=EDGE_CURVE ( 'NONE', #9814, #14447, #18347, .T. ) ;
#19609=DIRECTION ( 'NONE',  ( 0.000000000000000000, 0.000000000000000000, 1.000000000000000000 ) ) ;
#19610=ORIENTED_EDGE ( 'NONE', *, *, #128, .F. ) ;
#19611=CIRCLE ( 'NONE', #10077, 88.00000000000000000 ) ;
#19612=VECTOR ( 'NONE', #12928, 1000.000000000000000 ) ;
#19613=VERTEX_POINT ( 'NONE', #4584 ) ;
#19614=VERTEX_POINT ( 'NONE', #1476 ) ;
#19616=DIRECTION ( 'NONE',  ( 0.000000000000000000, 0.9848077530122074652, 0.1736481776669340227 ) ) ;
#19622=DIRECTION ( 'NONE',  ( -1.000000000000000000, -0.000000000000000000, 0.000000000000000000 ) ) ;
#19626=AXIS2_PLACEMENT_3D ( 'NONE', #11620, #18367, #10172 ) ;
#19629=CIRCLE ( 'NONE', #12569, 88.00000000000000000 ) ;
#19631=DIRECTION ( 'NONE',  ( -1.000000000000000000, -0.000000000000000000, -0.000000000000000000 ) ) ;
#19634=ORIENTED_EDGE ( 'NONE', *, *, #5671, .T. ) ;
#19639=CARTESIAN_POINT ( 'NONE',  ( 0.000000000000000000, 0.000000000000000000, 0.000000000000000000 ) ) ;
#19644=EDGE_LOOP ( 'NONE', ( #12672, #6933, #4263, #14517 ) ) ;
#19647=VERTEX_POINT ( 'NONE', #6255 ) ;
#19651=FACE_OUTER_BOUND ( 'NONE', #17385, .T. ) ;
#19653=DIRECTION ( 'NONE',  ( 1.000000000000000000, 0.000000000000000000, 0.000000000000000000 ) ) ;
#19654=ADVANCED_FACE ( 'NONE', ( #3141 ), #3033, .F. ) ;
#19655=DIRECTION ( 'NONE',  ( 0.000000000000000000, 0.000000000000000000, 1.000000000000000000 ) ) ;
#19656=FACE_OUTER_BOUND ( 'NONE', #8065, .T. ) ;
#19657=AXIS2_PLACEMENT_3D ( 'NONE', #8732, #15349, #18898 ) ;
#19658=AXIS2_PLACEMENT_3D ( 'NONE', #21832, #2942, #13206 ) ;
#19662=VERTEX_POINT ( 'NONE', #5013 ) ;
#19663=VERTEX_POINT ( 'NONE', #20157 ) ;
#19664=VERTEX_POINT ( 'NONE', #16719 ) ;
#19665=DIRECTION ( 'NONE',  ( 0.000000000000000000, 0.000000000000000000, 1.000000000000000000 ) ) ;
#19666=AXIS2_PLACEMENT_3D ( 'NONE', #1429, #11473, #11148 ) ;
#19667=ORIENTED_EDGE ( 'NONE', *, *, #8507, .T. ) ;
#19668=LINE ( 'NONE', #7632, #17374 ) ;
#19670=DIRECTION ( 'NONE',  ( -1.000000000000000000, 0.000000000000000000, -0.000000000000000000 ) ) ;
#19673=EDGE_CURVE ( 'NONE', #8121, #6764, #1271, .T. ) ;
#19675=CARTESIAN_POINT ( 'NONE',  ( 5.000000000000002665, -35.18804927320584142, 80.65854690202667143 ) ) ;
#19676=FACE_OUTER_BOUND ( 'NONE', #13157, .T. ) ;
#19677=VERTEX_POINT ( 'NONE', #18398 ) ;
#19680=AXIS2_PLACEMENT_3D ( 'NONE', #457, #10719, #5433 ) ;
#19681=AXIS2_PLACEMENT_3D ( 'NONE', #15544, #14104, #17094 ) ;
#19682=ORIENTED_EDGE ( 'NONE', *, *, #13738, .T. ) ;
#19683=CIRCLE ( 'NONE', #3463, 92.50100000000000477 ) ;
#19684=DIRECTION ( 'NONE',  ( 1.000000000000000000, -0.000000000000000000, -0.000000000000000000 ) ) ;
#19685=CARTESIAN_POINT ( 'NONE',  ( -10.00000000000000000, 0.000000000000000000, 0.000000000000000000 ) ) ;
#19686=VERTEX_POINT ( 'NONE', #9758 ) ;
#19687=CARTESIAN_POINT ( 'NONE',  ( 10.00000000000000000, -32.56745702629792305, 78.57830605990643846 ) ) ;
#19693=CYLINDRICAL_SURFACE ( 'NONE', #5079, 45.00000000000000000 ) ;
#19695=ORIENTED_EDGE ( 'NONE', *, *, #21745, .T. ) ;
#19696=CARTESIAN_POINT ( 'NONE',  ( 10.00000000000000000, 52.25832601289098278, 70.80301803122803506 ) ) ;
#19697=CARTESIAN_POINT ( 'NONE',  ( 0.000000000000000000, 0.000000000000000000, 0.000000000000000000 ) ) ;
#19702=CIRCLE ( 'NONE', #3838, 92.50100000000000477 ) ;
#19703=DIRECTION ( 'NONE',  ( 1.000000000000000000, 0.000000000000000000, 0.000000000000000000 ) ) ;
#19708=CYLINDRICAL_SURFACE ( 'NONE', #11485, 44.99999999999998579 ) ;
#19709=CARTESIAN_POINT ( 'NONE',  ( 0.000000000000000000, -86.54587337002867287, -15.93147207947093946 ) ) ;
#19710=VERTEX_POINT ( 'NONE', #21587 ) ;
#19711=VERTEX_POINT ( 'NONE', #10088 ) ;
#19713=EDGE_CURVE ( 'NONE', #6864, #7736, #20665, .T. ) ;
#19716=AXIS2_PLACEMENT_3D ( 'NONE', #19848, #4713, #6609 ) ;
#19719=CIRCLE ( 'NONE', #13357, 44.99999999999999289 ) ;
#19721=ORIENTED_EDGE ( 'NONE', *, *, #8132, .T. ) ;
#19723=EDGE_LOOP ( 'NONE', ( #15242, #11340, #9436, #17008 ) ) ;
#19725=CYLINDRICAL_SURFACE ( 'NONE', #13951, 88.00000000000000000 ) ;
#19726=EDGE_LOOP ( 'NONE', ( #2352, #18909, #67, #4420 ) ) ;
#19728=FACE_OUTER_BOUND ( 'NONE', #1977, .T. ) ;
#19730=EDGE_CURVE ( 'NONE', #8068, #286, #6581, .T. ) ;
#19731=CYLINDRICAL_SURFACE ( 'NONE', #17140, 88.00000000000000000 ) ;
#19732=EDGE_CURVE ( 'NONE', #5370, #13890, #11487, .T. ) ;
#19733=DIRECTION ( 'NONE',  ( 1.000000000000000000, 0.000000000000000000, 0.000000000000000000 ) ) ;
#19736=EDGE_CURVE ( 'NONE', #12830, #18956, #6196, .T. ) ;
#19739=ORIENTED_EDGE ( 'NONE', *, *, #6813, .T. ) ;
#19740=AXIS2_PLACEMENT_3D ( 'NONE', #5389, #6627, #3516 ) ;
#19742=ADVANCED_FACE ( 'NONE', ( #19042 ), #20586, .F. ) ;
#19743=DIRECTION ( 'NONE',  ( 0.000000000000000000, -0.8987940462991710344, 0.4383711467890689106 ) ) ;
#19746=EDGE_CURVE ( 'NONE', #8452, #11211, #477, .T. ) ;
#19748=CARTESIAN_POINT ( 'NONE',  ( 0.000000000000000000, 0.000000000000000000, 0.000000000000000000 ) ) ;
#19750=ORIENTED_EDGE ( 'NONE', *, *, #10648, .F. ) ;
#19751=CARTESIAN_POINT ( 'NONE',  ( 10.00000000000000000, -75.87763420127802760, -44.57111876559801544 ) ) ;
#19754=VERTEX_POINT ( 'NONE', #8865 ) ;
#19755=ORIENTED_EDGE ( 'NONE', *, *, #16912, .T. ) ;
#19756=DIRECTION ( 'NONE',  ( -1.000000000000000000, 0.000000000000000000, -0.000000000000000000 ) ) ;
#19757=CIRCLE ( 'NONE', #10928, 44.99999999999999289 ) ;
#19759=ORIENTED_EDGE ( 'NONE', *, *, #1379, .F. ) ;
#19760=DIRECTION ( 'NONE',  ( 0.000000000000000000, -9.251858538542973800E-16, -1.000000000000000000 ) ) ;
#19761=CARTESIAN_POINT ( 'NONE',  ( 10.00000000000000000, 91.70173545986537533, -12.13370160539944287 ) ) ;
#19764=ADVANCED_FACE ( 'NONE', ( #10523 ), #2026, .F. ) ;
#19766=DIRECTION ( 'NONE',  ( 0.000000000000000000, 0.000000000000000000, 1.000000000000000000 ) ) ;
#19767=DIRECTION ( 'NONE',  ( 0.000000000000000000, 0.2756373558169997184, -0.9612616959383185611 ) ) ;
#19768=CARTESIAN_POINT ( 'NONE',  ( 10.00000000000000000, -21.31452625070873452, -82.34610137166143318 ) ) ;
#19769=CYLINDRICAL_SURFACE ( 'NONE', #8642, 44.99999999999999289 ) ;
#19770=AXIS2_PLACEMENT_3D ( 'NONE', #19685, #17602, #11064 ) ;
#19771=FACE_OUTER_BOUND ( 'NONE', #300, .T. ) ;
#19773=VERTEX_POINT ( 'NONE', #20378 ) ;
#19774=EDGE_CURVE ( 'NONE', #7680, #3874, #15017, .T. ) ;
#19775=EDGE_LOOP ( 'NONE', ( #19158, #3333, #9910, #13179 ) ) ;
#19776=ORIENTED_EDGE ( 'NONE', *, *, #5550, .F. ) ;
#19777=ADVANCED_FACE ( 'NONE', ( #6792 ), #10303, .F. ) ;
#19778=EDGE_CURVE ( 'NONE', #5510, #5864, #16422, .T. ) ;
#19780=FACE_OUTER_BOUND ( 'NONE', #20562, .T. ) ;
#19782=CARTESIAN_POINT ( 'NONE',  ( -10.00000000000000000, 0.000000000000000000, 0.000000000000000000 ) ) ;
#19783=AXIS2_PLACEMENT_3D ( 'NONE', #8624, #7192, #20670 ) ;
#19787=CARTESIAN_POINT ( 'NONE',  ( 10.00000000000000000, -17.64925110578410639, -86.21197095186363413 ) ) ;
#19788=LINE ( 'NONE', #13145, #6612 ) ;
#19789=CARTESIAN_POINT ( 'NONE',  ( 10.00000000000000000, 0.000000000000000000, 0.000000000000000000 ) ) ;
#19793=( GEOMETRIC_REPRESENTATION_CONTEXT ( 3 ) GLOBAL_UNCERTAINTY_ASSIGNED_CONTEXT ( ( #4601 ) ) GLOBAL_UNIT_ASSIGNED_CONTEXT ( ( #13982, #18964, #14302 ) ) REPRESENTATION_CONTEXT ( 'NONE', 'WORKASPACE' ) );
#19794=ORIENTED_EDGE ( 'NONE', *, *, #1221, .F. ) ;
#19796=CARTESIAN_POINT ( 'NONE',  ( 0.000000000000000000, -56.05743251323810483, -67.83483072893858434 ) ) ;
#19797=DIRECTION ( 'NONE',  ( 0.000000000000000000, -0.9702957262759988044, 0.2419218955996582376 ) ) ;
#19800=EDGE_LOOP ( 'NONE', ( #4710, #8549, #5320, #2643 ) ) ;
#19801=EDGE_LOOP ( 'NONE', ( #2641, #20827, #18299, #20214 ) ) ;
#19802=VECTOR ( 'NONE', #19561, 1000.000000000000000 ) ;
#19804=CARTESIAN_POINT ( 'NONE',  ( 10.00000000000000000, 0.000000000000000000, 0.000000000000000000 ) ) ;
#19805=ORIENTED_EDGE ( 'NONE', *, *, #12048, .F. ) ;
#19807=DIRECTION ( 'NONE',  ( 0.000000000000000000, 0.000000000000000000, 1.000000000000000000 ) ) ;
#19809=LINE ( 'NONE', #13065, #11057 ) ;
#19811=CARTESIAN_POINT ( 'NONE',  ( 10.00000000000000000, -70.37753541435900217, -60.02863908169706519 ) ) ;
#19812=DIRECTION ( 'NONE',  ( -1.000000000000000000, 0.000000000000000000, 0.000000000000000000 ) ) ;
#19813=DIRECTION ( 'NONE',  ( 1.000000000000000000, 0.000000000000000000, 0.000000000000000000 ) ) ;
#19814=CARTESIAN_POINT ( 'NONE',  ( 10.00000000000000000, -66.01871308925419157, -64.79170103523090063 ) ) ;
#19816=ORIENTED_EDGE ( 'NONE', *, *, #10099, .T. ) ;
#19817=DIRECTION ( 'NONE',  ( -1.000000000000000000, 0.000000000000000000, 0.000000000000000000 ) ) ;
#19818=EDGE_CURVE ( 'NONE', #971, #1435, #8663, .T. ) ;
#19819=CIRCLE ( 'NONE', #18774, 44.99999999999998579 ) ;
#19822=ORIENTED_EDGE ( 'NONE', *, *, #6494, .T. ) ;
#19823=ORIENTED_EDGE ( 'NONE', *, *, #2884, .F. ) ;
#19824=ORIENTED_EDGE ( 'NONE', *, *, #4594, .T. ) ;
#19826=DIRECTION ( 'NONE',  ( 0.000000000000000000, 0.000000000000000000, -1.000000000000000000 ) ) ;
#19827=EDGE_CURVE ( 'NONE', #12369, #9115, #3729, .T. ) ;
#19829=CYLINDRICAL_SURFACE ( 'NONE', #2254, 44.99999999999999289 ) ;
#19832=CARTESIAN_POINT ( 'NONE',  ( 10.00000000000000000, 75.45728100697654384, -39.26051685138985903 ) ) ;
#19833=CYLINDRICAL_SURFACE ( 'NONE', #21644, 92.50100000000000477 ) ;
#19834=CYLINDRICAL_SURFACE ( 'NONE', #16617, 92.50100000000000477 ) ;
#19836=ORIENTED_EDGE ( 'NONE', *, *, #2283, .T. ) ;
#19838=CIRCLE ( 'NONE', #21607, 45.00000000000000000 ) ;
#19839=CARTESIAN_POINT ( 'NONE',  ( 0.000000000000000000, -21.31452625070873452, -82.34610137166143318 ) ) ;
#19844=DIRECTION ( 'NONE',  ( 0.000000000000000000, -0.6427876096865300370, -0.7660444431189857850 ) ) ;
#19845=EDGE_CURVE ( 'NONE', #7162, #15664, #5138, .T. ) ;
#19847=EDGE_CURVE ( 'NONE', #10308, #13383, #15504, .T. ) ;
#19848=CARTESIAN_POINT ( 'NONE',  ( -10.00000000000000000, 0.000000000000000000, 0.000000000000000000 ) ) ;
#19851=CARTESIAN_POINT ( 'NONE',  ( 10.00000000000000000, -84.19736439813830486, 38.30455363800902546 ) ) ;
#19856=ORIENTED_EDGE ( 'NONE', *, *, #15551, .T. ) ;
#19857=CARTESIAN_POINT ( 'NONE',  ( -10.00000000000000000, 0.000000000000000000, 0.000000000000000000 ) ) ;
#19859=CARTESIAN_POINT ( 'NONE',  ( 10.00000000000000000, -92.49798535263880694, 0.7467976319017460840 ) ) ;
#19861=FILL_AREA_STYLE ('',( #4844 ) ) ;
#19862=ADVANCED_FACE ( 'NONE', ( #20485 ), #5128, .F. ) ;
#19863=CIRCLE ( 'NONE', #5041, 88.00000000000000000 ) ;
#19864=DIRECTION ( 'NONE',  ( 1.000000000000000000, 0.000000000000000000, 0.000000000000000000 ) ) ;
#19865=DIRECTION ( 'NONE',  ( -1.000000000000000000, 0.000000000000000000, -0.000000000000000000 ) ) ;
#19866=CIRCLE ( 'NONE', #5066, 44.99999999999998579 ) ;
#19867=DIRECTION ( 'NONE',  ( 1.000000000000000000, 0.000000000000000000, 0.000000000000000000 ) ) ;
#19868=ADVANCED_FACE ( 'NONE', ( #18822 ), #18610, .F. ) ;
#19869=CARTESIAN_POINT ( 'NONE',  ( 0.000000000000000000, -65.64563793391792501, -54.09103124042881916 ) ) ;
#19870=AXIS2_PLACEMENT_3D ( 'NONE', #2876, #202, #8294 ) ;
#19872=CARTESIAN_POINT ( 'NONE',  ( 10.00000000000000000, 41.21966518005955038, 82.80926399530301296 ) ) ;
#19874=CIRCLE ( 'NONE', #8238, 44.99999999999999289 ) ;
#19876=ORIENTED_EDGE ( 'NONE', *, *, #3958, .T. ) ;
#19877=AXIS2_PLACEMENT_3D ( 'NONE', #11437, #17671, #8138 ) ;
#19878=ADVANCED_FACE ( 'NONE', ( #14268 ), #21238, .F. ) ;
#19879=EDGE_LOOP ( 'NONE', ( #13163, #11890, #4938, #4228 ) ) ;
#19880=AXIS2_PLACEMENT_3D ( 'NONE', #4561, #5895, #4233 ) ;
#19883=CIRCLE ( 'NONE', #17777, 92.50100000000000477 ) ;
#19884=ORIENTED_EDGE ( 'NONE', *, *, #16216, .T. ) ;
#19885=DIRECTION ( 'NONE',  ( 0.000000000000000000, 0.000000000000000000, 1.000000000000000000 ) ) ;
#19886=LINE ( 'NONE', #4753, #16321 ) ;
#19887=ADVANCED_FACE ( 'NONE', ( #2792 ), #7769, .F. ) ;
#19888=CIRCLE ( 'NONE', #10009, 44.99999999999999289 ) ;
#19889=CARTESIAN_POINT ( 'NONE',  ( 0.000000000000000000, -46.89573839703219704, -79.73220629831536144 ) ) ;
#19891=DIRECTION ( 'NONE',  ( -1.000000000000000000, -0.000000000000000000, -0.000000000000000000 ) ) ;
#19892=EDGE_CURVE ( 'NONE', #12050, #6056, #10425, .T. ) ;
#19894=DIRECTION ( 'NONE',  ( -1.000000000000000000, 0.000000000000000000, 0.000000000000000000 ) ) ;
#19895=VECTOR ( 'NONE', #1038, 1000.000000000000000 ) ;
#19897=VERTEX_POINT ( 'NONE', #19578 ) ;
#19898=AXIS2_PLACEMENT_3D ( 'NONE', #7684, #4591, #6260 ) ;
#19899=ADVANCED_FACE ( 'NONE', ( #14386 ), #10959, .F. ) ;
#19900=DIRECTION ( 'NONE',  ( 1.000000000000000000, -0.000000000000000000, 0.000000000000000000 ) ) ;
#19903=CARTESIAN_POINT ( 'NONE',  ( 0.000000000000000000, -57.47876254627099257, -62.70072803846446163 ) ) ;
#19904=CIRCLE ( 'NONE', #17453, 44.99999999999999289 ) ;
#19905=EDGE_CURVE ( 'NONE', #1976, #18330, #17491, .T. ) ;
#19907=DIRECTION ( 'NONE',  ( 0.000000000000000000, 0.000000000000000000, 1.000000000000000000 ) ) ;
#19908=ORIENTED_EDGE ( 'NONE', *, *, #1411, .F. ) ;
#19912=LINE ( 'NONE', #4890, #290 ) ;
#19918=DIRECTION ( 'NONE',  ( 0.000000000000000000, -0.9848077530122062440, -0.1736481776669404897 ) ) ;
#19919=DIRECTION ( 'NONE',  ( -1.000000000000000000, -0.000000000000000000, -0.000000000000000000 ) ) ;
#19921=CYLINDRICAL_SURFACE ( 'NONE', #19971, 44.99999999999999289 ) ;
#19922=DIRECTION ( 'NONE',  ( 0.000000000000000000, 0.000000000000000000, 1.000000000000000000 ) ) ;
#19923=AXIS2_PLACEMENT_3D ( 'NONE', #20453, #13910, #17349 ) ;
#19925=ORIENTED_EDGE ( 'NONE', *, *, #12322, .T. ) ;
#19927=CIRCLE ( 'NONE', #4410, 44.99999999999999289 ) ;
#19929=FACE_OUTER_BOUND ( 'NONE', #1027, .T. ) ;
#19930=ORIENTED_EDGE ( 'NONE', *, *, #18953, .F. ) ;
#19932=ORIENTED_EDGE ( 'NONE', *, *, #12846, .F. ) ;
#19934=AXIS2_PLACEMENT_3D ( 'NONE', #9686, #9249, #14461 ) ;
#19936=CARTESIAN_POINT ( 'NONE',  ( -10.00000000000000000, 0.000000000000000000, 0.000000000000000000 ) ) ;
#19937=ORIENTED_EDGE ( 'NONE', *, *, #2575, .F. ) ;
#19938=VECTOR ( 'NONE', #12765, 1000.000000000000000 ) ;
#19942=ORIENTED_EDGE ( 'NONE', *, *, #4096, .F. ) ;
#19943=CIRCLE ( 'NONE', #4419, 88.00000000000000000 ) ;
#19946=CARTESIAN_POINT ( 'NONE',  ( 10.00000000000000000, 0.000000000000000000, 0.000000000000000000 ) ) ;
#19948=CIRCLE ( 'NONE', #3717, 88.00000000000000000 ) ;
#19949=CARTESIAN_POINT ( 'NONE',  ( 10.00000000000000000, 48.19312842678564834, -70.09002648625148879 ) ) ;
#19952=AXIS2_PLACEMENT_3D ( 'NONE', #4592, #13420, #6590 ) ;
#19953=VERTEX_POINT ( 'NONE', #6009 ) ;
#19954=DIRECTION ( 'NONE',  ( 0.000000000000000000, 0.000000000000000000, 1.000000000000000000 ) ) ;
#19955=DIRECTION ( 'NONE',  ( 0.000000000000000000, -0.8290375725550469532, 0.5591929034707392443 ) ) ;
#19957=AXIS2_PLACEMENT_3D ( 'NONE', #16741, #16305, #21828 ) ;
#19959=EDGE_CURVE ( 'NONE', #6202, #589, #12829, .T. ) ;
#19960=CIRCLE ( 'NONE', #8321, 44.99999999999999289 ) ;
#19962=AXIS2_PLACEMENT_3D ( 'NONE', #1006, #4542, #14812 ) ;
#19963=ORIENTED_EDGE ( 'NONE', *, *, #15816, .F. ) ;
#19964=DIRECTION ( 'NONE',  ( -1.000000000000000000, 0.000000000000000000, 0.000000000000000000 ) ) ;
#19965=DIRECTION ( 'NONE',  ( -1.000000000000000000, -0.000000000000000000, -0.000000000000000000 ) ) ;
#19966=VERTEX_POINT ( 'NONE', #10739 ) ;
#19967=DIRECTION ( 'NONE',  ( 0.000000000000000000, -0.7431448254773999063, 0.6691306063588519093 ) ) ;
#19968=ORIENTED_EDGE ( 'NONE', *, *, #3044, .T. ) ;
#19970=DIRECTION ( 'NONE',  ( -1.000000000000000000, 0.000000000000000000, 0.000000000000000000 ) ) ;
#19971=AXIS2_PLACEMENT_3D ( 'NONE', #9746, #4793, #13070 ) ;
#19972=ORIENTED_EDGE ( 'NONE', *, *, #20181, .F. ) ;
#19974=CARTESIAN_POINT ( 'NONE',  ( 0.000000000000000000, -31.15801000616779248, -79.14775961996421927 ) ) ;
#19976=VECTOR ( 'NONE', #16360, 1000.000000000000000 ) ;
#19978=AXIS2_PLACEMENT_3D ( 'NONE', #8852, #12379, #19025 ) ;
#19979=FACE_OUTER_BOUND ( 'NONE', #9530, .T. ) ;
#19983=CARTESIAN_POINT ( 'NONE',  ( 10.00000000000000000, -48.19312842678424857, -70.09002648625245513 ) ) ;
#19984=EDGE_CURVE ( 'NONE', #13200, #15636, #8118, .T. ) ;
#19986=CARTESIAN_POINT ( 'NONE',  ( 0.000000000000000000, -69.25892805976543798, 49.38005998797819274 ) ) ;
#19987=DIRECTION ( 'NONE',  ( 0.000000000000000000, 0.000000000000000000, 1.000000000000000000 ) ) ;
#19988=DIRECTION ( 'NONE',  ( 0.000000000000000000, -0.7431448254774000173, 0.6691306063588519093 ) ) ;
#19989=EDGE_LOOP ( 'NONE', ( #15772, #2114, #8890, #21672 ) ) ;
#19992=AXIS2_PLACEMENT_3D ( 'NONE', #19030, #17800, #11049 ) ;
#19993=ORIENTED_EDGE ( 'NONE', *, *, #9480, .T. ) ;
#19997=ORIENTED_EDGE ( 'NONE', *, *, #2455, .F. ) ;
#19998=EDGE_CURVE ( 'NONE', #15560, #6332, #4327, .T. ) ;
#19999=DIRECTION ( 'NONE',  ( 0.000000000000000000, -0.1391731009600519209, -0.9902680687415721383 ) ) ;
#20000=ORIENTED_EDGE ( 'NONE', *, *, #11246, .F. ) ;
#20001=DIRECTION ( 'NONE',  ( 0.000000000000000000, 0.000000000000000000, 1.000000000000000000 ) ) ;
#20002=CARTESIAN_POINT ( 'NONE',  ( 5.000000000000002665, 11.59241532900628258, 87.23311244498744088 ) ) ;
#20003=AXIS2_PLACEMENT_3D ( 'NONE', #14918, #4980, #2988 ) ;
#20004=ADVANCED_FACE ( 'NONE', ( #11067 ), #17816, .F. ) ;
#20005=CARTESIAN_POINT ( 'NONE',  ( 0.000000000000000000, 0.000000000000000000, 0.000000000000000000 ) ) ;
#20006=CIRCLE ( 'NONE', #1303, 44.99999999999999289 ) ;
#20008=EDGE_CURVE ( 'NONE', #20663, #16623, #17499, .T. ) ;
#20009=AXIS2_PLACEMENT_3D ( 'NONE', #1527, #9809, #5070 ) ;
#20012=AXIS2_PLACEMENT_3D ( 'NONE', #1989, #13368, #4979 ) ;
#20013=DIRECTION ( 'NONE',  ( -1.000000000000000000, -0.000000000000000000, 0.000000000000000000 ) ) ;
#20014=DIRECTION ( 'NONE',  ( 0.000000000000000000, 0.000000000000000000, 1.000000000000000000 ) ) ;
#20015=EDGE_CURVE ( 'NONE', #11182, #6332, #14773, .T. ) ;
#20016=ORIENTED_EDGE ( 'NONE', *, *, #20082, .F. ) ;
#20017=CARTESIAN_POINT ( 'NONE',  ( 0.000000000000000000, 68.36541360927260769, -50.60987712331631627 ) ) ;
#20018=EDGE_LOOP ( 'NONE', ( #9560, #9730, #9191, #3249 ) ) ;
#20021=CIRCLE ( 'NONE', #8728, 92.50100000000000477 ) ;
#20024=DIRECTION ( 'NONE',  ( 0.000000000000000000, 0.000000000000000000, -1.000000000000000000 ) ) ;
#20025=EDGE_LOOP ( 'NONE', ( #11290, #13631, #12499, #2090 ) ) ;
#20026=ADVANCED_FACE ( 'NONE', ( #7982 ), #6444, .F. ) ;
#20029=ORIENTED_EDGE ( 'NONE', *, *, #6143, .T. ) ;
#20030=DIRECTION ( 'NONE',  ( -1.000000000000000000, 0.000000000000000000, 0.000000000000000000 ) ) ;
#20032=EDGE_CURVE ( 'NONE', #1246, #4660, #1014, .T. ) ;
#20033=CARTESIAN_POINT ( 'NONE',  ( 10.00000000000000000, -92.49798535263882115, -0.7467976319030308341 ) ) ;
#20034=DIRECTION ( 'NONE',  ( 1.000000000000000000, 0.000000000000000000, 0.000000000000000000 ) ) ;
#20037=DIRECTION ( 'NONE',  ( 0.000000000000000000, 0.000000000000000000, 1.000000000000000000 ) ) ;
#20039=EDGE_CURVE ( 'NONE', #10149, #5754, #14714, .T. ) ;
#20042=ORIENTED_EDGE ( 'NONE', *, *, #9072, .T. ) ;
#20043=VECTOR ( 'NONE', #16607, 1000.000000000000000 ) ;
#20044=DIRECTION ( 'NONE',  ( 0.000000000000000000, 0.000000000000000000, 1.000000000000000000 ) ) ;
#20046=ORIENTED_EDGE ( 'NONE', *, *, #13110, .T. ) ;
#20047=DIRECTION ( 'NONE',  ( -1.000000000000000000, -0.000000000000000000, -0.000000000000000000 ) ) ;
#20048=EDGE_CURVE ( 'NONE', #3139, #13772, #6662, .T. ) ;
#20049=VERTEX_POINT ( 'NONE', #15042 ) ;
#20050=VECTOR ( 'NONE', #5758, 1000.000000000000000 ) ;
#20051=VECTOR ( 'NONE', #20597, 1000.000000000000000 ) ;
#20052=EDGE_LOOP ( 'NONE', ( #10445, #1918, #10551, #5981 ) ) ;
#20054=ORIENTED_EDGE ( 'NONE', *, *, #1249, .F. ) ;
#20057=CARTESIAN_POINT ( 'NONE',  ( 10.00000000000000000, -71.33759994382000968, 58.88447872958963814 ) ) ;
#20058=AXIS2_PLACEMENT_3D ( 'NONE', #7853, #4651, #16683 ) ;
#20062=CARTESIAN_POINT ( 'NONE',  ( -10.00000000000000000, 0.000000000000000000, 0.000000000000000000 ) ) ;
#20063=DIRECTION ( 'NONE',  ( -1.000000000000000000, -0.000000000000000000, -0.000000000000000000 ) ) ;
#20065=DIRECTION ( 'NONE',  ( 0.000000000000000000, 0.000000000000000000, 1.000000000000000000 ) ) ;
#20068=ORIENTED_EDGE ( 'NONE', *, *, #7761, .T. ) ;
#20069=CARTESIAN_POINT ( 'NONE',  ( 0.000000000000000000, 48.19312842678472464, 70.09002648625214249 ) ) ;
#20070=CIRCLE ( 'NONE', #2091, 88.00000000000000000 ) ;
#20072=VECTOR ( 'NONE', #12719, 1000.000000000000000 ) ;
#20074=AXIS2_PLACEMENT_3D ( 'NONE', #14916, #9938, #18360 ) ;
#20075=CIRCLE ( 'NONE', #6317, 88.00000000000000000 ) ;
#20076=AXIS2_PLACEMENT_3D ( 'NONE', #603, #14079, #2250 ) ;
#20078=DIRECTION ( 'NONE',  ( 1.000000000000000000, 0.000000000000000000, 0.000000000000000000 ) ) ;
#20079=EDGE_LOOP ( 'NONE', ( #10608, #2834, #19884, #3393 ) ) ;
#20081=DIRECTION ( 'NONE',  ( 0.000000000000000000, 0.000000000000000000, 1.000000000000000000 ) ) ;
#20082=EDGE_CURVE ( 'NONE', #19773, #1794, #19355, .T. ) ;
#20083=ORIENTED_EDGE ( 'NONE', *, *, #12217, .F. ) ;
#20085=VERTEX_POINT ( 'NONE', #7867 ) ;
#20086=VERTEX_POINT ( 'NONE', #9612 ) ;
#20087=CARTESIAN_POINT ( 'NONE',  ( 0.000000000000000000, 0.000000000000000000, 0.000000000000000000 ) ) ;
#20088=ORIENTED_EDGE ( 'NONE', *, *, #13126, .T. ) ;
#20090=AXIS2_PLACEMENT_3D ( 'NONE', #9911, #14889, #19760 ) ;
#20092=DIRECTION ( 'NONE',  ( -1.000000000000000000, -0.000000000000000000, 0.000000000000000000 ) ) ;
#20093=VECTOR ( 'NONE', #8359, 1000.000000000000000 ) ;
#20095=AXIS2_PLACEMENT_3D ( 'NONE', #17656, #5618, #636 ) ;
#20096=CIRCLE ( 'NONE', #15491, 92.50100000000000477 ) ;
#20097=DIRECTION ( 'NONE',  ( 1.000000000000000000, 0.000000000000000000, 0.000000000000000000 ) ) ;
#20099=CARTESIAN_POINT ( 'NONE',  ( 0.000000000000000000, 0.000000000000000000, 0.000000000000000000 ) ) ;
#20100=CARTESIAN_POINT ( 'NONE',  ( -10.00000000000000000, 0.000000000000000000, 0.000000000000000000 ) ) ;
#20107=AXIS2_PLACEMENT_3D ( 'NONE', #15630, #3926, #10233 ) ;
#20108=ORIENTED_EDGE ( 'NONE', *, *, #4363, .F. ) ;
#20110=AXIS2_PLACEMENT_3D ( 'NONE', #9338, #5934, #19187 ) ;
#20111=ORIENTED_EDGE ( 'NONE', *, *, #20414, .F. ) ;
#20112=VERTEX_POINT ( 'NONE', #4556 ) ;
#20114=ORIENTED_EDGE ( 'NONE', *, *, #16743, .T. ) ;
#20115=CARTESIAN_POINT ( 'NONE',  ( 10.00000000000000000, 0.000000000000000000, 0.000000000000000000 ) ) ;
#20116=VERTEX_POINT ( 'NONE', #16594 ) ;
#20117=CYLINDRICAL_SURFACE ( 'NONE', #1854, 44.99999999999999289 ) ;
#20119=EDGE_CURVE ( 'NONE', #10039, #12967, #11397, .T. ) ;
#20120=DIRECTION ( 'NONE',  ( 0.000000000000000000, 0.000000000000000000, 1.000000000000000000 ) ) ;
#20122=CIRCLE ( 'NONE', #9501, 45.00000000000000000 ) ;
#20125=CARTESIAN_POINT ( 'NONE',  ( 10.00000000000000000, -68.93609746931198856, 54.69748134696436637 ) ) ;
#20127=FACE_OUTER_BOUND ( 'NONE', #16574, .T. ) ;
#20129=ORIENTED_EDGE ( 'NONE', *, *, #3615, .F. ) ;
#20130=CARTESIAN_POINT ( 'NONE',  ( 0.000000000000000000, 52.25832601289098278, 70.80301803122803506 ) ) ;
#20131=EDGE_CURVE ( 'NONE', #21840, #14663, #2078, .T. ) ;
#20132=ORIENTED_EDGE ( 'NONE', *, *, #8798, .F. ) ;
#20133=EDGE_CURVE ( 'NONE', #16928, #3486, #15826, .T. ) ;
#20134=ADVANCED_FACE ( 'NONE', ( #21565 ), #11514, .F. ) ;
#20135=CIRCLE ( 'NONE', #15538, 44.99999999999998579 ) ;
#20136=CARTESIAN_POINT ( 'NONE',  ( 10.00000000000000000, 9.646732466565339337, 84.51112348751853176 ) ) ;
#20138=ORIENTED_EDGE ( 'NONE', *, *, #6219, .T. ) ;
#20139=DIRECTION ( 'NONE',  ( -1.000000000000000000, -0.000000000000000000, -0.000000000000000000 ) ) ;
#20140=EDGE_CURVE ( 'NONE', #1976, #6010, #9451, .T. ) ;
#20141=ORIENTED_EDGE ( 'NONE', *, *, #15816, .T. ) ;
#20142=CARTESIAN_POINT ( 'NONE',  ( 0.000000000000000000, -89.12061559554348378, 24.77803214283513356 ) ) ;
#20143=DIRECTION ( 'NONE',  ( 0.000000000000000000, -1.850371707708594444E-14, -1.000000000000000000 ) ) ;
#20144=DIRECTION ( 'NONE',  ( 1.000000000000000000, 0.000000000000000000, 0.000000000000000000 ) ) ;
#20146=DIRECTION ( 'NONE',  ( 1.000000000000000000, -0.000000000000000000, -0.000000000000000000 ) ) ;
#20149=EDGE_CURVE ( 'NONE', #7036, #19371, #20764, .T. ) ;
#20150=DIRECTION ( 'NONE',  ( 1.000000000000000000, 0.000000000000000000, 0.000000000000000000 ) ) ;
#20152=EDGE_CURVE ( 'NONE', #14408, #3061, #11601, .T. ) ;
#20153=LINE ( 'NONE', #18286, #8402 ) ;
#20155=ORIENTED_EDGE ( 'NONE', *, *, #15673, .T. ) ;
#20156=VECTOR ( 'NONE', #14968, 1000.000000000000000 ) ;
#20157=CARTESIAN_POINT ( 'NONE',  ( 0.000000000000000000, -56.35896156214997887, 73.34918167666290856 ) ) ;
#20158=ORIENTED_EDGE ( 'NONE', *, *, #9430, .F. ) ;
#20159=ORIENTED_EDGE ( 'NONE', *, *, #6269, .T. ) ;
#20160=DIRECTION ( 'NONE',  ( 0.000000000000000000, 0.2079116908177531808, 0.9781476007338069101 ) ) ;
#20161=EDGE_CURVE ( 'NONE', #1536, #14184, #8311, .T. ) ;
#20164=DIRECTION ( 'NONE',  ( 1.000000000000000000, 0.000000000000000000, -0.000000000000000000 ) ) ;
#20165=CARTESIAN_POINT ( 'NONE',  ( -10.00000000000000000, 0.000000000000000000, 0.000000000000000000 ) ) ;
#20166=VERTEX_POINT ( 'NONE', #11726 ) ;
#20167=LINE ( 'NONE', #11873, #16391 ) ;
#20169=CYLINDRICAL_SURFACE ( 'NONE', #3731, 88.00000000000000000 ) ;
#20171=LINE ( 'NONE', #17297, #479 ) ;
#20174=VERTEX_POINT ( 'NONE', #3552 ) ;
#20175=EDGE_CURVE ( 'NONE', #13650, #18608, #20075, .T. ) ;
#20177=CARTESIAN_POINT ( 'NONE',  ( 0.000000000000000000, 84.19736439813857487, -38.30455363800847124 ) ) ;
#20178=ORIENTED_EDGE ( 'NONE', *, *, #12935, .F. ) ;
#20180=ADVANCED_FACE ( 'NONE', ( #125 ), #6875, .F. ) ;
#20181=EDGE_CURVE ( 'NONE', #13328, #19013, #10176, .T. ) ;
#20185=FACE_OUTER_BOUND ( 'NONE', #9948, .T. ) ;
#20186=ORIENTED_EDGE ( 'NONE', *, *, #15032, .T. ) ;
#20187=DIRECTION ( 'NONE',  ( 0.000000000000000000, 0.000000000000000000, 1.000000000000000000 ) ) ;
#20188=AXIS2_PLACEMENT_3D ( 'NONE', #10132, #13447, #1423 ) ;
#20189=ORIENTED_EDGE ( 'NONE', *, *, #9175, .F. ) ;
#20190=ORIENTED_EDGE ( 'NONE', *, *, #1537, .T. ) ;
#20191=VERTEX_POINT ( 'NONE', #1680 ) ;
#20192=CARTESIAN_POINT ( 'NONE',  ( 10.00000000000000000, 0.000000000000000000, 0.000000000000000000 ) ) ;
#20193=ORIENTED_EDGE ( 'NONE', *, *, #11511, .F. ) ;
#20194=CARTESIAN_POINT ( 'NONE',  ( 10.00000000000000000, 0.000000000000000000, 0.000000000000000000 ) ) ;
#20195=CARTESIAN_POINT ( 'NONE',  ( -10.00000000000000000, 0.000000000000000000, 0.000000000000000000 ) ) ;
#20196=LINE ( 'NONE', #18542, #5770 ) ;
#20199=AXIS2_PLACEMENT_3D ( 'NONE', #18917, #12167, #245 ) ;
#20200=DIRECTION ( 'NONE',  ( -1.000000000000000000, -0.000000000000000000, -0.000000000000000000 ) ) ;
#20202=CARTESIAN_POINT ( 'NONE',  ( 0.000000000000000000, 92.49798535263880694, -0.7467976319023919007 ) ) ;
#20203=CIRCLE ( 'NONE', #6442, 92.50099999999999056 ) ;
#20205=VECTOR ( 'NONE', #13882, 1000.000000000000000 ) ;
#20206=CARTESIAN_POINT ( 'NONE',  ( 0.000000000000000000, 0.000000000000000000, 0.000000000000000000 ) ) ;
#20207=VERTEX_POINT ( 'NONE', #15148 ) ;
#20208=DIRECTION ( 'NONE',  ( 0.000000000000000000, -0.7431448254773861395, -0.6691306063588670083 ) ) ;
#20214=ORIENTED_EDGE ( 'NONE', *, *, #10361, .T. ) ;
#20215=DIRECTION ( 'NONE',  ( -1.000000000000000000, 0.000000000000000000, 0.000000000000000000 ) ) ;
#20216=AXIS2_PLACEMENT_3D ( 'NONE', #20005, #11822, #16913 ) ;
#20217=CIRCLE ( 'NONE', #13151, 44.99999999999999289 ) ;
#20218=ORIENTED_EDGE ( 'NONE', *, *, #2283, .F. ) ;
#20220=CARTESIAN_POINT ( 'NONE',  ( 0.000000000000000000, -41.87002153499058466, -74.04114219178087808 ) ) ;
#20224=CARTESIAN_POINT ( 'NONE',  ( 5.000000000000002665, -85.54350296776125617, 20.64725405482824883 ) ) ;
#20229=EDGE_LOOP ( 'NONE', ( #15313, #15282, #4656, #8849 ) ) ;
#20232=AXIS2_PLACEMENT_3D ( 'NONE', #3184, #20092, #6735 ) ;
#20234=EDGE_CURVE ( 'NONE', #18952, #10029, #13343, .T. ) ;
#20236=ORIENTED_EDGE ( 'NONE', *, *, #18393, .T. ) ;
#20239=ORIENTED_EDGE ( 'NONE', *, *, #20284, .T. ) ;
#20243=DIRECTION ( 'NONE',  ( 1.000000000000000000, 0.000000000000000000, 0.000000000000000000 ) ) ;
#20245=EDGE_LOOP ( 'NONE', ( #17788, #6923, #15974, #10241 ) ) ;
#20246=CARTESIAN_POINT ( 'NONE',  ( 0.000000000000000000, 74.74361964203228581, 40.60271866773572214 ) ) ;
#20247=VECTOR ( 'NONE', #10752, 1000.000000000000000 ) ;
#20248=CARTESIAN_POINT ( 'NONE',  ( 10.00000000000000000, -33.95793648385753727, -86.04239391578025220 ) ) ;
#20249=CYLINDRICAL_SURFACE ( 'NONE', #19533, 44.99999999999999289 ) ;
#20250=CARTESIAN_POINT ( 'NONE',  ( 5.000000000000000000, 60.65279801375342572, 63.75921967137637836 ) ) ;
#20251=CIRCLE ( 'NONE', #10713, 44.99999999999999289 ) ;
#20256=EDGE_CURVE ( 'NONE', #6428, #11431, #8598, .T. ) ;
#20257=ORIENTED_EDGE ( 'NONE', *, *, #1265, .F. ) ;
#20258=ADVANCED_FACE ( 'NONE', ( #5396 ), #13456, .F. ) ;
#20260=DIRECTION ( 'NONE',  ( -1.000000000000000000, 0.000000000000000000, 0.000000000000000000 ) ) ;
#20262=CARTESIAN_POINT ( 'NONE',  ( 0.000000000000000000, 72.58367602204255320, -49.75550195834793499 ) ) ;
#20264=DIRECTION ( 'NONE',  ( 0.000000000000000000, 0.000000000000000000, 1.000000000000000000 ) ) ;
#20265=ORIENTED_EDGE ( 'NONE', *, *, #2882, .F. ) ;
#20266=AXIS2_PLACEMENT_3D ( 'NONE', #7796, #1389, #19616 ) ;
#20268=EDGE_CURVE ( 'NONE', #20166, #9696, #15447, .T. ) ;
#20269=ORIENTED_EDGE ( 'NONE', *, *, #1503, .F. ) ;
#20270=CARTESIAN_POINT ( 'NONE',  ( 10.00000000000000000, -84.80486432185219314, 36.94008646920367056 ) ) ;
#20271=VERTEX_POINT ( 'NONE', #15219 ) ;
#20272=ORIENTED_EDGE ( 'NONE', *, *, #19845, .F. ) ;
#20274=CARTESIAN_POINT ( 'NONE',  ( 10.00000000000000000, 78.83848282823907994, 48.38314403117527718 ) ) ;
#20278=DIRECTION ( 'NONE',  ( 0.000000000000000000, -0.5877852522924797984, 0.8090169943749425663 ) ) ;
#20280=DIRECTION ( 'NONE',  ( -1.000000000000000000, 0.000000000000000000, -0.000000000000000000 ) ) ;
#20281=DIRECTION ( 'NONE',  ( 0.000000000000000000, 0.000000000000000000, 1.000000000000000000 ) ) ;
#20283=AXIS2_PLACEMENT_3D ( 'NONE', #8977, #16046, #2471 ) ;
#20284=EDGE_CURVE ( 'NONE', #845, #18327, #1365, .T. ) ;
#20287=LINE ( 'NONE', #18632, #18567 ) ;
#20288=EDGE_CURVE ( 'NONE', #16240, #9108, #13713, .T. ) ;
#20290=ORIENTED_EDGE ( 'NONE', *, *, #4405, .F. ) ;
#20291=CYLINDRICAL_SURFACE ( 'NONE', #18280, 44.99999999999999289 ) ;
#20293=AXIS2_PLACEMENT_3D ( 'NONE', #14130, #10701, #9043 ) ;
#20294=LINE ( 'NONE', #15089, #17631 ) ;
#20297=ORIENTED_EDGE ( 'NONE', *, *, #11108, .F. ) ;
#20298=CIRCLE ( 'NONE', #11155, 88.00000000000000000 ) ;
#20299=CARTESIAN_POINT ( 'NONE',  ( 0.000000000000000000, -30.71797041605752554, -82.46457599186584275 ) ) ;
#20302=ORIENTED_EDGE ( 'NONE', *, *, #3673, .T. ) ;
#20303=ORIENTED_EDGE ( 'NONE', *, *, #9027, .T. ) ;
#20304=VERTEX_POINT ( 'NONE', #18345 ) ;
#20306=EDGE_CURVE ( 'NONE', #1, #15334, #2093, .T. ) ;
#20307=AXIS2_PLACEMENT_3D ( 'NONE', #12136, #3748, #10480 ) ;
#20309=CARTESIAN_POINT ( 'NONE',  ( 10.00000000000000000, -75.87763420127865288, 44.57111876559696384 ) ) ;
#20310=CARTESIAN_POINT ( 'NONE',  ( 10.00000000000000000, -21.65267340503310223, 89.93106657554424999 ) ) ;
#20311=LINE ( 'NONE', #1741, #9260 ) ;
#20314=ADVANCED_FACE ( 'NONE', ( #16897 ), #1531, .F. ) ;
#20315=CIRCLE ( 'NONE', #4416, 92.50100000000000477 ) ;
#20316=CARTESIAN_POINT ( 'NONE',  ( 10.00000000000000000, 0.000000000000000000, 0.000000000000000000 ) ) ;
#20318=DIRECTION ( 'NONE',  ( 1.000000000000000000, 0.000000000000000000, 0.000000000000000000 ) ) ;
#20319=CARTESIAN_POINT ( 'NONE',  ( 0.000000000000000000, -80.18694381077126820, 28.37681241246628616 ) ) ;
#20320=CIRCLE ( 'NONE', #16424, 44.99999999999999289 ) ;
#20322=LINE ( 'NONE', #20432, #11486 ) ;
#20324=ORIENTED_EDGE ( 'NONE', *, *, #17422, .T. ) ;
#20325=EDGE_LOOP ( 'NONE', ( #7381, #21466, #4513, #2277 ) ) ;
#20327=CARTESIAN_POINT ( 'NONE',  ( 0.000000000000000000, 45.60224695560570041, 80.47900393021744492 ) ) ;
#20328=ORIENTED_EDGE ( 'NONE', *, *, #3097, .F. ) ;
#20329=CIRCLE ( 'NONE', #7964, 45.00000000000000000 ) ;
#20330=VERTEX_POINT ( 'NONE', #6847 ) ;
#20331=AXIS2_PLACEMENT_3D ( 'NONE', #8470, #4115, #8677 ) ;
#20332=VECTOR ( 'NONE', #14623, 1000.000000000000000 ) ;
#20335=CIRCLE ( 'NONE', #1276, 44.99999999999999289 ) ;
#20337=ORIENTED_EDGE ( 'NONE', *, *, #7863, .T. ) ;
#20338=CARTESIAN_POINT ( 'NONE',  ( 10.00000000000000000, 0.000000000000000000, 0.000000000000000000 ) ) ;
#20344=DIRECTION ( 'NONE',  ( 1.000000000000000000, 0.000000000000000000, 0.000000000000000000 ) ) ;
#20345=DIRECTION ( 'NONE',  ( 1.000000000000000000, 0.000000000000000000, 0.000000000000000000 ) ) ;
#20346=CYLINDRICAL_SURFACE ( 'NONE', #9473, 44.99999999999998579 ) ;
#20348=ORIENTED_EDGE ( 'NONE', *, *, #18949, .T. ) ;
#20349=CIRCLE ( 'NONE', #3404, 92.50100000000001899 ) ;
#20350=CARTESIAN_POINT ( 'NONE',  ( 0.000000000000000000, 87.58454185039451545, -8.540961822680756654 ) ) ;
#20352=ORIENTED_EDGE ( 'NONE', *, *, #10758, .T. ) ;
#20357=ORIENTED_EDGE ( 'NONE', *, *, #17195, .T. ) ;
#20359=DIRECTION ( 'NONE',  ( 1.000000000000000000, 0.000000000000000000, 0.000000000000000000 ) ) ;
#20360=VERTEX_POINT ( 'NONE', #3738 ) ;
#20361=AXIS2_PLACEMENT_3D ( 'NONE', #11917, #18667, #8817 ) ;
#20362=CIRCLE ( 'NONE', #19992, 92.50100000000000477 ) ;
#20363=CARTESIAN_POINT ( 'NONE',  ( 0.000000000000000000, -35.34277389771475697, -85.48288328206420772 ) ) ;
#20364=CARTESIAN_POINT ( 'NONE',  ( 10.00000000000000000, -70.37753541435900217, -60.02863908169706519 ) ) ;
#20365=DIRECTION ( 'NONE',  ( 0.000000000000000000, 0.000000000000000000, 1.000000000000000000 ) ) ;
#20366=DIRECTION ( 'NONE',  ( 1.000000000000000000, 0.000000000000000000, -0.000000000000000000 ) ) ;
#20367=EDGE_CURVE ( 'NONE', #5777, #13297, #19093, .T. ) ;
#20370=CARTESIAN_POINT ( 'NONE',  ( 0.000000000000000000, -46.93287725819731548, -70.94007663282492615 ) ) ;
#20373=CIRCLE ( 'NONE', #3082, 88.00000000000000000 ) ;
#20374=CIRCLE ( 'NONE', #16488, 92.50100000000000477 ) ;
#20378=CARTESIAN_POINT ( 'NONE',  ( 0.000000000000000000, 39.87723064937233630, -83.46401306393528330 ) ) ;
#20379=ORIENTED_EDGE ( 'NONE', *, *, #2046, .F. ) ;
#20381=CARTESIAN_POINT ( 'NONE',  ( 0.000000000000000000, 81.83745710415276164, 32.35167097270178260 ) ) ;
#20382=ORIENTED_EDGE ( 'NONE', *, *, #18669, .T. ) ;
#20384=EDGE_LOOP ( 'NONE', ( #10960, #18636, #15891, #1998 ) ) ;
#20385=CARTESIAN_POINT ( 'NONE',  ( 0.000000000000000000, 0.000000000000000000, 0.000000000000000000 ) ) ;
#20387=DIRECTION ( 'NONE',  ( -1.000000000000000000, 0.000000000000000000, 0.000000000000000000 ) ) ;
#20390=DIRECTION ( 'NONE',  ( 1.000000000000000000, 0.000000000000000000, 0.000000000000000000 ) ) ;
#20392=FACE_OUTER_BOUND ( 'NONE', #19115, .T. ) ;
#20394=ADVANCED_FACE ( 'NONE', ( #2182 ), #7161, .F. ) ;
#20396=DIRECTION ( 'NONE',  ( 0.000000000000000000, 0.000000000000000000, 1.000000000000000000 ) ) ;
#20397=ORIENTED_EDGE ( 'NONE', *, *, #20152, .T. ) ;
#20398=FACE_OUTER_BOUND ( 'NONE', #9227, .T. ) ;
#20399=ADVANCED_FACE ( 'NONE', ( #10471 ), #13892, .F. ) ;
#20401=ORIENTED_EDGE ( 'NONE', *, *, #13794, .F. ) ;
#20402=DIRECTION ( 'NONE',  ( 1.000000000000000000, 0.000000000000000000, 0.000000000000000000 ) ) ;
#20404=CIRCLE ( 'NONE', #17577, 88.00000000000000000 ) ;
#20405=AXIS2_PLACEMENT_3D ( 'NONE', #1251, #1573, #18384 ) ;
#20406=FACE_OUTER_BOUND ( 'NONE', #2738, .T. ) ;
#20408=VECTOR ( 'NONE', #58, 1000.000000000000000 ) ;
#20411=ORIENTED_EDGE ( 'NONE', *, *, #20677, .T. ) ;
#20412=EDGE_CURVE ( 'NONE', #8121, #15908, #3140, .T. ) ;
#20413=VERTEX_POINT ( 'NONE', #14003 ) ;
#20414=EDGE_CURVE ( 'NONE', #7194, #15275, #3849, .T. ) ;
#20415=EDGE_LOOP ( 'NONE', ( #4537, #6146, #13842, #11088 ) ) ;
#20417=CARTESIAN_POINT ( 'NONE',  ( 0.000000000000000000, -27.00677879429080974, 80.65868421664423238 ) ) ;
#20418=VERTEX_POINT ( 'NONE', #3949 ) ;
#20421=DIRECTION ( 'NONE',  ( -1.000000000000000000, 0.000000000000000000, 0.000000000000000000 ) ) ;
#20423=DIRECTION ( 'NONE',  ( -1.000000000000000000, -0.000000000000000000, -0.000000000000000000 ) ) ;
#20424=DIRECTION ( 'NONE',  ( 0.000000000000000000, -0.9945218953682722907, -0.1045284632676634767 ) ) ;
#20426=AXIS2_PLACEMENT_3D ( 'NONE', #10153, #20215, #6427 ) ;
#20427=CARTESIAN_POINT ( 'NONE',  ( 0.000000000000000000, -45.60224695560514618, -80.47900393021774335 ) ) ;
#20429=VECTOR ( 'NONE', #4989, 1000.000000000000000 ) ;
#20430=DIRECTION ( 'NONE',  ( 0.000000000000000000, 0.000000000000000000, 1.000000000000000000 ) ) ;
#20432=CARTESIAN_POINT ( 'NONE',  ( 10.00000000000000000, -15.32665449651862843, -91.22241316115434984 ) ) ;
#20434=DIRECTION ( 'NONE',  ( -1.000000000000000000, -0.000000000000000000, -0.000000000000000000 ) ) ;
#20435=VERTEX_POINT ( 'NONE', #7277 ) ;
#20437=VERTEX_POINT ( 'NONE', #847 ) ;
#20438=DIRECTION ( 'NONE',  ( 0.000000000000000000, 0.9945218953682728458, 0.1045284632676570791 ) ) ;
#20440=ORIENTED_EDGE ( 'NONE', *, *, #562, .F. ) ;
#20444=AXIS2_PLACEMENT_3D ( 'NONE', #15470, #17132, #3641 ) ;
#20445=ORIENTED_EDGE ( 'NONE', *, *, #7355, .T. ) ;
#20446=DIRECTION ( 'NONE',  ( 0.000000000000000000, -0.1391731009600725710, 0.9902680687415692518 ) ) ;
#20447=EDGE_CURVE ( 'NONE', #18539, #10503, #12350, .T. ) ;
#20449=CYLINDRICAL_SURFACE ( 'NONE', #1158, 45.00000000000000000 ) ;
#20451=DIRECTION ( 'NONE',  ( 0.000000000000000000, 0.000000000000000000, 1.000000000000000000 ) ) ;
#20453=CARTESIAN_POINT ( 'NONE',  ( 10.00000000000000000, 0.000000000000000000, 0.000000000000000000 ) ) ;
#20455=CARTESIAN_POINT ( 'NONE',  ( 10.00000000000000000, -35.34277389771592226, 85.48288328206373876 ) ) ;
#20456=CIRCLE ( 'NONE', #9482, 44.99999999999998579 ) ;
#20461=AXIS2_PLACEMENT_3D ( 'NONE', #11698, #17103, #5293 ) ;
#20464=EDGE_CURVE ( 'NONE', #19773, #301, #5610, .T. ) ;
#20467=CARTESIAN_POINT ( 'NONE',  ( 0.000000000000000000, -62.44821182181044605, -68.23969402963567177 ) ) ;
#20468=ORIENTED_EDGE ( 'NONE', *, *, #21637, .F. ) ;
#20469=ORIENTED_EDGE ( 'NONE', *, *, #162, .F. ) ;
#20471=ORIENTED_EDGE ( 'NONE', *, *, #13204, .F. ) ;
#20472=CIRCLE ( 'NONE', #9502, 88.00000000000000000 ) ;
#20473=FACE_OUTER_BOUND ( 'NONE', #17786, .T. ) ;
#20476=DIRECTION ( 'NONE',  ( -1.000000000000000000, -0.000000000000000000, -0.000000000000000000 ) ) ;
#20478=DIRECTION ( 'NONE',  ( 0.000000000000000000, 0.4067366430757948792, 0.9135454576426031981 ) ) ;
#20479=CARTESIAN_POINT ( 'NONE',  ( 10.00000000000000000, 86.66425444033963288, -32.33793443156312009 ) ) ;
#20480=ORIENTED_EDGE ( 'NONE', *, *, #21127, .T. ) ;
#20484=ORIENTED_EDGE ( 'NONE', *, *, #12443, .T. ) ;
#20485=FACE_OUTER_BOUND ( 'NONE', #19228, .T. ) ;
#20492=CARTESIAN_POINT ( 'NONE',  ( 5.000000000000000000, -64.95266917914277371, -59.37298010463037912 ) ) ;
#20493=CARTESIAN_POINT ( 'NONE',  ( -10.00000000000000000, 0.000000000000000000, 0.000000000000000000 ) ) ;
#20495=CARTESIAN_POINT ( 'NONE',  ( 0.000000000000000000, -83.03980459022467642, -18.42770452393328995 ) ) ;
#20496=DIRECTION ( 'NONE',  ( 1.000000000000000000, 0.000000000000000000, 0.000000000000000000 ) ) ;
#20499=LINE ( 'NONE', #18516, #5769 ) ;
#20501=ORIENTED_EDGE ( 'NONE', *, *, #19319, .F. ) ;
#20502=DIRECTION ( 'NONE',  ( 1.000000000000000000, 0.000000000000000000, 0.000000000000000000 ) ) ;
#20504=EDGE_CURVE ( 'NONE', #15756, #2852, #9835, .T. ) ;
#20506=CYLINDRICAL_SURFACE ( 'NONE', #17221, 88.00000000000000000 ) ;
#20507=VERTEX_POINT ( 'NONE', #4274 ) ;
#20508=CYLINDRICAL_SURFACE ( 'NONE', #1744, 88.00000000000000000 ) ;
#20513=ORIENTED_EDGE ( 'NONE', *, *, #72, .F. ) ;
#20515=ORIENTED_EDGE ( 'NONE', *, *, #3887, .F. ) ;
#20517=ORIENTED_EDGE ( 'NONE', *, *, #15293, .T. ) ;
#20518=DIRECTION ( 'NONE',  ( 0.000000000000000000, 0.5299192642331999048, 0.8480480961564290654 ) ) ;
#20519=CARTESIAN_POINT ( 'NONE',  ( 10.00000000000000000, 0.000000000000000000, 0.000000000000000000 ) ) ;
#20522=DIRECTION ( 'NONE',  ( 0.000000000000000000, 0.000000000000000000, 1.000000000000000000 ) ) ;
#20525=DIRECTION ( 'NONE',  ( 0.000000000000000000, 0.7880107536067190166, 0.6156614753256620665 ) ) ;
#20526=DIRECTION ( 'NONE',  ( 1.000000000000000000, 0.000000000000000000, 0.000000000000000000 ) ) ;
#20528=EDGE_LOOP ( 'NONE', ( #4685, #17259, #21265, #7889 ) ) ;
#20529=FACE_OUTER_BOUND ( 'NONE', #990, .T. ) ;
#20530=DIRECTION ( 'NONE',  ( -1.000000000000000000, -0.000000000000000000, 0.000000000000000000 ) ) ;
#20532=EDGE_CURVE ( 'NONE', #14363, #11540, #665, .T. ) ;
#20535=ORIENTED_EDGE ( 'NONE', *, *, #2018, .F. ) ;
#20536=ADVANCED_FACE ( 'NONE', ( #14879 ), #14441, .F. ) ;
#20537=DIRECTION ( 'NONE',  ( 1.000000000000000000, 0.000000000000000000, 0.000000000000000000 ) ) ;
#20538=VERTEX_POINT ( 'NONE', #21519 ) ;
#20542=DIRECTION ( 'NONE',  ( 1.000000000000000000, 0.000000000000000000, 0.000000000000000000 ) ) ;
#20543=VERTEX_POINT ( 'NONE', #16097 ) ;
#20545=CARTESIAN_POINT ( 'NONE',  ( 10.00000000000000000, 0.000000000000000000, 0.000000000000000000 ) ) ;
#20547=DIRECTION ( 'NONE',  ( 1.000000000000000000, 0.000000000000000000, 0.000000000000000000 ) ) ;
#20548=CARTESIAN_POINT ( 'NONE',  ( 0.000000000000000000, 41.87002153499211232, -74.04114219178001122 ) ) ;
#20550=VECTOR ( 'NONE', #4424, 1000.000000000000000 ) ;
#20551=DIRECTION ( 'NONE',  ( 0.000000000000000000, 0.000000000000000000, 1.000000000000000000 ) ) ;
#20555=DIRECTION ( 'NONE',  ( 0.000000000000000000, 0.000000000000000000, 1.000000000000000000 ) ) ;
#20560=ORIENTED_EDGE ( 'NONE', *, *, #4449, .T. ) ;
#20561=DIRECTION ( 'NONE',  ( -1.000000000000000000, -0.000000000000000000, 0.000000000000000000 ) ) ;
#20562=EDGE_LOOP ( 'NONE', ( #14809, #4155, #4152, #11749 ) ) ;
#20565=ADVANCED_FACE ( 'NONE', ( #11238, #18088 ), #17990, .F. ) ;
#20566=CARTESIAN_POINT ( 'NONE',  ( 0.000000000000000000, -71.33759994382000968, 58.88447872958963814 ) ) ;
#20567=VERTEX_POINT ( 'NONE', #21185 ) ;
#20568=ADVANCED_FACE ( 'NONE', ( #3059 ), #9558, .F. ) ;
#20569=DIRECTION ( 'NONE',  ( 1.000000000000000000, 0.000000000000000000, 0.000000000000000000 ) ) ;
#20571=DIRECTION ( 'NONE',  ( 1.000000000000000000, 0.000000000000000000, 0.000000000000000000 ) ) ;
#20573=CARTESIAN_POINT ( 'NONE',  ( 5.000000000000000000, -60.65279801375299229, -63.75921967137679047 ) ) ;
#20574=EDGE_CURVE ( 'NONE', #8180, #3874, #1412, .T. ) ;
#20575=EDGE_CURVE ( 'NONE', #18927, #19144, #21490, .T. ) ;
#20576=DIRECTION ( 'NONE',  ( -1.000000000000000000, 0.000000000000000000, 0.000000000000000000 ) ) ;
#20578=CARTESIAN_POINT ( 'NONE',  ( 10.00000000000000000, -71.72924546249915068, -45.71766382684744201 ) ) ;
#20580=AXIS2_PLACEMENT_3D ( 'NONE', #2351, #13956, #8657 ) ;
#20581=EDGE_CURVE ( 'NONE', #378, #15558, #1180, .T. ) ;
#20582=DIRECTION ( 'NONE',  ( 0.000000000000000000, 0.000000000000000000, 1.000000000000000000 ) ) ;
#20586=CYLINDRICAL_SURFACE ( 'NONE', #3019, 92.50100000000000477 ) ;
#20587=ORIENTED_EDGE ( 'NONE', *, *, #11903, .F. ) ;
#20589=CARTESIAN_POINT ( 'NONE',  ( 10.00000000000000000, 71.33759994381962599, 58.88447872959010709 ) ) ;
#20590=ORIENTED_EDGE ( 'NONE', *, *, #1044, .T. ) ;
#20591=ORIENTED_EDGE ( 'NONE', *, *, #2100, .T. ) ;
#20592=DIRECTION ( 'NONE',  ( 0.000000000000000000, 0.6427876096865353661, 0.7660444431189813441 ) ) ;
#20593=CARTESIAN_POINT ( 'NONE',  ( 10.00000000000000000, 21.31452625071037943, -82.34610137166097843 ) ) ;
#20596=CARTESIAN_POINT ( 'NONE',  ( -10.00000000000000000, 0.000000000000000000, 0.000000000000000000 ) ) ;
#20597=DIRECTION ( 'NONE',  ( -1.000000000000000000, 0.000000000000000000, 0.000000000000000000 ) ) ;
#20598=CARTESIAN_POINT ( 'NONE',  ( -10.00000000000000000, 0.000000000000000000, 0.000000000000000000 ) ) ;
#20600=CYLINDRICAL_SURFACE ( 'NONE', #16703, 44.99999999999998579 ) ;
#20602=AXIS2_PLACEMENT_3D ( 'NONE', #13195, #21505, #16297 ) ;
#20603=ORIENTED_EDGE ( 'NONE', *, *, #10407, .T. ) ;
#20604=DIRECTION ( 'NONE',  ( 1.000000000000000000, 0.000000000000000000, 0.000000000000000000 ) ) ;
#20605=AXIS2_PLACEMENT_3D ( 'NONE', #12740, #12311, #7452 ) ;
#20606=ORIENTED_EDGE ( 'NONE', *, *, #17310, .F. ) ;
#20608=CARTESIAN_POINT ( 'NONE',  ( 10.00000000000000000, -83.35585896458628952, 16.94078559807922346 ) ) ;
#20609=ORIENTED_EDGE ( 'NONE', *, *, #18382, .F. ) ;
#20612=ORIENTED_EDGE ( 'NONE', *, *, #13888, .F. ) ;
#20613=CIRCLE ( 'NONE', #11087, 44.99999999999999289 ) ;
#20615=ORIENTED_EDGE ( 'NONE', *, *, #16079, .F. ) ;
#20618=VERTEX_POINT ( 'NONE', #14659 ) ;
#20619=AXIS2_PLACEMENT_3D ( 'NONE', #1060, #11433, #12872 ) ;
#20620=DIRECTION ( 'NONE',  ( -1.000000000000000000, 0.000000000000000000, 0.000000000000000000 ) ) ;
#20621=CARTESIAN_POINT ( 'NONE',  ( 10.00000000000000000, 0.000000000000000000, 0.000000000000000000 ) ) ;
#20624=DIRECTION ( 'NONE',  ( -1.000000000000000000, -0.000000000000000000, -0.000000000000000000 ) ) ;
#20626=DIRECTION ( 'NONE',  ( 0.000000000000000000, -0.2079116908177664480, 0.9781476007338041345 ) ) ;
#20628=ORIENTED_EDGE ( 'NONE', *, *, #21258, .F. ) ;
#20629=EDGE_CURVE ( 'NONE', #9563, #8475, #20294, .T. ) ;
#20634=CARTESIAN_POINT ( 'NONE',  ( 10.00000000000000000, 66.01871308925549897, -64.79170103522952218 ) ) ;
#20635=AXIS2_PLACEMENT_3D ( 'NONE', #2684, #1138, #11190 ) ;
#20638=ORIENTED_EDGE ( 'NONE', *, *, #9277, .F. ) ;
#20639=FACE_OUTER_BOUND ( 'NONE', #11918, .T. ) ;
#20641=ORIENTED_EDGE ( 'NONE', *, *, #19845, .T. ) ;
#20643=ORIENTED_EDGE ( 'NONE', *, *, #7, .F. ) ;
#20644=CARTESIAN_POINT ( 'NONE',  ( 10.00000000000000000, 0.000000000000000000, 0.000000000000000000 ) ) ;
#20645=DIRECTION ( 'NONE',  ( 1.000000000000000000, 0.000000000000000000, 0.000000000000000000 ) ) ;
#20646=DIRECTION ( 'NONE',  ( 0.000000000000000000, 0.2079116908177599810, -0.9781476007338055778 ) ) ;
#20648=AXIS2_PLACEMENT_3D ( 'NONE', #9779, #9897, #18082 ) ;
#20651=CIRCLE ( 'NONE', #15715, 92.50100000000000477 ) ;
#20654=DIRECTION ( 'NONE',  ( 0.000000000000000000, -0.1391731009600517821, -0.9902680687415721383 ) ) ;
#20655=CYLINDRICAL_SURFACE ( 'NONE', #15774, 44.99999999999999289 ) ;
#20656=CARTESIAN_POINT ( 'NONE',  ( 10.00000000000000000, 0.000000000000000000, 0.000000000000000000 ) ) ;
#20657=CARTESIAN_POINT ( 'NONE',  ( 10.00000000000000000, 89.12061559554334167, 24.77803214283572686 ) ) ;
#20660=ORIENTED_EDGE ( 'NONE', *, *, #18958, .F. ) ;
#20663=VERTEX_POINT ( 'NONE', #21613 ) ;
#20664=ORIENTED_EDGE ( 'NONE', *, *, #11483, .T. ) ;
#20665=CIRCLE ( 'NONE', #9699, 45.00000000000000711 ) ;
#20666=VECTOR ( 'NONE', #5469, 1000.000000000000000 ) ;
#20667=ORIENTED_EDGE ( 'NONE', *, *, #19188, .T. ) ;
#20669=CIRCLE ( 'NONE', #18907, 44.99999999999998579 ) ;
#20670=DIRECTION ( 'NONE',  ( 0.000000000000000000, 0.000000000000000000, 1.000000000000000000 ) ) ;
#20671=ORIENTED_EDGE ( 'NONE', *, *, #13204, .T. ) ;
#20672=ORIENTED_EDGE ( 'NONE', *, *, #15492, .F. ) ;
#20673=DIRECTION ( 'NONE',  ( 0.000000000000000000, -0.5877852522924632561, -0.8090169943749546677 ) ) ;
#20676=EDGE_CURVE ( 'NONE', #155, #15057, #16920, .T. ) ;
#20677=EDGE_CURVE ( 'NONE', #11211, #5130, #3511, .T. ) ;
#20678=DIRECTION ( 'NONE',  ( -1.000000000000000000, -0.000000000000000000, -0.000000000000000000 ) ) ;
#20684=AXIS2_PLACEMENT_3D ( 'NONE', #14136, #8620, #10605 ) ;
#20687=DIRECTION ( 'NONE',  ( 0.000000000000000000, 0.9848077530122085754, -0.1736481776669273613 ) ) ;
#20688=CARTESIAN_POINT ( 'NONE',  ( 0.000000000000000000, -52.96496548042809138, -66.55750800669412115 ) ) ;
#20692=ADVANCED_FACE ( 'NONE', ( #16975 ), #8572, .F. ) ;
#20694=ADVANCED_FACE ( 'NONE', ( #20406 ), #11998, .F. ) ;
#20695=CARTESIAN_POINT ( 'NONE',  ( 10.00000000000000000, 73.32282170386913833, -48.65967342042704757 ) ) ;
#20696=ORIENTED_EDGE ( 'NONE', *, *, #6219, .F. ) ;
#20697=CIRCLE ( 'NONE', #10473, 44.99999999999999289 ) ;
#20698=CARTESIAN_POINT ( 'NONE',  ( 10.00000000000000000, 0.000000000000000000, 0.000000000000000000 ) ) ;
#20700=AXIS2_PLACEMENT_3D ( 'NONE', #2877, #21441, #18132 ) ;
#20703=DIRECTION ( 'NONE',  ( 0.000000000000000000, 0.000000000000000000, 1.000000000000000000 ) ) ;
#20705=ORIENTED_EDGE ( 'NONE', *, *, #13020, .F. ) ;
#20707=CARTESIAN_POINT ( 'NONE',  ( 0.000000000000000000, -71.72924546249979016, 45.71766382684644725 ) ) ;
#20708=EDGE_CURVE ( 'NONE', #1355, #20086, #16220, .T. ) ;
#20712=DIRECTION ( 'NONE',  ( -1.000000000000000000, 0.000000000000000000, -0.000000000000000000 ) ) ;
#20714=CYLINDRICAL_SURFACE ( 'NONE', #8940, 88.00000000000000000 ) ;
#20715=DIRECTION ( 'NONE',  ( 0.000000000000000000, 0.000000000000000000, 1.000000000000000000 ) ) ;
#20716=CIRCLE ( 'NONE', #15058, 45.00000000000000000 ) ;
#20717=VERTEX_POINT ( 'NONE', #722 ) ;
#20719=CARTESIAN_POINT ( 'NONE',  ( 0.000000000000000000, -79.38136668499713267, -37.98155635597392887 ) ) ;
#20720=VERTEX_POINT ( 'NONE', #15747 ) ;
#20722=DIRECTION ( 'NONE',  ( 0.000000000000000000, 0.000000000000000000, 1.000000000000000000 ) ) ;
#20724=CARTESIAN_POINT ( 'NONE',  ( 10.00000000000000000, -24.89070495400676819, -84.40647372620527733 ) ) ;
#20726=ORIENTED_EDGE ( 'NONE', *, *, #14777, .F. ) ;
#20727=ADVANCED_FACE ( 'NONE', ( #5481 ), #20508, .F. ) ;
#20731=VERTEX_POINT ( 'NONE', #3705 ) ;
#20732=AXIS2_PLACEMENT_3D ( 'NONE', #392, #5587, #3815 ) ;
#20733=VERTEX_POINT ( 'NONE', #12098 ) ;
#20734=CYLINDRICAL_SURFACE ( 'NONE', #11076, 92.50100000000000477 ) ;
#20738=CARTESIAN_POINT ( 'NONE',  ( 0.000000000000000000, -88.70892494636754577, 26.21376805916555242 ) ) ;
#20740=CARTESIAN_POINT ( 'NONE',  ( 10.00000000000000000, -91.70173545986527586, 12.13370160540012499 ) ) ;
#20741=CYLINDRICAL_SURFACE ( 'NONE', #21271, 88.00000000000000000 ) ;
#20743=FACE_OUTER_BOUND ( 'NONE', #18473, .T. ) ;
#20745=AXIS2_PLACEMENT_3D ( 'NONE', #14383, #10626, #14497 ) ;
#20747=AXIS2_PLACEMENT_3D ( 'NONE', #3132, #9634, #20037 ) ;
#20749=DIRECTION ( 'NONE',  ( -1.000000000000000000, -0.000000000000000000, -0.000000000000000000 ) ) ;
#20752=VERTEX_POINT ( 'NONE', #20724 ) ;
#20754=ORIENTED_EDGE ( 'NONE', *, *, #5535, .T. ) ;
#20756=ORIENTED_EDGE ( 'NONE', *, *, #5684, .T. ) ;
#20760=CARTESIAN_POINT ( 'NONE',  ( 10.00000000000000000, 0.000000000000000000, 0.000000000000000000 ) ) ;
#20763=CIRCLE ( 'NONE', #15825, 92.50100000000000477 ) ;
#20764=CIRCLE ( 'NONE', #21128, 44.99999999999998579 ) ;
#20765=CIRCLE ( 'NONE', #8417, 92.50100000000000477 ) ;
#20767=CYLINDRICAL_SURFACE ( 'NONE', #13865, 92.50100000000000477 ) ;
#20768=DIRECTION ( 'NONE',  ( 0.000000000000000000, 0.9993908270190955401, 0.03489949670250440394 ) ) ;
#20769=CARTESIAN_POINT ( 'NONE',  ( 10.00000000000000000, 78.04699792498145428, 49.64978465107317618 ) ) ;
#20771=DIRECTION ( 'NONE',  ( -1.000000000000000000, -0.000000000000000000, 0.000000000000000000 ) ) ;
#20772=VERTEX_POINT ( 'NONE', #7359 ) ;
#20773=CARTESIAN_POINT ( 'NONE',  ( 5.000000000000002665, -29.47587714450981622, -82.91666097089152743 ) ) ;
#20774=ORIENTED_EDGE ( 'NONE', *, *, #16609, .T. ) ;
#20777=ORIENTED_EDGE ( 'NONE', *, *, #8828, .F. ) ;
#20778=AXIS2_PLACEMENT_3D ( 'NONE', #3524, #94, #1756 ) ;
#20779=ORIENTED_EDGE ( 'NONE', *, *, #7937, .T. ) ;
#20780=CYLINDRICAL_SURFACE ( 'NONE', #18026, 44.99999999999999289 ) ;
#20781=ORIENTED_EDGE ( 'NONE', *, *, #16943, .F. ) ;
#20782=ORIENTED_EDGE ( 'NONE', *, *, #16150, .F. ) ;
#20785=ORIENTED_EDGE ( 'NONE', *, *, #14980, .T. ) ;
#20786=CARTESIAN_POINT ( 'NONE',  ( -10.00000000000000000, 0.000000000000000000, 0.000000000000000000 ) ) ;
#20788=EDGE_CURVE ( 'NONE', #5152, #4275, #19388, .T. ) ;
#20789=AXIS2_PLACEMENT_3D ( 'NONE', #13778, #8583, #4128 ) ;
#20791=DIRECTION ( 'NONE',  ( -1.000000000000000000, -0.000000000000000000, -0.000000000000000000 ) ) ;
#20796=FACE_OUTER_BOUND ( 'NONE', #19047, .T. ) ;
#20798=CARTESIAN_POINT ( 'NONE',  ( 0.000000000000000000, 0.000000000000000000, 0.000000000000000000 ) ) ;
#20802=EDGE_CURVE ( 'NONE', #11838, #15174, #3161, .T. ) ;
#20804=AXIS2_PLACEMENT_3D ( 'NONE', #6118, #2804, #7661 ) ;
#20808=AXIS2_PLACEMENT_3D ( 'NONE', #13623, #13178, #11539 ) ;
#20809=DIRECTION ( 'NONE',  ( -1.000000000000000000, 0.000000000000000000, -0.000000000000000000 ) ) ;
#20810=CIRCLE ( 'NONE', #2462, 44.99999999999999289 ) ;
#20811=VERTEX_POINT ( 'NONE', #2484 ) ;
#20812=DIRECTION ( 'NONE',  ( 0.000000000000000000, -0.7880107536067275653, 0.6156614753256510753 ) ) ;
#20815=DIRECTION ( 'NONE',  ( 1.000000000000000000, 0.000000000000000000, 0.000000000000000000 ) ) ;
#20816=EDGE_CURVE ( 'NONE', #16786, #16161, #21161, .T. ) ;
#20817=CYLINDRICAL_SURFACE ( 'NONE', #10736, 88.00000000000000000 ) ;
#20818=CARTESIAN_POINT ( 'NONE',  ( 0.000000000000000000, 0.000000000000000000, 0.000000000000000000 ) ) ;
#20819=CARTESIAN_POINT ( 'NONE',  ( 10.00000000000000000, -73.32282170386815778, -48.65967342042856103 ) ) ;
#20820=DIRECTION ( 'NONE',  ( 1.000000000000000000, 0.000000000000000000, 0.000000000000000000 ) ) ;
#20822=EDGE_CURVE ( 'NONE', #8047, #20435, #5804, .T. ) ;
#20824=AXIS2_PLACEMENT_3D ( 'NONE', #7533, #16152, #11289 ) ;
#20826=CARTESIAN_POINT ( 'NONE',  ( 0.000000000000000000, 8.134922360107273320, -84.67002113262471141 ) ) ;
#20827=ORIENTED_EDGE ( 'NONE', *, *, #20581, .F. ) ;
#20832=DIRECTION ( 'NONE',  ( 1.000000000000000000, -0.000000000000000000, 0.000000000000000000 ) ) ;
#20834=ORIENTED_EDGE ( 'NONE', *, *, #16216, .F. ) ;
#20835=VERTEX_POINT ( 'NONE', #9640 ) ;
#20836=ORIENTED_EDGE ( 'NONE', *, *, #17859, .F. ) ;
#20837=ORIENTED_EDGE ( 'NONE', *, *, #18011, .F. ) ;
#20838=FACE_OUTER_BOUND ( 'NONE', #11951, .T. ) ;
#20839=DIRECTION ( 'NONE',  ( 0.000000000000000000, -0.7880107536067275653, 0.6156614753256510753 ) ) ;
#20845=EDGE_CURVE ( 'NONE', #9349, #5274, #19404, .T. ) ;
#20846=DIRECTION ( 'NONE',  ( 0.000000000000000000, -0.2079116908177664480, 0.9781476007338041345 ) ) ;
#20848=ADVANCED_FACE ( 'NONE', ( #19490 ), #4357, .F. ) ;
#20849=EDGE_LOOP ( 'NONE', ( #15336, #17626, #3167, #2558 ) ) ;
#20850=EDGE_CURVE ( 'NONE', #10454, #3353, #9869, .T. ) ;
#20856=ORIENTED_EDGE ( 'NONE', *, *, #14306, .T. ) ;
#20857=DIRECTION ( 'NONE',  ( -1.000000000000000000, -0.000000000000000000, 0.000000000000000000 ) ) ;
#20860=ORIENTED_EDGE ( 'NONE', *, *, #10313, .F. ) ;
#20862=ORIENTED_EDGE ( 'NONE', *, *, #10388, .F. ) ;
#20863=CARTESIAN_POINT ( 'NONE',  ( 10.00000000000000000, -25.56104204395249369, -81.12843256239690959 ) ) ;
#20865=DIRECTION ( 'NONE',  ( 0.000000000000000000, 0.9993908270190957621, -0.03489949670249752750 ) ) ;
#20868=CARTESIAN_POINT ( 'NONE',  ( 10.00000000000000000, 78.04699792498145428, 49.64978465107317618 ) ) ;
#20869=CARTESIAN_POINT ( 'NONE',  ( 5.000000000000000000, 85.54350296776112828, 20.64725405482881726 ) ) ;
#20873=EDGE_LOOP ( 'NONE', ( #15720, #5351, #7357, #20664 ) ) ;
#20874=CARTESIAN_POINT ( 'NONE',  ( 10.00000000000000000, -57.53593069156319473, -72.42963261301021305 ) ) ;
#20875=ORIENTED_EDGE ( 'NONE', *, *, #12559, .T. ) ;
#20877=VERTEX_POINT ( 'NONE', #4681 ) ;
#20878=ORIENTED_EDGE ( 'NONE', *, *, #395, .F. ) ;
#20881=ORIENTED_EDGE ( 'NONE', *, *, #864, .T. ) ;
#20884=LINE ( 'NONE', #1000, #20050 ) ;
#20886=CYLINDRICAL_SURFACE ( 'NONE', #7622, 88.00000000000000000 ) ;
#20888=CARTESIAN_POINT ( 'NONE',  ( 0.000000000000000000, -81.83745710415254848, -32.35167097270233683 ) ) ;
#20891=DIRECTION ( 'NONE',  ( -1.000000000000000000, -0.000000000000000000, -0.000000000000000000 ) ) ;
#20892=CYLINDRICAL_SURFACE ( 'NONE', #16444, 92.50100000000000477 ) ;
#20894=CARTESIAN_POINT ( 'NONE',  ( 10.00000000000000000, 10.41137886060107576, 91.91321010181850681 ) ) ;
#20895=CIRCLE ( 'NONE', #4668, 44.99999999999999289 ) ;
#20896=ORIENTED_EDGE ( 'NONE', *, *, #14819, .T. ) ;
#20900=CIRCLE ( 'NONE', #18782, 88.00000000000000000 ) ;
#20901=CIRCLE ( 'NONE', #7846, 44.99999999999998579 ) ;
#20904=ORIENTED_EDGE ( 'NONE', *, *, #440, .F. ) ;
#20909=ORIENTED_EDGE ( 'NONE', *, *, #13752, .T. ) ;
#20910=ORIENTED_EDGE ( 'NONE', *, *, #8646, .F. ) ;
#20913=AXIS2_PLACEMENT_3D ( 'NONE', #7082, #3863, #13809 ) ;
#20914=AXIS2_PLACEMENT_3D ( 'NONE', #6533, #15340, #13361 ) ;
#20915=LINE ( 'NONE', #3801, #14265 ) ;
#20917=EDGE_CURVE ( 'NONE', #5377, #15908, #12858, .T. ) ;
#20918=EDGE_CURVE ( 'NONE', #14957, #4858, #3178, .T. ) ;
#20919=CYLINDRICAL_SURFACE ( 'NONE', #8664, 44.99999999999999289 ) ;
#20920=DIRECTION ( 'NONE',  ( 0.000000000000000000, -0.5877852522924632561, -0.8090169943749545567 ) ) ;
#20921=AXIS2_PLACEMENT_3D ( 'NONE', #3794, #14066, #7116 ) ;
#20923=DIRECTION ( 'NONE',  ( 1.000000000000000000, 0.000000000000000000, 0.000000000000000000 ) ) ;
#20925=AXIS2_PLACEMENT_3D ( 'NONE', #12382, #17588, #9067 ) ;
#20926=ORIENTED_EDGE ( 'NONE', *, *, #16700, .T. ) ;
#20927=DIRECTION ( 'NONE',  ( 0.000000000000000000, 0.000000000000000000, 1.000000000000000000 ) ) ;
#20928=COLOUR_RGB ( '', 0.31764706, 0.68627451, 0.89019608) ;
#20929=ORIENTED_EDGE ( 'NONE', *, *, #21523, .T. ) ;
#20931=ADVANCED_FACE ( 'NONE', ( #19929 ), #16615, .F. ) ;
#20938=EDGE_CURVE ( 'NONE', #9562, #1096, #3239, .T. ) ;
#20939=CIRCLE ( 'NONE', #13173, 44.99999999999999289 ) ;
#20940=EDGE_LOOP ( 'NONE', ( #2886, #10665, #11813, #8713 ) ) ;
#20941=ORIENTED_EDGE ( 'NONE', *, *, #6624, .T. ) ;
#20942=ORIENTED_EDGE ( 'NONE', *, *, #15668, .T. ) ;
#20945=ORIENTED_EDGE ( 'NONE', *, *, #7306, .T. ) ;
#20946=CIRCLE ( 'NONE', #494, 88.00000000000000000 ) ;
#20948=LINE ( 'NONE', #2384, #15315 ) ;
#20949=DIRECTION ( 'NONE',  ( 1.000000000000000000, 0.000000000000000000, 0.000000000000000000 ) ) ;
#20952=DIRECTION ( 'NONE',  ( 1.000000000000000000, 0.000000000000000000, 0.000000000000000000 ) ) ;
#20953=DIRECTION ( 'NONE',  ( -1.000000000000000000, -0.000000000000000000, -0.000000000000000000 ) ) ;
#20955=ORIENTED_EDGE ( 'NONE', *, *, #18891, .T. ) ;
#20959=EDGE_CURVE ( 'NONE', #827, #19897, #9513, .T. ) ;
#20960=ORIENTED_EDGE ( 'NONE', *, *, #552, .F. ) ;
#20961=AXIS2_PLACEMENT_3D ( 'NONE', #13854, #20712, #5575 ) ;
#20964=LINE ( 'NONE', #19519, #3125 ) ;
#20967=VECTOR ( 'NONE', #10570, 1000.000000000000000 ) ;
#20968=ORIENTED_EDGE ( 'NONE', *, *, #4465, .T. ) ;
#20969=ORIENTED_EDGE ( 'NONE', *, *, #16182, .F. ) ;
#20970=FACE_OUTER_BOUND ( 'NONE', #17399, .T. ) ;
#20973=ORIENTED_EDGE ( 'NONE', *, *, #5270, .F. ) ;
#20975=CARTESIAN_POINT ( 'NONE',  ( 10.00000000000000000, 92.32475887865433606, -5.707354816229567973 ) ) ;
#20977=CARTESIAN_POINT ( 'NONE',  ( 10.00000000000000000, -83.03980459022491800, 18.42770452393216374 ) ) ;
#20978=AXIS2_PLACEMENT_3D ( 'NONE', #21361, #6356, #17947 ) ;
#20980=EDGE_CURVE ( 'NONE', #4497, #6588, #3882, .T. ) ;
#20981=DIRECTION ( 'NONE',  ( 0.000000000000000000, 0.7880107536067190166, 0.6156614753256620665 ) ) ;
#20983=LINE ( 'NONE', #4522, #876 ) ;
#20985=CARTESIAN_POINT ( 'NONE',  ( 10.00000000000000000, 85.54350296776112828, 20.64725405482881726 ) ) ;
#20986=CARTESIAN_POINT ( 'NONE',  ( -10.00000000000000000, 0.000000000000000000, 0.000000000000000000 ) ) ;
#20987=AXIS2_PLACEMENT_3D ( 'NONE', #7229, #7343, #17391 ) ;
#20989=DIRECTION ( 'NONE',  ( -1.000000000000000000, -0.000000000000000000, -0.000000000000000000 ) ) ;
#20990=ORIENTED_EDGE ( 'NONE', *, *, #17606, .F. ) ;
#20992=ORIENTED_EDGE ( 'NONE', *, *, #7981, .F. ) ;
#20993=CIRCLE ( 'NONE', #6890, 45.00000000000000000 ) ;
#20995=AXIS2_PLACEMENT_3D ( 'NONE', #5182, #3846, #7063 ) ;
#20996=CIRCLE ( 'NONE', #1256, 44.99999999999999289 ) ;
#20998=VERTEX_POINT ( 'NONE', #20262 ) ;
#20999=CIRCLE ( 'NONE', #14657, 44.99999999999998579 ) ;
#21000=CARTESIAN_POINT ( 'NONE',  ( 0.000000000000000000, 60.65655256511237781, 59.63197188857542841 ) ) ;
#21001=ORIENTED_EDGE ( 'NONE', *, *, #9706, .F. ) ;
#21002=DIRECTION ( 'NONE',  ( 1.000000000000000000, 0.000000000000000000, 0.000000000000000000 ) ) ;
#21007=CARTESIAN_POINT ( 'NONE',  ( 0.000000000000000000, 92.22057093985038989, -7.197311757039553726 ) ) ;
#21008=CIRCLE ( 'NONE', #3373, 45.00000000000000000 ) ;
#21009=FACE_OUTER_BOUND ( 'NONE', #21810, .T. ) ;
#21010=DIRECTION ( 'NONE',  ( -1.000000000000000000, -0.000000000000000000, -0.000000000000000000 ) ) ;
#21012=VERTEX_POINT ( 'NONE', #15061 ) ;
#21013=VECTOR ( 'NONE', #18497, 1000.000000000000000 ) ;
#21015=DIRECTION ( 'NONE',  ( 0.000000000000000000, -0.5299192642332118952, 0.8480480961564216269 ) ) ;
#21016=CIRCLE ( 'NONE', #14303, 88.00000000000000000 ) ;
#21021=ORIENTED_EDGE ( 'NONE', *, *, #17937, .F. ) ;
#21023=DIRECTION ( 'NONE',  ( 0.000000000000000000, 0.06975647374412546897, -0.9975640502598241977 ) ) ;
#21026=ORIENTED_EDGE ( 'NONE', *, *, #6069, .T. ) ;
#21027=CARTESIAN_POINT ( 'NONE',  ( 10.00000000000000000, 0.000000000000000000, 0.000000000000000000 ) ) ;
#21030=DIRECTION ( 'NONE',  ( -1.000000000000000000, -0.000000000000000000, -0.000000000000000000 ) ) ;
#21031=AXIS2_PLACEMENT_3D ( 'NONE', #7285, #12677, #14012 ) ;
#21032=DIRECTION ( 'NONE',  ( 0.000000000000000000, 0.000000000000000000, 1.000000000000000000 ) ) ;
#21034=DIRECTION ( 'NONE',  ( -1.000000000000000000, -0.000000000000000000, 0.000000000000000000 ) ) ;
#21035=DIRECTION ( 'NONE',  ( 0.000000000000000000, 0.000000000000000000, 1.000000000000000000 ) ) ;
#21037=DIRECTION ( 'NONE',  ( -1.000000000000000000, -0.000000000000000000, 0.000000000000000000 ) ) ;
#21039=ORIENTED_EDGE ( 'NONE', *, *, #4279, .F. ) ;
#21041=ORIENTED_EDGE ( 'NONE', *, *, #20234, .F. ) ;
#21042=CIRCLE ( 'NONE', #13277, 44.99999999999998579 ) ;
#21043=VECTOR ( 'NONE', #1549, 1000.000000000000000 ) ;
#21044=VECTOR ( 'NONE', #12115, 1000.000000000000000 ) ;
#21045=DIRECTION ( 'NONE',  ( -1.000000000000000000, -0.000000000000000000, -0.000000000000000000 ) ) ;
#21046=ORIENTED_EDGE ( 'NONE', *, *, #5738, .F. ) ;
#21047=ADVANCED_FACE ( 'NONE', ( #1806 ), #10084, .F. ) ;
#21049=ORIENTED_EDGE ( 'NONE', *, *, #2874, .T. ) ;
#21050=VERTEX_POINT ( 'NONE', #6462 ) ;
#21051=ORIENTED_EDGE ( 'NONE', *, *, #15248, .T. ) ;
#21052=VERTEX_POINT ( 'NONE', #3465 ) ;
#21054=CARTESIAN_POINT ( 'NONE',  ( 5.000000000000002665, -23.62010150527279961, 84.77081340225898032 ) ) ;
#21055=EDGE_CURVE ( 'NONE', #10855, #21383, #2460, .T. ) ;
#21056=ORIENTED_EDGE ( 'NONE', *, *, #14465, .F. ) ;
#21057=CIRCLE ( 'NONE', #12937, 88.00000000000000000 ) ;
#21058=DIRECTION ( 'NONE',  ( -1.000000000000000000, 0.000000000000000000, -0.000000000000000000 ) ) ;
#21059=DIRECTION ( 'NONE',  ( 0.000000000000000000, 0.6946583704589934793, 0.7193398003386547446 ) ) ;
#21060=CIRCLE ( 'NONE', #6599, 44.99999999999999289 ) ;
#21061=DIRECTION ( 'NONE',  ( 0.000000000000000000, 1.603655480014115143E-14, -1.000000000000000000 ) ) ;
#21063=VECTOR ( 'NONE', #3752, 1000.000000000000000 ) ;
#21064=CARTESIAN_POINT ( 'NONE',  ( 0.000000000000000000, 30.71797041605924505, -82.46457599186518905 ) ) ;
#21065=EDGE_CURVE ( 'NONE', #21597, #7542, #7407, .T. ) ;
#21066=ORIENTED_EDGE ( 'NONE', *, *, #6776, .F. ) ;
#21067=CARTESIAN_POINT ( 'NONE',  ( 10.00000000000000000, 76.53853822674039975, -43.42639941457040464 ) ) ;
#21069=CARTESIAN_POINT ( 'NONE',  ( 10.00000000000000000, 43.18649929580192293, 73.28107340219430910 ) ) ;
#21071=AXIS2_PLACEMENT_3D ( 'NONE', #8933, #10702, #11027 ) ;
#21077=EDGE_LOOP ( 'NONE', ( #7975, #4253, #20878, #19755 ) ) ;
#21078=CARTESIAN_POINT ( 'NONE',  ( 0.000000000000000000, 0.000000000000000000, 0.000000000000000000 ) ) ;
#21079=AXIS2_PLACEMENT_3D ( 'NONE', #6515, #16328, #1196 ) ;
#21085=ORIENTED_EDGE ( 'NONE', *, *, #16640, .T. ) ;
#21086=DIRECTION ( 'NONE',  ( -1.000000000000000000, -0.000000000000000000, -0.000000000000000000 ) ) ;
#21087=DIRECTION ( 'NONE',  ( -1.000000000000000000, -0.000000000000000000, -0.000000000000000000 ) ) ;
#21090=EDGE_CURVE ( 'NONE', #4970, #18142, #20122, .T. ) ;
#21093=AXIS2_PLACEMENT_3D ( 'NONE', #8991, #2697, #720 ) ;
#21094=DIRECTION ( 'NONE',  ( -1.000000000000000000, -0.000000000000000000, -0.000000000000000000 ) ) ;
#21095=DIRECTION ( 'NONE',  ( 1.000000000000000000, 0.000000000000000000, 0.000000000000000000 ) ) ;
#21097=CARTESIAN_POINT ( 'NONE',  ( 10.00000000000000000, -71.72924546249979016, 45.71766382684644725 ) ) ;
#21098=ADVANCED_FACE ( 'NONE', ( #7006 ), #2345, .F. ) ;
#21099=CARTESIAN_POINT ( 'NONE',  ( 10.00000000000000000, 19.83954325428658194, 82.71385593638699163 ) ) ;
#21100=ADVANCED_FACE ( 'NONE', ( #5344 ), #3573, .F. ) ;
#21101=DIRECTION ( 'NONE',  ( 0.000000000000000000, 0.000000000000000000, 1.000000000000000000 ) ) ;
#21104=ORIENTED_EDGE ( 'NONE', *, *, #1864, .F. ) ;
#21107=EDGE_CURVE ( 'NONE', #8068, #1586, #2815, .T. ) ;
#21108=ORIENTED_EDGE ( 'NONE', *, *, #16726, .F. ) ;
#21109=CIRCLE ( 'NONE', #11586, 92.50099999999999056 ) ;
#21110=ORIENTED_EDGE ( 'NONE', *, *, #3290, .T. ) ;
#21111=CARTESIAN_POINT ( 'NONE',  ( 10.00000000000000000, 2.208823992045340301, -85.03123271466934341 ) ) ;
#21113=DIRECTION ( 'NONE',  ( -1.000000000000000000, 0.000000000000000000, 0.000000000000000000 ) ) ;
#21114=CARTESIAN_POINT ( 'NONE',  ( 10.00000000000000000, 0.000000000000000000, 0.000000000000000000 ) ) ;
#21116=EDGE_CURVE ( 'NONE', #16361, #10612, #5640, .T. ) ;
#21117=CARTESIAN_POINT ( 'NONE',  ( 0.000000000000000000, 35.34277389771654043, -85.48288328206348297 ) ) ;
#21119=DIRECTION ( 'NONE',  ( 0.000000000000000000, 0.000000000000000000, -1.000000000000000000 ) ) ;
#21120=EDGE_CURVE ( 'NONE', #4745, #12130, #6363, .T. ) ;
#21121=CARTESIAN_POINT ( 'NONE',  ( 5.000000000000002665, 17.64925110578583300, -86.21197095186326464 ) ) ;
#21124=VECTOR ( 'NONE', #15127, 1000.000000000000000 ) ;
#21126=AXIS2_PLACEMENT_3D ( 'NONE', #7848, #7962, #14587 ) ;
#21127=EDGE_CURVE ( 'NONE', #21050, #15057, #10411, .T. ) ;
#21128=AXIS2_PLACEMENT_3D ( 'NONE', #4887, #9514, #11628 ) ;
#21129=AXIS2_PLACEMENT_3D ( 'NONE', #7351, #15738, #16968 ) ;
#21131=VECTOR ( 'NONE', #12714, 1000.000000000000000 ) ;
#21133=DIRECTION ( 'NONE',  ( 0.000000000000000000, 0.000000000000000000, 1.000000000000000000 ) ) ;
#21134=CARTESIAN_POINT ( 'NONE',  ( 5.000000000000002665, 76.53853822674039975, -43.42639941457040464 ) ) ;
#21135=LINE ( 'NONE', #2458, #7085 ) ;
#21136=ORIENTED_EDGE ( 'NONE', *, *, #5142, .T. ) ;
#21137=AXIS2_PLACEMENT_3D ( 'NONE', #17865, #17650, #12877 ) ;
#21138=DIRECTION ( 'NONE',  ( 0.000000000000000000, -0.4694715627858797591, -0.8829475928589327616 ) ) ;
#21139=ORIENTED_EDGE ( 'NONE', *, *, #6495, .T. ) ;
#21140=EDGE_LOOP ( 'NONE', ( #21428, #13932, #6582, #3698 ) ) ;
#21143=CARTESIAN_POINT ( 'NONE',  ( 5.000000000000002665, 83.89484365856945658, -26.56417150042864961 ) ) ;
#21144=ORIENTED_EDGE ( 'NONE', *, *, #4737, .T. ) ;
#21148=CIRCLE ( 'NONE', #5265, 44.99999999999999289 ) ;
#21152=DIRECTION ( 'NONE',  ( 1.000000000000000000, 0.000000000000000000, 0.000000000000000000 ) ) ;
#21153=CARTESIAN_POINT ( 'NONE',  ( 0.000000000000000000, 85.22372865846323009, -21.92979875759543162 ) ) ;
#21154=CARTESIAN_POINT ( 'NONE',  ( 0.000000000000000000, 0.000000000000000000, 0.000000000000000000 ) ) ;
#21155=CARTESIAN_POINT ( 'NONE',  ( 10.00000000000000000, 0.000000000000000000, 0.000000000000000000 ) ) ;
#21157=ORIENTED_EDGE ( 'NONE', *, *, #3392, .T. ) ;
#21158=CARTESIAN_POINT ( 'NONE',  ( 10.00000000000000000, 56.35896156214949571, 73.34918167666329225 ) ) ;
#21161=CIRCLE ( 'NONE', #18349, 88.00000000000000000 ) ;
#21162=DIRECTION ( 'NONE',  ( -1.000000000000000000, 0.000000000000000000, 0.000000000000000000 ) ) ;
#21164=CARTESIAN_POINT ( 'NONE',  ( 10.00000000000000000, -57.06999622551760609, -66.98518889142141575 ) ) ;
#21167=ORIENTED_EDGE ( 'NONE', *, *, #4317, .T. ) ;
#21168=VERTEX_POINT ( 'NONE', #7112 ) ;
#21173=CARTESIAN_POINT ( 'NONE',  ( 0.000000000000000000, -73.32282170386815778, -48.65967342042856103 ) ) ;
#21174=DIRECTION ( 'NONE',  ( 0.000000000000000000, 0.4067366430757946572, 0.9135454576426033091 ) ) ;
#21177=CARTESIAN_POINT ( 'NONE',  ( 10.00000000000000000, 17.64925110578469258, 86.21197095186350623 ) ) ;
#21181=CARTESIAN_POINT ( 'NONE',  ( 10.00000000000000000, 0.000000000000000000, 0.000000000000000000 ) ) ;
#21184=ORIENTED_EDGE ( 'NONE', *, *, #6106, .T. ) ;
#21185=CARTESIAN_POINT ( 'NONE',  ( 10.00000000000000000, -11.59241532900569993, -87.23311244498751194 ) ) ;
#21188=DIRECTION ( 'NONE',  ( 0.000000000000000000, 0.000000000000000000, 1.000000000000000000 ) ) ;
#21191=ORIENTED_EDGE ( 'NONE', *, *, #9993, .F. ) ;
#21192=VERTEX_POINT ( 'NONE', #20695 ) ;
#21196=DIRECTION ( 'NONE',  ( 1.000000000000000000, 0.000000000000000000, 0.000000000000000000 ) ) ;
#21197=CARTESIAN_POINT ( 'NONE',  ( 10.00000000000000000, -3.974475837765555575, 92.41557521768190497 ) ) ;
#21198=DIRECTION ( 'NONE',  ( 1.000000000000000000, -0.000000000000000000, -0.000000000000000000 ) ) ;
#21199=EDGE_CURVE ( 'NONE', #14906, #6904, #368, .T. ) ;
#21201=EDGE_CURVE ( 'NONE', #13715, #17704, #2830, .T. ) ;
#21202=CARTESIAN_POINT ( 'NONE',  ( 10.00000000000000000, -78.01214607583776228, 33.90124636420084414 ) ) ;
#21205=DIRECTION ( 'NONE',  ( -1.000000000000000000, -0.000000000000000000, -0.000000000000000000 ) ) ;
#21206=DIRECTION ( 'NONE',  ( 0.000000000000000000, 0.7431448254773953543, -0.6691306063588569053 ) ) ;
#21209=ORIENTED_EDGE ( 'NONE', *, *, #14901, .F. ) ;
#21210=ORIENTED_EDGE ( 'NONE', *, *, #6689, .T. ) ;
#21212=EDGE_CURVE ( 'NONE', #11183, #5893, #6742, .T. ) ;
#21213=ORIENTED_EDGE ( 'NONE', *, *, #9581, .F. ) ;
#21214=VECTOR ( 'NONE', #3388, 1000.000000000000000 ) ;
#21216=ADVANCED_FACE ( 'NONE', ( #14266 ), #6107, .F. ) ;
#21217=CARTESIAN_POINT ( 'NONE',  ( 10.00000000000000000, 0.000000000000000000, 0.000000000000000000 ) ) ;
#21219=CARTESIAN_POINT ( 'NONE',  ( 0.000000000000000000, 41.21966518006070146, -82.80926399530243032 ) ) ;
#21221=DIRECTION ( 'NONE',  ( 0.000000000000000000, -0.8987940462991619306, -0.4383711467890878399 ) ) ;
#21223=DIRECTION ( 'NONE',  ( -1.000000000000000000, -0.000000000000000000, 0.000000000000000000 ) ) ;
#21225=EDGE_CURVE ( 'NONE', #13181, #19466, #13053, .T. ) ;
#21226=DIRECTION ( 'NONE',  ( 1.000000000000000000, 0.000000000000000000, 0.000000000000000000 ) ) ;
#21229=EDGE_CURVE ( 'NONE', #17490, #8447, #17658, .T. ) ;
#21231=VERTEX_POINT ( 'NONE', #17928 ) ;
#21235=ADVANCED_FACE ( 'NONE', ( #9283 ), #7648, .F. ) ;
#21238=CYLINDRICAL_SURFACE ( 'NONE', #3363, 44.99999999999999289 ) ;
#21240=EDGE_CURVE ( 'NONE', #19614, #16153, #8480, .T. ) ;
#21241=ORIENTED_EDGE ( 'NONE', *, *, #10681, .F. ) ;
#21243=DIRECTION ( 'NONE',  ( 0.000000000000000000, 0.2756373558169998295, -0.9612616959383187831 ) ) ;
#21244=VERTEX_POINT ( 'NONE', #4117 ) ;
#21245=ORIENTED_EDGE ( 'NONE', *, *, #14866, .T. ) ;
#21246=EDGE_CURVE ( 'NONE', #3976, #15380, #21135, .T. ) ;
#21248=CARTESIAN_POINT ( 'NONE',  ( 5.000000000000002665, 81.83745710415318797, -32.35167097270070258 ) ) ;
#21249=EDGE_CURVE ( 'NONE', #9563, #12067, #11666, .T. ) ;
#21250=DIRECTION ( 'NONE',  ( -1.000000000000000000, 0.000000000000000000, 0.000000000000000000 ) ) ;
#21252=DIRECTION ( 'NONE',  ( -1.000000000000000000, -0.000000000000000000, -0.000000000000000000 ) ) ;
#21253=DIRECTION ( 'NONE',  ( -1.000000000000000000, -0.000000000000000000, -0.000000000000000000 ) ) ;
#21255=DIRECTION ( 'NONE',  ( 0.000000000000000000, 0.8290375725550390706, 0.5591929034707507906 ) ) ;
#21256=CARTESIAN_POINT ( 'NONE',  ( 10.00000000000000000, 0.000000000000000000, 0.000000000000000000 ) ) ;
#21258=EDGE_CURVE ( 'NONE', #6908, #2135, #1775, .T. ) ;
#21259=ORIENTED_EDGE ( 'NONE', *, *, #10802, .T. ) ;
#21260=CYLINDRICAL_SURFACE ( 'NONE', #18168, 88.00000000000000000 ) ;
#21261=ORIENTED_EDGE ( 'NONE', *, *, #641, .T. ) ;
#21262=DIRECTION ( 'NONE',  ( 0.000000000000000000, 0.000000000000000000, 1.000000000000000000 ) ) ;
#21264=CARTESIAN_POINT ( 'NONE',  ( 0.000000000000000000, 57.53593069156372053, 72.42963261300981515 ) ) ;
#21265=ORIENTED_EDGE ( 'NONE', *, *, #14464, .F. ) ;
#21266=ORIENTED_EDGE ( 'NONE', *, *, #555, .T. ) ;
#21267=EDGE_LOOP ( 'NONE', ( #6189, #7068, #5647, #17200 ) ) ;
#21268=ORIENTED_EDGE ( 'NONE', *, *, #12665, .T. ) ;
#21270=DIRECTION ( 'NONE',  ( 1.000000000000000000, 0.000000000000000000, 0.000000000000000000 ) ) ;
#21271=AXIS2_PLACEMENT_3D ( 'NONE', #5387, #8706, #12016 ) ;
#21274=AXIS2_PLACEMENT_3D ( 'NONE', #573, #7321, #19127 ) ;
#21276=CARTESIAN_POINT ( 'NONE',  ( 0.000000000000000000, 83.89484365856912973, 26.56417150042976161 ) ) ;
#21277=CARTESIAN_POINT ( 'NONE',  ( 10.00000000000000000, -36.39558101400082535, -80.12091913260421450 ) ) ;
#21278=CARTESIAN_POINT ( 'NONE',  ( 0.000000000000000000, 84.79630770241084292, -6.691460262315676033 ) ) ;
#21279=DIRECTION ( 'NONE',  ( -1.000000000000000000, 0.000000000000000000, 0.000000000000000000 ) ) ;
#21280=ORIENTED_EDGE ( 'NONE', *, *, #13948, .T. ) ;
#21281=CARTESIAN_POINT ( 'NONE',  ( 10.00000000000000000, 39.87723064937119233, 83.46401306393586594 ) ) ;
#21285=ORIENTED_EDGE ( 'NONE', *, *, #18023, .F. ) ;
#21286=CARTESIAN_POINT ( 'NONE',  ( 10.00000000000000000, -74.74361964203257003, 40.60271866773520344 ) ) ;
#21288=CARTESIAN_POINT ( 'NONE',  ( 10.00000000000000000, 75.45728100697598961, 39.26051685139091063 ) ) ;
#21290=CARTESIAN_POINT ( 'NONE',  ( 10.00000000000000000, -69.74988376403980794, -53.65588238863407611 ) ) ;
#21291=AXIS2_PLACEMENT_3D ( 'NONE', #16112, #15994, #7725 ) ;
#21292=ORIENTED_EDGE ( 'NONE', *, *, #19340, .T. ) ;
#21293=ADVANCED_FACE ( 'NONE', ( #16365 ), #901, .F. ) ;
#21294=VERTEX_POINT ( 'NONE', #21340 ) ;
#21296=ORIENTED_EDGE ( 'NONE', *, *, #16609, .F. ) ;
#21299=DIRECTION ( 'NONE',  ( 0.000000000000000000, 0.000000000000000000, 1.000000000000000000 ) ) ;
#21301=CARTESIAN_POINT ( 'NONE',  ( 10.00000000000000000, 0.000000000000000000, 0.000000000000000000 ) ) ;
#21302=EDGE_CURVE ( 'NONE', #18196, #13383, #10601, .T. ) ;
#21303=VECTOR ( 'NONE', #13873, 1000.000000000000000 ) ;
#21306=DIRECTION ( 'NONE',  ( -1.000000000000000000, -0.000000000000000000, 0.000000000000000000 ) ) ;
#21307=CYLINDRICAL_SURFACE ( 'NONE', #12319, 88.00000000000000000 ) ;
#21308=CIRCLE ( 'NONE', #21653, 92.50100000000000477 ) ;
#21312=ORIENTED_EDGE ( 'NONE', *, *, #782, .F. ) ;
#21314=ORIENTED_EDGE ( 'NONE', *, *, #13110, .F. ) ;
#21318=DIRECTION ( 'NONE',  ( -1.000000000000000000, -0.000000000000000000, 0.000000000000000000 ) ) ;
#21319=CIRCLE ( 'NONE', #2965, 92.50100000000000477 ) ;
#21320=ORIENTED_EDGE ( 'NONE', *, *, #20032, .T. ) ;
#21322=CARTESIAN_POINT ( 'NONE',  ( 10.00000000000000000, 84.12297548659721258, 32.40974838672968872 ) ) ;
#21323=CYLINDRICAL_SURFACE ( 'NONE', #1969, 44.99999999999998579 ) ;
#21324=CARTESIAN_POINT ( 'NONE',  ( 0.000000000000000000, -14.02138820414970688, 83.89630571862279851 ) ) ;
#21328=DIRECTION ( 'NONE',  ( -1.000000000000000000, -0.000000000000000000, -0.000000000000000000 ) ) ;
#21329=EDGE_CURVE ( 'NONE', #11211, #9563, #20135, .T. ) ;
#21331=VERTEX_POINT ( 'NONE', #17702 ) ;
#21333=CARTESIAN_POINT ( 'NONE',  ( -10.00000000000000000, 0.000000000000000000, 0.000000000000000000 ) ) ;
#21334=CIRCLE ( 'NONE', #14262, 45.00000000000000711 ) ;
#21338=DIRECTION ( 'NONE',  ( 0.000000000000000000, 0.000000000000000000, 1.000000000000000000 ) ) ;
#21339=CIRCLE ( 'NONE', #8999, 88.00000000000000000 ) ;
#21340=CARTESIAN_POINT ( 'NONE',  ( 10.00000000000000000, -87.92084725184950855, 3.731570516142653116 ) ) ;
#21342=EDGE_LOOP ( 'NONE', ( #6037, #11897, #21167, #20397 ) ) ;
#21344=EDGE_CURVE ( 'NONE', #5130, #3522, #18373, .T. ) ;
#21346=ORIENTED_EDGE ( 'NONE', *, *, #18790, .F. ) ;
#21347=EDGE_LOOP ( 'NONE', ( #15624, #17929, #8885, #7956 ) ) ;
#21353=VERTEX_POINT ( 'NONE', #1349 ) ;
#21356=FACE_OUTER_BOUND ( 'NONE', #6990, .T. ) ;
#21357=DIRECTION ( 'NONE',  ( -1.000000000000000000, -0.000000000000000000, -0.000000000000000000 ) ) ;
#21358=AXIS2_PLACEMENT_3D ( 'NONE', #16641, #13099, #3166 ) ;
#21359=CARTESIAN_POINT ( 'NONE',  ( 10.00000000000000000, 0.000000000000000000, 0.000000000000000000 ) ) ;
#21360=AXIS2_PLACEMENT_3D ( 'NONE', #7008, #8546, #5346 ) ;
#21361=CARTESIAN_POINT ( 'NONE',  ( 10.00000000000000000, 0.000000000000000000, 0.000000000000000000 ) ) ;
#21363=CARTESIAN_POINT ( 'NONE',  ( 10.00000000000000000, 0.000000000000000000, 0.000000000000000000 ) ) ;
#21364=CARTESIAN_POINT ( 'NONE',  ( 0.000000000000000000, -35.18804927320584142, 80.65854690202667143 ) ) ;
#21366=CYLINDRICAL_SURFACE ( 'NONE', #18972, 44.99999999999999289 ) ;
#21368=ORIENTED_EDGE ( 'NONE', *, *, #13768, .T. ) ;
#21370=FACE_OUTER_BOUND ( 'NONE', #495, .T. ) ;
#21371=ORIENTED_EDGE ( 'NONE', *, *, #19605, .F. ) ;
#21372=VECTOR ( 'NONE', #12980, 1000.000000000000000 ) ;
#21374=VECTOR ( 'NONE', #10401, 1000.000000000000000 ) ;
#21378=CARTESIAN_POINT ( 'NONE',  ( 0.000000000000000000, 0.000000000000000000, 0.000000000000000000 ) ) ;
#21379=CIRCLE ( 'NONE', #11850, 44.99999999999999289 ) ;
#21382=AXIS2_PLACEMENT_3D ( 'NONE', #5998, #19453, #14489 ) ;
#21383=VERTEX_POINT ( 'NONE', #20130 ) ;
#21384=ADVANCED_FACE ( 'NONE', ( #8521 ), #21667, .F. ) ;
#21385=ORIENTED_EDGE ( 'NONE', *, *, #7436, .F. ) ;
#21387=CARTESIAN_POINT ( 'NONE',  ( 10.00000000000000000, -23.62010150527165919, -84.77081340225927875 ) ) ;
#21388=DIRECTION ( 'NONE',  ( 0.000000000000000000, -6.982962677686266711E-15, 1.000000000000000000 ) ) ;
#21389=ORIENTED_EDGE ( 'NONE', *, *, #14017, .F. ) ;
#21391=DIRECTION ( 'NONE',  ( 1.000000000000000000, 0.000000000000000000, 0.000000000000000000 ) ) ;
#21392=DIRECTION ( 'NONE',  ( 0.000000000000000000, 0.000000000000000000, 1.000000000000000000 ) ) ;
#21393=DIRECTION ( 'NONE',  ( -1.000000000000000000, -0.000000000000000000, -0.000000000000000000 ) ) ;
#21398=CARTESIAN_POINT ( 'NONE',  ( 10.00000000000000000, 0.000000000000000000, 0.000000000000000000 ) ) ;
#21399=DIRECTION ( 'NONE',  ( 1.000000000000000000, 0.000000000000000000, 0.000000000000000000 ) ) ;
#21400=EDGE_LOOP ( 'NONE', ( #17205, #10013, #14247, #18079 ) ) ;
#21401=EDGE_CURVE ( 'NONE', #16630, #3522, #7420, .T. ) ;
#21402=CYLINDRICAL_SURFACE ( 'NONE', #16134, 44.99999999999999289 ) ;
#21403=ORIENTED_EDGE ( 'NONE', *, *, #7705, .F. ) ;
#21404=DIRECTION ( 'NONE',  ( 1.000000000000000000, 0.000000000000000000, 0.000000000000000000 ) ) ;
#21405=DIRECTION ( 'NONE',  ( 0.000000000000000000, 0.000000000000000000, 1.000000000000000000 ) ) ;
#21406=VERTEX_POINT ( 'NONE', #4659 ) ;
#21409=AXIS2_PLACEMENT_3D ( 'NONE', #2143, #8876, #20278 ) ;
#21410=VERTEX_POINT ( 'NONE', #8192 ) ;
#21416=CARTESIAN_POINT ( 'NONE',  ( 10.00000000000000000, 0.000000000000000000, 0.000000000000000000 ) ) ;
#21417=LINE ( 'NONE', #13021, #6631 ) ;
#21418=CARTESIAN_POINT ( 'NONE',  ( 10.00000000000000000, 0.000000000000000000, 0.000000000000000000 ) ) ;
#21419=DIRECTION ( 'NONE',  ( 0.000000000000000000, 0.5299192642332061221, -0.8480480961564251796 ) ) ;
#21421=CIRCLE ( 'NONE', #14709, 44.99999999999999289 ) ;
#21423=AXIS2_PLACEMENT_3D ( 'NONE', #634, #7065, #7385 ) ;
#21424=AXIS2_PLACEMENT_3D ( 'NONE', #7294, #14020, #20768 ) ;
#21426=ORIENTED_EDGE ( 'NONE', *, *, #10707, .T. ) ;
#21427=ORIENTED_EDGE ( 'NONE', *, *, #8300, .F. ) ;
#21428=ORIENTED_EDGE ( 'NONE', *, *, #549, .F. ) ;
#21431=DIRECTION ( 'NONE',  ( -1.000000000000000000, -0.000000000000000000, -0.000000000000000000 ) ) ;
#21432=AXIS2_PLACEMENT_3D ( 'NONE', #3078, #19867, #14564 ) ;
#21433=ORIENTED_EDGE ( 'NONE', *, *, #11162, .T. ) ;
#21434=DIRECTION ( 'NONE',  ( 0.000000000000000000, 0.06975647374411846069, 0.9975640502598246417 ) ) ;
#21437=CARTESIAN_POINT ( 'NONE',  ( 10.00000000000000000, -3.728035544475628793, -84.97818067823773447 ) ) ;
#21439=DIRECTION ( 'NONE',  ( 0.000000000000000000, 0.000000000000000000, 1.000000000000000000 ) ) ;
#21440=CARTESIAN_POINT ( 'NONE',  ( 10.00000000000000000, 72.58367602204255320, -49.75550195834793499 ) ) ;
#21441=DIRECTION ( 'NONE',  ( -1.000000000000000000, 0.000000000000000000, 0.000000000000000000 ) ) ;
#21442=DIRECTION ( 'NONE',  ( 0.000000000000000000, 0.000000000000000000, 1.000000000000000000 ) ) ;
#21444=EDGE_CURVE ( 'NONE', #15380, #4970, #6382, .T. ) ;
#21445=ORIENTED_EDGE ( 'NONE', *, *, #21229, .F. ) ;
#21446=FACE_OUTER_BOUND ( 'NONE', #1187, .T. ) ;
#21449=AXIS2_PLACEMENT_3D ( 'NONE', #19137, #12291, #3895 ) ;
#21451=ORIENTED_EDGE ( 'NONE', *, *, #15301, .T. ) ;
#21453=ADVANCED_FACE ( 'NONE', ( #11394 ), #16479, .F. ) ;
#21454=ORIENTED_EDGE ( 'NONE', *, *, #12198, .F. ) ;
#21455=DIRECTION ( 'NONE',  ( -1.000000000000000000, 0.000000000000000000, -0.000000000000000000 ) ) ;
#21456=DIRECTION ( 'NONE',  ( -1.000000000000000000, -0.000000000000000000, -0.000000000000000000 ) ) ;
#21457=ORIENTED_EDGE ( 'NONE', *, *, #9178, .F. ) ;
#21458=CARTESIAN_POINT ( 'NONE',  ( 5.000000000000002665, -0.6609040254605889064, -87.99751818016876825 ) ) ;
#21462=CIRCLE ( 'NONE', #14762, 88.00000000000000000 ) ;
#21464=CARTESIAN_POINT ( 'NONE',  ( 0.000000000000000000, -78.80192417387900150, -39.16958956249377621 ) ) ;
#21465=ORIENTED_EDGE ( 'NONE', *, *, #13948, .F. ) ;
#21466=ORIENTED_EDGE ( 'NONE', *, *, #12945, .T. ) ;
#21468=DIRECTION ( 'NONE',  ( 1.000000000000000000, 0.000000000000000000, -0.000000000000000000 ) ) ;
#21470=CARTESIAN_POINT ( 'NONE',  ( 10.00000000000000000, 0.000000000000000000, 0.000000000000000000 ) ) ;
#21471=CARTESIAN_POINT ( 'NONE',  ( 10.00000000000000000, -56.35896156214997887, 73.34918167666290856 ) ) ;
#21473=DIRECTION ( 'NONE',  ( 0.000000000000000000, 0.000000000000000000, 1.000000000000000000 ) ) ;
#21474=AXIS2_PLACEMENT_3D ( 'NONE', #14603, #1562, #16485 ) ;
#21475=DIRECTION ( 'NONE',  ( -1.000000000000000000, -0.000000000000000000, 0.000000000000000000 ) ) ;
#21476=CIRCLE ( 'NONE', #7363, 92.50100000000000477 ) ;
#21477=CYLINDRICAL_SURFACE ( 'NONE', #7539, 92.50100000000000477 ) ;
#21478=DIRECTION ( 'NONE',  ( 0.000000000000000000, 0.000000000000000000, 1.000000000000000000 ) ) ;
#21479=LINE ( 'NONE', #13071, #6646 ) ;
#21481=EDGE_CURVE ( 'NONE', #481, #11418, #5328, .T. ) ;
#21482=ADVANCED_FACE ( 'NONE', ( #15146 ), #21, .F. ) ;
#21486=CARTESIAN_POINT ( 'NONE',  ( 10.00000000000000000, 79.66702613806732813, 29.80527447819576636 ) ) ;
#21487=AXIS2_PLACEMENT_3D ( 'NONE', #12034, #7076, #10264 ) ;
#21488=DIRECTION ( 'NONE',  ( 0.000000000000000000, 0.000000000000000000, 1.000000000000000000 ) ) ;
#21490=CIRCLE ( 'NONE', #12303, 92.50100000000003320 ) ;
#21491=DIRECTION ( 'NONE',  ( 0.000000000000000000, 0.9510565162951544194, -0.3090169943749448977 ) ) ;
#21492=CIRCLE ( 'NONE', #3843, 44.99999999999999289 ) ;
#21493=ORIENTED_EDGE ( 'NONE', *, *, #837, .F. ) ;
#21494=EDGE_CURVE ( 'NONE', #20304, #301, #6871, .T. ) ;
#21495=ORIENTED_EDGE ( 'NONE', *, *, #13831, .T. ) ;
#21496=ORIENTED_EDGE ( 'NONE', *, *, #15358, .T. ) ;
#21498=CARTESIAN_POINT ( 'NONE',  ( 0.000000000000000000, 46.93287725819874368, -70.94007663282398823 ) ) ;
#21500=VERTEX_POINT ( 'NONE', #9055 ) ;
#21501=EDGE_CURVE ( 'NONE', #20567, #11727, #5664, .T. ) ;
#21502=DIRECTION ( 'NONE',  ( 0.000000000000000000, 0.06975647374412555224, -0.9975640502598241977 ) ) ;
#21505=DIRECTION ( 'NONE',  ( 1.000000000000000000, 0.000000000000000000, 0.000000000000000000 ) ) ;
#21508=AXIS2_PLACEMENT_3D ( 'NONE', #10455, #3506, #15314 ) ;
#21509=AXIS2_PLACEMENT_3D ( 'NONE', #931, #12532, #4145 ) ;
#21510=AXIS2_PLACEMENT_3D ( 'NONE', #11780, #13435, #13209 ) ;
#21511=ORIENTED_EDGE ( 'NONE', *, *, #6379, .F. ) ;
#21514=ADVANCED_FACE ( 'NONE', ( #14030 ), #20780, .F. ) ;
#21515=CARTESIAN_POINT ( 'NONE',  ( 0.000000000000000000, -87.58454185039434492, -8.540961822682595184 ) ) ;
#21516=VERTEX_POINT ( 'NONE', #15362 ) ;
#21518=VERTEX_POINT ( 'NONE', #13716 ) ;
#21519=CARTESIAN_POINT ( 'NONE',  ( 10.00000000000000000, -85.54350296776125617, 20.64725405482824883 ) ) ;
#21521=EDGE_LOOP ( 'NONE', ( #3765, #18354, #6490, #21524 ) ) ;
#21522=CARTESIAN_POINT ( 'NONE',  ( 0.000000000000000000, 78.01214607583800387, -33.90124636420030413 ) ) ;
#21523=EDGE_CURVE ( 'NONE', #2135, #3522, #10716, .T. ) ;
#21524=ORIENTED_EDGE ( 'NONE', *, *, #4741, .T. ) ;
#21525=ORIENTED_EDGE ( 'NONE', *, *, #17712, .F. ) ;
#21527=LINE ( 'NONE', #16551, #6237 ) ;
#21528=EDGE_CURVE ( 'NONE', #1002, #5874, #5429, .T. ) ;
#21533=EDGE_CURVE ( 'NONE', #19231, #16476, #17026, .T. ) ;
#21534=EDGE_CURVE ( 'NONE', #2262, #11402, #13072, .T. ) ;
#21535=CARTESIAN_POINT ( 'NONE',  ( 10.00000000000000000, 17.64925110578583300, -86.21197095186326464 ) ) ;
#21536=DIRECTION ( 'NONE',  ( 0.000000000000000000, 0.000000000000000000, 1.000000000000000000 ) ) ;
#21538=DIRECTION ( 'NONE',  ( 0.000000000000000000, 0.4067366430757947127, 0.9135454576426031981 ) ) ;
#21540=AXIS2_PLACEMENT_3D ( 'NONE', #19903, #13051, #19797 ) ;
#21543=VERTEX_POINT ( 'NONE', #122 ) ;
#21544=VERTEX_POINT ( 'NONE', #1884 ) ;
#21545=ORIENTED_EDGE ( 'NONE', *, *, #45, .F. ) ;
#21549=CYLINDRICAL_SURFACE ( 'NONE', #6803, 92.50100000000000477 ) ;
#21554=CARTESIAN_POINT ( 'NONE',  ( -10.00000000000000000, 0.000000000000000000, 0.000000000000000000 ) ) ;
#21555=CARTESIAN_POINT ( 'NONE',  ( 10.00000000000000000, 0.000000000000000000, 0.000000000000000000 ) ) ;
#21556=CARTESIAN_POINT ( 'NONE',  ( 0.000000000000000000, 75.45728100697654384, -39.26051685138985903 ) ) ;
#21557=AXIS2_PLACEMENT_3D ( 'NONE', #1494, #13315, #1721 ) ;
#21558=ORIENTED_EDGE ( 'NONE', *, *, #12001, .T. ) ;
#21561=ORIENTED_EDGE ( 'NONE', *, *, #18702, .F. ) ;
#21562=ORIENTED_EDGE ( 'NONE', *, *, #21748, .T. ) ;
#21564=VERTEX_POINT ( 'NONE', #20467 ) ;
#21565=FACE_OUTER_BOUND ( 'NONE', #16548, .T. ) ;
#21566=VERTEX_POINT ( 'NONE', #13600 ) ;
#21567=ORIENTED_EDGE ( 'NONE', *, *, #8798, .T. ) ;
#21568=EDGE_CURVE ( 'NONE', #20538, #19711, #14131, .T. ) ;
#21570=CARTESIAN_POINT ( 'NONE',  ( 0.000000000000000000, -27.00677879428973682, -80.65868421664460186 ) ) ;
#21574=DIRECTION ( 'NONE',  ( -1.000000000000000000, 0.000000000000000000, -0.000000000000000000 ) ) ;
#21576=DIRECTION ( 'NONE',  ( -1.000000000000000000, 0.000000000000000000, 0.000000000000000000 ) ) ;
#21578=DIRECTION ( 'NONE',  ( -1.000000000000000000, 0.000000000000000000, -0.000000000000000000 ) ) ;
#21579=ADVANCED_FACE ( 'NONE', ( #3764 ), #12264, .F. ) ;
#21581=DIRECTION ( 'NONE',  ( 0.000000000000000000, 0.000000000000000000, 1.000000000000000000 ) ) ;
#21585=DIRECTION ( 'NONE',  ( 0.000000000000000000, 0.5877852522924690293, 0.8090169943749504489 ) ) ;
#21586=ORIENTED_EDGE ( 'NONE', *, *, #18957, .T. ) ;
#21587=CARTESIAN_POINT ( 'NONE',  ( 0.000000000000000000, -60.65279801375385915, 63.75921967137595914 ) ) ;
#21588=VERTEX_POINT ( 'NONE', #13923 ) ;
#21589=EDGE_LOOP ( 'NONE', ( #5014, #2158, #8674, #11458 ) ) ;
#21590=DIRECTION ( 'NONE',  ( 1.000000000000000000, 0.000000000000000000, 0.000000000000000000 ) ) ;
#21591=ORIENTED_EDGE ( 'NONE', *, *, #10146, .T. ) ;
#21593=EDGE_CURVE ( 'NONE', #75, #5185, #3877, .T. ) ;
#21594=VERTEX_POINT ( 'NONE', #17143 ) ;
#21595=DIRECTION ( 'NONE',  ( -1.000000000000000000, -0.000000000000000000, -0.000000000000000000 ) ) ;
#21596=DIRECTION ( 'NONE',  ( 1.000000000000000000, 0.000000000000000000, 0.000000000000000000 ) ) ;
#21597=VERTEX_POINT ( 'NONE', #3978 ) ;
#21603=DIRECTION ( 'NONE',  ( -1.000000000000000000, 0.000000000000000000, 0.000000000000000000 ) ) ;
#21604=ORIENTED_EDGE ( 'NONE', *, *, #5736, .F. ) ;
#21605=DIRECTION ( 'NONE',  ( 1.000000000000000000, 0.000000000000000000, 0.000000000000000000 ) ) ;
#21607=AXIS2_PLACEMENT_3D ( 'NONE', #460, #5762, #19237 ) ;
#21608=CARTESIAN_POINT ( 'NONE',  ( 0.000000000000000000, 64.66851233300727131, 55.25552418572984692 ) ) ;
#21610=ADVANCED_FACE ( 'NONE', ( #2210 ), #8945, .F. ) ;
#21612=ORIENTED_EDGE ( 'NONE', *, *, #10758, .F. ) ;
#21613=CARTESIAN_POINT ( 'NONE',  ( 10.00000000000000000, -86.54587337002888603, 15.93147207946976707 ) ) ;
#21620=ORIENTED_EDGE ( 'NONE', *, *, #10310, .F. ) ;
#21622=DIRECTION ( 'NONE',  ( -1.000000000000000000, 0.000000000000000000, 0.000000000000000000 ) ) ;
#21623=ORIENTED_EDGE ( 'NONE', *, *, #2167, .T. ) ;
#21625=EDGE_CURVE ( 'NONE', #4602, #13330, #9903, .T. ) ;
#21626=DIRECTION ( 'NONE',  ( 0.000000000000000000, 0.9848077530122085754, -0.1736481776669272226 ) ) ;
#21628=DIRECTION ( 'NONE',  ( 0.000000000000000000, 0.000000000000000000, 1.000000000000000000 ) ) ;
#21629=DIRECTION ( 'NONE',  ( 0.000000000000000000, 0.000000000000000000, 1.000000000000000000 ) ) ;
#21630=CIRCLE ( 'NONE', #20216, 92.50100000000000477 ) ;
#21631=FACE_OUTER_BOUND ( 'NONE', #9134, .T. ) ;
#21633=AXIS2_PLACEMENT_3D ( 'NONE', #5243, #6905, #20160 ) ;
#21634=CARTESIAN_POINT ( 'NONE',  ( 10.00000000000000000, -81.83745710415297481, 32.35167097270122838 ) ) ;
#21637=EDGE_CURVE ( 'NONE', #1263, #6576, #11341, .T. ) ;
#21638=DIRECTION ( 'NONE',  ( 0.000000000000000000, 0.4694715627858916940, -0.8829475928589264333 ) ) ;
#21640=AXIS2_PLACEMENT_3D ( 'NONE', #20977, #7823, #5852 ) ;
#21641=ORIENTED_EDGE ( 'NONE', *, *, #1122, .F. ) ;
#21643=ORIENTED_EDGE ( 'NONE', *, *, #641, .F. ) ;
#21644=AXIS2_PLACEMENT_3D ( 'NONE', #9991, #16735, #1606 ) ;
#21645=VERTEX_POINT ( 'NONE', #21290 ) ;
#21647=ORIENTED_EDGE ( 'NONE', *, *, #14210, .F. ) ;
#21648=CARTESIAN_POINT ( 'NONE',  ( 10.00000000000000000, -27.87320266523616752, 88.20158487341750231 ) ) ;
#21649=EDGE_CURVE ( 'NONE', #19231, #7150, #10252, .T. ) ;
#21650=ORIENTED_EDGE ( 'NONE', *, *, #15435, .T. ) ;
#21653=AXIS2_PLACEMENT_3D ( 'NONE', #4374, #9125, #11114 ) ;
#21654=FACE_OUTER_BOUND ( 'NONE', #15094, .T. ) ;
#21655=CYLINDRICAL_SURFACE ( 'NONE', #20074, 88.00000000000000000 ) ;
#21657=CARTESIAN_POINT ( 'NONE',  ( 10.00000000000000000, -2.481790431839894673, 92.46770094066590673 ) ) ;
#21658=CARTESIAN_POINT ( 'NONE',  ( 10.00000000000000000, -8.925965667928249303, -92.06933331948791022 ) ) ;
#21659=AXIS2_PLACEMENT_3D ( 'NONE', #16709, #18715, #6686 ) ;
#21660=ORIENTED_EDGE ( 'NONE', *, *, #14627, .F. ) ;
#21663=DIRECTION ( 'NONE',  ( 0.000000000000000000, -0.8660254037844328234, -0.5000000000000101030 ) ) ;
#21664=VERTEX_POINT ( 'NONE', #19851 ) ;
#21667=CYLINDRICAL_SURFACE ( 'NONE', #14480, 45.00000000000000000 ) ;
#21669=ORIENTED_EDGE ( 'NONE', *, *, #13640, .T. ) ;
#21670=DIRECTION ( 'NONE',  ( 0.000000000000000000, 1.850371707708594760E-15, -1.000000000000000000 ) ) ;
#21671=ORIENTED_EDGE ( 'NONE', *, *, #851, .T. ) ;
#21672=ORIENTED_EDGE ( 'NONE', *, *, #13881, .T. ) ;
#21676=VERTEX_POINT ( 'NONE', #19751 ) ;
#21678=VECTOR ( 'NONE', #19147, 1000.000000000000000 ) ;
#21680=CARTESIAN_POINT ( 'NONE',  ( 10.00000000000000000, 0.000000000000000000, 0.000000000000000000 ) ) ;
#21682=FACE_OUTER_BOUND ( 'NONE', #21347, .T. ) ;
#21685=CARTESIAN_POINT ( 'NONE',  ( 10.00000000000000000, 80.18694381077108346, 28.37681241246682973 ) ) ;
#21687=ORIENTED_EDGE ( 'NONE', *, *, #7645, .T. ) ;
#21688=AXIS2_PLACEMENT_3D ( 'NONE', #12805, #16557, #21628 ) ;
#21693=DIRECTION ( 'NONE',  ( 0.000000000000000000, -0.9510565162951503115, -0.3090169943749573322 ) ) ;
#21694=ORIENTED_EDGE ( 'NONE', *, *, #14846, .T. ) ;
#21696=ORIENTED_EDGE ( 'NONE', *, *, #4594, .F. ) ;
#21698=ORIENTED_EDGE ( 'NONE', *, *, #7481, .T. ) ;
#21699=CARTESIAN_POINT ( 'NONE',  ( 10.00000000000000000, -69.25892805976475586, -49.38005998797915908 ) ) ;
#21700=ORIENTED_EDGE ( 'NONE', *, *, #3163, .T. ) ;
#21701=ORIENTED_EDGE ( 'NONE', *, *, #19732, .T. ) ;
#21704=VERTEX_POINT ( 'NONE', #11241 ) ;
#21708=CARTESIAN_POINT ( 'NONE',  ( 10.00000000000000000, 0.000000000000000000, 0.000000000000000000 ) ) ;
#21712=CARTESIAN_POINT ( 'NONE',  ( 10.00000000000000000, 24.89070495400845573, -84.40647372620476574 ) ) ;
#21714=ORIENTED_EDGE ( 'NONE', *, *, #4869, .T. ) ;
#21716=DIRECTION ( 'NONE',  ( 0.000000000000000000, -0.9702957262759939194, -0.2419218955996776110 ) ) ;
#21718=ORIENTED_EDGE ( 'NONE', *, *, #6691, .T. ) ;
#21720=AXIS2_PLACEMENT_3D ( 'NONE', #16395, #8122, #18177 ) ;
#21721=CARTESIAN_POINT ( 'NONE',  ( 0.000000000000000000, 0.000000000000000000, 0.000000000000000000 ) ) ;
#21722=VECTOR ( 'NONE', #17484, 1000.000000000000000 ) ;
#21723=VERTEX_POINT ( 'NONE', #14662 ) ;
#21725=DIRECTION ( 'NONE',  ( 0.000000000000000000, 0.000000000000000000, 1.000000000000000000 ) ) ;
#21728=DIRECTION ( 'NONE',  ( 1.000000000000000000, 0.000000000000000000, -0.000000000000000000 ) ) ;
#21730=ORIENTED_EDGE ( 'NONE', *, *, #11716, .F. ) ;
#21731=CARTESIAN_POINT ( 'NONE',  ( 5.000000000000002665, -79.38136668499764426, 37.98155635597287016 ) ) ;
#21732=ORIENTED_EDGE ( 'NONE', *, *, #15940, .T. ) ;
#21733=EDGE_CURVE ( 'NONE', #16240, #20720, #12718, .T. ) ;
#21734=DIRECTION ( 'NONE',  ( 0.000000000000000000, 0.000000000000000000, 1.000000000000000000 ) ) ;
#21736=CARTESIAN_POINT ( 'NONE',  ( 5.000000000000002665, 6.797690662955227836, 87.73705831432218361 ) ) ;
#21737=AXIS2_PLACEMENT_3D ( 'NONE', #16686, #11829, #13149 ) ;
#21739=SURFACE_STYLE_FILL_AREA ( #19861 ) ;
#21740=AXIS2_PLACEMENT_3D ( 'NONE', #5790, #14172, #12514 ) ;
#21742=CARTESIAN_POINT ( 'NONE',  ( 0.000000000000000000, -68.36541360927154187, -50.60987712331774446 ) ) ;
#21744=DIRECTION ( 'NONE',  ( -1.000000000000000000, -0.000000000000000000, -0.000000000000000000 ) ) ;
#21745=EDGE_CURVE ( 'NONE', #17337, #2668, #6061, .T. ) ;
#21746=DIRECTION ( 'NONE',  ( -1.000000000000000000, 0.000000000000000000, -0.000000000000000000 ) ) ;
#21747=ADVANCED_FACE ( 'NONE', ( #17880 ), #16215, .F. ) ;
#21748=EDGE_CURVE ( 'NONE', #8019, #14362, #3912, .T. ) ;
#21749=DIRECTION ( 'NONE',  ( -1.000000000000000000, -0.000000000000000000, -0.000000000000000000 ) ) ;
#21752=DIRECTION ( 'NONE',  ( 1.000000000000000000, 0.000000000000000000, 0.000000000000000000 ) ) ;
#21755=AXIS2_PLACEMENT_3D ( 'NONE', #13494, #10192, #5336 ) ;
#21759=EDGE_CURVE ( 'NONE', #14362, #13200, #13657, .T. ) ;
#21760=DIRECTION ( 'NONE',  ( 1.000000000000000000, 0.000000000000000000, 0.000000000000000000 ) ) ;
#21763=EDGE_CURVE ( 'NONE', #13276, #7808, #10334, .T. ) ;
#21764=AXIS2_PLACEMENT_3D ( 'NONE', #19454, #21010, #4312 ) ;
#21765=CARTESIAN_POINT ( 'NONE',  ( 10.00000000000000000, 0.000000000000000000, 0.000000000000000000 ) ) ;
#21766=VECTOR ( 'NONE', #13433, 1000.000000000000000 ) ;
#21767=CARTESIAN_POINT ( 'NONE',  ( 0.000000000000000000, 33.95793648385932784, -86.04239391577952745 ) ) ;
#21769=DIRECTION ( 'NONE',  ( 1.000000000000000000, 0.000000000000000000, 0.000000000000000000 ) ) ;
#21770=CARTESIAN_POINT ( 'NONE',  ( 5.000000000000000000, 78.80192417387979731, -39.16958956249220591 ) ) ;
#21772=DIRECTION ( 'NONE',  ( 0.000000000000000000, 0.000000000000000000, 1.000000000000000000 ) ) ;
#21773=ADVANCED_FACE ( 'NONE', ( #8252 ), #8476, .F. ) ;
#21774=ORIENTED_EDGE ( 'NONE', *, *, #12448, .T. ) ;
#21775=ORIENTED_EDGE ( 'NONE', *, *, #3830, .F. ) ;
#21776=VECTOR ( 'NONE', #11258, 1000.000000000000000 ) ;
#21780=CARTESIAN_POINT ( 'NONE',  ( 10.00000000000000000, -78.04699792498111321, -49.64978465107371619 ) ) ;
#21781=ORIENTED_EDGE ( 'NONE', *, *, #4884, .F. ) ;
#21782=VERTEX_POINT ( 'NONE', #15419 ) ;
#21785=DIRECTION ( 'NONE',  ( -1.000000000000000000, -0.000000000000000000, -0.000000000000000000 ) ) ;
#21786=VERTEX_POINT ( 'NONE', #16752 ) ;
#21788=EDGE_CURVE ( 'NONE', #6618, #8570, #10624, .T. ) ;
#21789=DIRECTION ( 'NONE',  ( -1.000000000000000000, 0.000000000000000000, 0.000000000000000000 ) ) ;
#21791=DIRECTION ( 'NONE',  ( 0.000000000000000000, 0.000000000000000000, 1.000000000000000000 ) ) ;
#21792=DIRECTION ( 'NONE',  ( -1.000000000000000000, -0.000000000000000000, -0.000000000000000000 ) ) ;
#21793=EDGE_CURVE ( 'NONE', #14824, #6420, #7450, .T. ) ;
#21794=EDGE_CURVE ( 'NONE', #797, #21353, #13548, .T. ) ;
#21796=DIRECTION ( 'NONE',  ( 0.000000000000000000, 0.000000000000000000, 1.000000000000000000 ) ) ;
#21797=DIRECTION ( 'NONE',  ( 1.000000000000000000, 0.000000000000000000, 0.000000000000000000 ) ) ;
#21799=VECTOR ( 'NONE', #10230, 1000.000000000000000 ) ;
#21801=ORIENTED_EDGE ( 'NONE', *, *, #2179, .F. ) ;
#21802=VECTOR ( 'NONE', #1802, 1000.000000000000000 ) ;
#21803=CARTESIAN_POINT ( 'NONE',  ( 0.000000000000000000, -81.55207211302061410, -24.17537951050148592 ) ) ;
#21805=ORIENTED_EDGE ( 'NONE', *, *, #5270, .T. ) ;
#21806=CARTESIAN_POINT ( 'NONE',  ( 0.000000000000000000, -85.05652083079338865, -0.7600687895868707411 ) ) ;
#21807=ORIENTED_EDGE ( 'NONE', *, *, #21302, .T. ) ;
#21808=CIRCLE ( 'NONE', #646, 92.50099999999999056 ) ;
#21810=EDGE_LOOP ( 'NONE', ( #11101, #15268, #942, #2404 ) ) ;
#21812=ORIENTED_EDGE ( 'NONE', *, *, #6135, .F. ) ;
#21813=VECTOR ( 'NONE', #15718, 1000.000000000000000 ) ;
#21814=VERTEX_POINT ( 'NONE', #20299 ) ;
#21818=AXIS2_PLACEMENT_3D ( 'NONE', #13146, #7967, #8081 ) ;
#21819=EDGE_LOOP ( 'NONE', ( #2946, #19942, #15013, #8860 ) ) ;
#21823=FACE_OUTER_BOUND ( 'NONE', #3943, .T. ) ;
#21828=DIRECTION ( 'NONE',  ( 0.000000000000000000, 0.000000000000000000, 1.000000000000000000 ) ) ;
#21832=CARTESIAN_POINT ( 'NONE',  ( -10.00000000000000000, 0.000000000000000000, 0.000000000000000000 ) ) ;
#21835=DIRECTION ( 'NONE',  ( 0.000000000000000000, 0.000000000000000000, 1.000000000000000000 ) ) ;
#21836=VERTEX_POINT ( 'NONE', #16979 ) ;
#21837=CARTESIAN_POINT ( 'NONE',  ( 0.000000000000000000, 0.000000000000000000, 0.000000000000000000 ) ) ;
#21838=ORIENTED_EDGE ( 'NONE', *, *, #15131, .T. ) ;
#21839=ORIENTED_EDGE ( 'NONE', *, *, #21116, .F. ) ;
#21840=VERTEX_POINT ( 'NONE', #1623 ) ;
#21841=FACE_OUTER_BOUND ( 'NONE', #14687, .T. ) ;
#21842=ORIENTED_EDGE ( 'NONE', *, *, #11627, .T. ) ;
#21843=DIRECTION ( 'NONE',  ( -1.000000000000000000, -0.000000000000000000, 0.000000000000000000 ) ) ;
#21844=CIRCLE ( 'NONE', #19027, 44.99999999999999289 ) ;
#21846=DIRECTION ( 'NONE',  ( 0.000000000000000000, 0.000000000000000000, 1.000000000000000000 ) ) ;
#21849=DIRECTION ( 'NONE',  ( -1.000000000000000000, 0.000000000000000000, 0.000000000000000000 ) ) ;
#21852=AXIS2_PLACEMENT_3D ( 'NONE', #12553, #8905, #740 ) ;
#21853=DIRECTION ( 'NONE',  ( 0.000000000000000000, -0.6946583704590034714, 0.7193398003386451967 ) ) ;
#21854=DIRECTION ( 'NONE',  ( 0.000000000000000000, 0.000000000000000000, 1.000000000000000000 ) ) ;
#21856=ADVANCED_FACE ( 'NONE', ( #1733 ), #5165, .F. ) ;
ENDSEC;
END-ISO-10303-21;
